ISO-10303-21;
HEADER;
FILE_DESCRIPTION (('STEP AP214'),
    '1' );
FILE_NAME ('hex flange nut gradea 1_iso_ISO - 4161 - M10 - N.step',
    '2026-10-08T13:56:24',
    ( '' ),
    ( '' ),
    'SwSTEP 2.0',
    'SolidWorks 2026',
    '' );
FILE_SCHEMA (( 'AUTOMOTIVE_DESIGN' ));
ENDSEC;

DATA;
#3=CARTESIAN_POINT ( 'NONE',  ( -7.500000000000003553, -3.160302461882598557, -7.231849989190477501 ) ) ;
#16=CARTESIAN_POINT ( 'NONE',  ( 7.922281120364393914, 4.573931137438269623, -8.047472243342932430 ) ) ;
#23=SURFACE_STYLE_FILL_AREA ( #9793 ) ;
#29=CARTESIAN_POINT ( 'NONE',  ( -3.033343224707664376, 3.753672977998667726, -2.999999998634409248 ) ) ;
#31=CARTESIAN_POINT ( 'NONE',  ( 0.5093500532425063732, 4.799145180956616130, -5.374999998634406140 ) ) ;
#34=( BOUNDED_CURVE ( )  B_SPLINE_CURVE ( 2, ( #15482, #12870, #10698, #767, #4553, #15316, #15635, #9486, #1883, #6824, #14418 ),
 .UNSPECIFIED., .F., .F. ) 
 B_SPLINE_CURVE_WITH_KNOTS ( ( 3, 2, 2, 2, 2, 3 ),
 ( 0.2545872658012772738, 0.2625000000000000111, 0.2750000000000000222, 0.2874999999999999778, 0.2999999999999999889, 0.3045872658012772627 ),
 .UNSPECIFIED. ) 
 CURVE ( )  GEOMETRIC_REPRESENTATION_ITEM ( )  RATIONAL_B_SPLINE_CURVE ( ( 0.9646335149384808183, 0.9518143178943437865, 1.000000000000000000, 0.9238795325112867385, 1.000000000000000000, 0.9238795325112867385, 1.000000000000000000, 0.9238795325112867385, 1.000000000000000000, 0.9720652146169430630, 0.9646335149384808183 ) ) 
 REPRESENTATION_ITEM ( '' )  );
#41=ORIENTED_EDGE ( 'NONE', *, *, #9292, .F. ) ;
#42=CARTESIAN_POINT ( 'NONE',  ( -1.261996585732579224, 4.276409079477648589, -4.312499998634405252 ) ) ;
#46=CARTESIAN_POINT ( 'NONE',  ( -5.000000000000091482, -0.7223674278660691117, -2.521799365517155334 ) ) ;
#48=CARTESIAN_POINT ( 'NONE',  ( 3.401574460001763001, -4.209348295687703967, 0.9375000027311842787 ) ) ;
#53=CARTESIAN_POINT ( 'NONE',  ( -3.753672977998669946, -3.033343224707661712, -4.749999998634407028 ) ) ;
#64=DIRECTION ( 'NONE',  ( 0.000000000000000000, 0.000000000000000000, 1.000000000000000000 ) ) ;
#66=CARTESIAN_POINT ( 'NONE',  ( -5.000000000000003553, -1.404940523648820476E-14, -7.545263047592946748 ) ) ;
#67=CARTESIAN_POINT ( 'NONE',  ( 4.391654775818395251, -2.390265326283149694, -0.1250000000000035805 ) ) ;
#68=CARTESIAN_POINT ( 'NONE',  ( -4.209348295687703079, -3.401574460001763445, -2.312499997268814944 ) ) ;
#71=CARTESIAN_POINT ( 'NONE',  ( -3.033343224707664376, 3.753672977998667726, -2.249999998634408804 ) ) ;
#89=DIRECTION ( 'NONE',  ( 0.000000000000000000, 0.000000000000000000, 1.000000000000000000 ) ) ;
#95=ORIENTED_EDGE ( 'NONE', *, *, #15170, .F. ) ;
#97=ORIENTED_EDGE ( 'NONE', *, *, #4296, .T. ) ;
#100=EDGE_CURVE ( 'NONE', #1601, #9532, #5846, .T. ) ;
#104=CARTESIAN_POINT ( 'NONE',  ( 0.5093500532425063732, 4.799145180956616130, -2.124999998634406584 ) ) ;
#106=CARTESIAN_POINT ( 'NONE',  ( -3.916244202832140253, 2.131511515620587272, -5.187499998634406140 ) ) ;
#117=CARTESIAN_POINT ( 'NONE',  ( -4.799145180956616130, 0.5093500532425063732, -2.124999998634406584 ) ) ;
#126=CARTESIAN_POINT ( 'NONE',  ( -5.381735091635034607, 0.5711823568785950878, -3.437499997268817609 ) ) ;
#133=CARTESIAN_POINT ( 'NONE',  ( -1.261996585732579224, 4.276409079477648589, -5.062499998634406140 ) ) ;
#146=CARTESIAN_POINT ( 'NONE',  ( -1.306442393143577574, -8.377108146505392483, -7.792327460285857654 ) ) ;
#147=CARTESIAN_POINT ( 'NONE',  ( -2.500000000000011102, 7.216878364870347617, -7.063244554130012176 ) ) ;
#149=CARTESIAN_POINT ( 'NONE',  ( 4.391654775818395251, -2.390265326283149694, -5.125000000000000888 ) ) ;
#153=CARTESIAN_POINT ( 'NONE',  ( -3.033343224707664376, 3.753672977998667726, -1.249999998634407916 ) ) ;
#157=B_SPLINE_CURVE_WITH_KNOTS ( 'NONE', 3,
 ( #8766, #7551, #13667, #2597, #1388, #6333, #11408, #199, #5118 ),
 .UNSPECIFIED., .F., .F.,
 ( 4, 2, 1, 2, 4 ),
 ( 0.000000000000000000, 0.002165063509461097498, 0.004330127018922194995, 0.006495190528383292493, 0.008660254037844389990 ),
 .UNSPECIFIED. ) ;
#169=CARTESIAN_POINT ( 'NONE',  ( 3.753672977998667726, 3.033343224707664820, -3.249999998634409692 ) ) ;
#176=CARTESIAN_POINT ( 'NONE',  ( 3.280815508853480278, 7.221948645665444921, -7.591546097228401457 ) ) ;
#185=DIRECTION ( 'NONE',  ( 1.000000000000000000, 0.000000000000000000, 0.000000000000000000 ) ) ;
#192=CARTESIAN_POINT ( 'NONE',  ( 2.131511515620586383, 3.916244202832140253, -3.187499998634407916 ) ) ;
#195=CARTESIAN_POINT ( 'NONE',  ( 4.799145180956616130, -0.5093500532425063732, -6.624999998634407916 ) ) ;
#197=DIRECTION ( 'NONE',  ( -0.9591083387322728582, -0.2830392103123166025, 0.000000000000000000 ) ) ;
#199=CARTESIAN_POINT ( 'NONE',  ( -7.500000000000000888, -3.608439182435168036, -7.298562697733108173 ) ) ;
#208=CARTESIAN_POINT ( 'NONE',  ( -4.799145180956616130, 0.5093500532425063732, -8.124999998634407916 ) ) ;
#210=CARTESIAN_POINT ( 'NONE',  ( -4.795541693661363958, -1.415196051561583790, -5.374999997268817609 ) ) ;
#215=CARTESIAN_POINT ( 'NONE',  ( -4.209348295687703967, -3.401574460001763001, -5.312499997268816720 ) ) ;
#219=EDGE_LOOP ( 'NONE', ( #418, #2815, #404, #4757, #14320 ) ) ;
#230=CARTESIAN_POINT ( 'NONE',  ( -4.336808689942017736E-16, 9.147862274876558786, -8.047472243342932430 ) ) ;
#239=CARTESIAN_POINT ( 'NONE',  ( -4.391654775818395251, 2.390265326283148806, -5.625000000000001776 ) ) ;
#245=CARTESIAN_POINT ( 'NONE',  ( -4.276409079477644148, -1.261996585732578335, -7.062499998634407916 ) ) ;
#247=DIRECTION ( 'NONE',  ( 0.000000000000000000, 0.000000000000000000, -1.000000000000000000 ) ) ;
#258=CARTESIAN_POINT ( 'NONE',  ( 1.261996585732578113, -4.276409079477644148, -0.5624999986344088043 ) ) ;
#264=CARTESIAN_POINT ( 'NONE',  ( -5.000000000000004441, -1.011557177027151181E-15, -3.545263047592942307 ) ) ;
#271=CARTESIAN_POINT ( 'NONE',  ( 0.000000000000000000, 0.000000000000000000, 0.000000000000000000 ) ) ;
#280=CARTESIAN_POINT ( 'NONE',  ( -3.033343224707664376, 3.753672977998667726, -7.249999998634409692 ) ) ;
#281=CARTESIAN_POINT ( 'NONE',  ( 7.500000000000004441, -4.330127018922205195, -1.000000000000000888 ) ) ;
#282=LINE ( 'NONE', #2509, #5643 ) ;
#289=CARTESIAN_POINT ( 'NONE',  ( 4.799145180956616130, -0.5093500532425063732, -6.624999998634407916 ) ) ;
#294=EDGE_CURVE ( 'NONE', #14177, #3976, #9330, .T. ) ;
#298=CARTESIAN_POINT ( 'NONE',  ( -1.415196051561583790, 4.795541693661363958, -5.624999997268814944 ) ) ;
#299=CARTESIAN_POINT ( 'NONE',  ( 4.209348295687701302, 3.401574460001766109, -8.812499997268812280 ) ) ;
#302=ORIENTED_EDGE ( 'NONE', *, *, #11651, .T. ) ;
#303=CARTESIAN_POINT ( 'NONE',  ( 0.000000000000000000, 0.000000000000000000, 0.000000000000000000 ) ) ;
#309=CARTESIAN_POINT ( 'NONE',  ( -4.613983237546152694, 6.452243898629810737, -7.591546097228399681 ) ) ;
#313=DIRECTION ( 'NONE',  ( 0.000000000000000000, 0.000000000000000000, 1.000000000000000000 ) ) ;
#314=CARTESIAN_POINT ( 'NONE',  ( -5.174575781537456898, -5.672711317431625488, -7.030005583190793494 ) ) ;
#318=CARTESIAN_POINT ( 'NONE',  ( 4.391654775818395251, -2.390265326283149694, -7.125000000000002665 ) ) ;
#322=CARTESIAN_POINT ( 'NONE',  ( 1.261996585732578113, -4.276409079477644148, -6.812499998634407028 ) ) ;
#329=DIRECTION ( 'NONE',  ( 0.000000000000000000, 0.000000000000000000, 1.000000000000000000 ) ) ;
#333=CARTESIAN_POINT ( 'NONE',  ( 3.753672977998667726, 3.033343224707664820, -2.249999998634408804 ) ) ;
#334=CARTESIAN_POINT ( 'NONE',  ( 4.267391354405730475, 1.319746117868581647, -0.3789984458506751586 ) ) ;
#338=LINE ( 'NONE', #12747, #2295 ) ;
#343=ORIENTED_EDGE ( 'NONE', *, *, #4233, .F. ) ;
#355=CARTESIAN_POINT ( 'NONE',  ( 1.261996585732578113, -4.276409079477644148, -3.812499998634408360 ) ) ;
#363=CARTESIAN_POINT ( 'NONE',  ( 4.276409079477644148, 1.261996585732577891, -7.562499998634407916 ) ) ;
#366=( BOUNDED_CURVE ( )  B_SPLINE_CURVE ( 2, ( #11943, #1934, #7944, #15606, #11870, #816, #6883, #8181, #4525, #6731, #5816 ),
 .UNSPECIFIED., .F., .F. ) 
 B_SPLINE_CURVE_WITH_KNOTS ( ( 3, 2, 2, 2, 2, 3 ),
 ( 0.8045872658012773737, 0.8125000000000000000, 0.8249999999999999556, 0.8375000000000000222, 0.8499999999999999778, 0.8545872658012773071 ),
 .UNSPECIFIED. ) 
 CURVE ( )  GEOMETRIC_REPRESENTATION_ITEM ( )  RATIONAL_B_SPLINE_CURVE ( ( 0.9646335149384803742, 0.9518143178943441196, 1.000000000000000000, 0.9238795325112867385, 1.000000000000000000, 0.9238795325112867385, 1.000000000000000000, 0.9238795325112867385, 1.000000000000000000, 0.9720652146169428409, 0.9646335149384808183 ) ) 
 REPRESENTATION_ITEM ( '' )  );
#369=CARTESIAN_POINT ( 'NONE',  ( 4.391654775818395251, -2.390265326283149694, -2.999999997268815832 ) ) ;
#371=CARTESIAN_POINT ( 'NONE',  ( -3.519724167363775358, 2.954775574544003636, -0.2910937876543309155 ) ) ;
#375=CARTESIAN_POINT ( 'NONE',  ( 7.500000000000000888, 1.443375672974059665, -7.063244554130003294 ) ) ;
#380=CARTESIAN_POINT ( 'NONE',  ( -4.209348295687703079, -3.401574460001763445, -0.4375000000000013323 ) ) ;
#383=EDGE_CURVE ( 'NONE', #5937, #2401, #5386, .T. ) ;
#386=CARTESIAN_POINT ( 'NONE',  ( 5.000000000000000000, 0.000000000000000000, 0.000000000000000000 ) ) ;
#389=CARTESIAN_POINT ( 'NONE',  ( -4.209348295687703967, -3.401574460001763001, -6.437500000000003553 ) ) ;
#392=CARTESIAN_POINT ( 'NONE',  ( -3.753672977998669946, -3.033343224707661712, -7.999999998634409692 ) ) ;
#400=EDGE_CURVE ( 'NONE', #3541, #15546, #10896, .T. ) ;
#404=ORIENTED_EDGE ( 'NONE', *, *, #14622, .T. ) ;
#407=CARTESIAN_POINT ( 'NONE',  ( 3.033343224707661712, -3.753672977998669502, -1.499999998634408138 ) ) ;
#408=CARTESIAN_POINT ( 'NONE',  ( 4.458734125001844184, 0.2692756610531124029, -0.3789984458506765463 ) ) ;
#418=ORIENTED_EDGE ( 'NONE', *, *, #14329, .F. ) ;
#429=CARTESIAN_POINT ( 'NONE',  ( -1.415196051561583790, 4.795541693661363958, -0.6249999972688171646 ) ) ;
#431=CARTESIAN_POINT ( 'NONE',  ( 0.000000000000000000, 0.000000000000000000, -25.03750572909317285 ) ) ;
#438=B_SPLINE_CURVE_WITH_KNOTS ( 'NONE', 3,
 ( #10170, #8965, #1830, #1670, #1596, #11449, #6705, #4348, #11608 ),
 .UNSPECIFIED., .F., .F.,
 ( 4, 2, 1, 2, 4 ),
 ( 0.000000000000000000, 0.002165063509461097498, 0.004330127018922194995, 0.006495190528383292493, 0.008660254037844389990 ),
 .UNSPECIFIED. ) ;
#440=CARTESIAN_POINT ( 'NONE',  ( 3.916244202832140253, -2.131511515620588160, -7.687499998634407916 ) ) ;
#442=LINE ( 'NONE', #15389, #913 ) ;
#449=CARTESIAN_POINT ( 'NONE',  ( -1.415196051561583790, 4.795541693661363958, -2.624999997268815388 ) ) ;
#450=CARTESIAN_POINT ( 'NONE',  ( -4.999999999999847233, 1.272547481429013860, -8.461597479913463005 ) ) ;
#456=PLANE ( 'NONE',  #8190 ) ;
#471=CARTESIAN_POINT ( 'NONE',  ( 2.390265326283148806, 4.391654775818395251, -5.875000000000001776 ) ) ;
#474=CARTESIAN_POINT ( 'NONE',  ( -6.902527771671635115, -4.675077770780904807, -0.7026937717022864183 ) ) ;
#477=CARTESIAN_POINT ( 'NONE',  ( -1.261996585732579224, 4.276409079477648589, -7.312499998634407916 ) ) ;
#480=VECTOR ( 'NONE', #9120, 1000.000000000000000 ) ;
#489=CARTESIAN_POINT ( 'NONE',  ( 7.500000000000000000, 4.732328341851992803, -7.493855119309153601 ) ) ;
#490=CARTESIAN_POINT ( 'NONE',  ( -0.5093500532425060401, -4.799145180956616130, -2.624999998634407028 ) ) ;
#495=CARTESIAN_POINT ( 'NONE',  ( 3.033343224707661712, -3.753672977998669946, -5.499999998634407916 ) ) ;
#496=CARTESIAN_POINT ( 'NONE',  ( -7.500000000000000000, -4.330127018922196314, -7.422398894150035176 ) ) ;
#502=DIRECTION ( 'NONE',  ( 1.000000000000000000, 0.000000000000000000, 0.000000000000000000 ) ) ;
#505=CARTESIAN_POINT ( 'NONE',  ( 5.276498195232060873, -6.073236878018049900, -7.633618187056725901 ) ) ;
#507=EDGE_LOOP ( 'NONE', ( #8212, #12137, #15528 ) ) ;
#508=CARTESIAN_POINT ( 'NONE',  ( 7.500000000000001776, 0.000000000000000000, 0.000000000000000000 ) ) ;
#513=VERTEX_POINT ( 'NONE', #14500 ) ;
#520=EDGE_CURVE ( 'NONE', #13539, #6761, #9245, .T. ) ;
#531=CARTESIAN_POINT ( 'NONE',  ( 0.000000000000000000, 0.000000000000000000, 0.000000000000000000 ) ) ;
#532=CARTESIAN_POINT ( 'NONE',  ( 5.000000000000002665, 1.275685995473128912E-14, -4.920263044861760804 ) ) ;
#533=CARTESIAN_POINT ( 'NONE',  ( 4.391654775818395251, -2.390265326283149694, -7.999999997268813168 ) ) ;
#535=CARTESIAN_POINT ( 'NONE',  ( -4.795541693661363958, -1.415196051561583790, -8.374999997268814056 ) ) ;
#540=FACE_OUTER_BOUND ( 'NONE', #7813, .T. ) ;
#541=CARTESIAN_POINT ( 'NONE',  ( 3.753672977998667726, 3.033343224707664376, -8.249999998634409692 ) ) ;
#542=CARTESIAN_POINT ( 'NONE',  ( 5.000000000000004441, 6.350331166892669572E-15, -1.045263047592943417 ) ) ;
#547=CARTESIAN_POINT ( 'NONE',  ( -7.922281120364393914, 4.573931137438272287, -8.047472243342932430 ) ) ;
#553=CARTESIAN_POINT ( 'NONE',  ( -5.381735091635034607, 0.5711823568785950878, -7.562500000000005329 ) ) ;
#557=CARTESIAN_POINT ( 'NONE',  ( -2.131511515620587272, -3.916244202832140253, -5.937499998634407028 ) ) ;
#563=LINE ( 'NONE', #9209, #9705 ) ;
#565=CARTESIAN_POINT ( 'NONE',  ( -5.000000000000092371, -0.7223674278660636716, -6.521799365517155778 ) ) ;
#566=EDGE_CURVE ( 'NONE', #15546, #13370, #8395, .T. ) ;
#567=FACE_OUTER_BOUND ( 'NONE', #4201, .T. ) ;
#568=CARTESIAN_POINT ( 'NONE',  ( -3.916244202832140253, 2.131511515620587272, -3.937499998634404808 ) ) ;
#571=CARTESIAN_POINT ( 'NONE',  ( -2.131511515620587272, -3.916244202832140253, -5.687499998634406140 ) ) ;
#578=ORIENTED_EDGE ( 'NONE', *, *, #400, .F. ) ;
#589=CARTESIAN_POINT ( 'NONE',  ( 2.390265326283148806, 4.391654775818395251, -5.875000000000001776 ) ) ;
#590=CARTESIAN_POINT ( 'NONE',  ( -5.000000000000092371, -0.7223674278660648929, -0.3967993627859714989 ) ) ;
#591=CARTESIAN_POINT ( 'NONE',  ( 4.799145180956616130, -0.5093500532425063732, -7.624999998634408804 ) ) ;
#605=CARTESIAN_POINT ( 'NONE',  ( 4.391654775818395251, -2.390265326283149694, -2.999999997268815832 ) ) ;
#610=CARTESIAN_POINT ( 'NONE',  ( 3.401574460001763001, -4.209348295687703967, -6.062499997268814056 ) ) ;
#625=EDGE_CURVE ( 'NONE', #8156, #9146, #15845, .T. ) ;
#632=CARTESIAN_POINT ( 'NONE',  ( -7.500000000000000888, -4.330127018922199866, -1.000000000000000888 ) ) ;
#634=CARTESIAN_POINT ( 'NONE',  ( 2.131511515620586383, 3.916244202832140253, -0.1874999986344084990 ) ) ;
#635=VERTEX_POINT ( 'NONE', #5988 ) ;
#637=VERTEX_POINT ( 'NONE', #15936 ) ;
#640=CARTESIAN_POINT ( 'NONE',  ( -4.999999999999847233, 1.272547481429013860, -7.586597482644652501 ) ) ;
#643=CARTESIAN_POINT ( 'NONE',  ( 4.391654775818395251, -2.390265326283149694, -6.125000000000001776 ) ) ;
#647=CARTESIAN_POINT ( 'NONE',  ( -3.033343224707664820, 3.753672977998667726, -5.999999998634408804 ) ) ;
#648=CARTESIAN_POINT ( 'NONE',  ( 0.000000000000000000, 0.000000000000000000, -25.03750572909317285 ) ) ;
#650=CARTESIAN_POINT ( 'NONE',  ( -3.033343224707664376, 3.753672977998667726, -5.999999998634407916 ) ) ;
#657=CARTESIAN_POINT ( 'NONE',  ( 0.5711823568785988625, 5.381735091635026613, -6.812500000000005329 ) ) ;
#667=CARTESIAN_POINT ( 'NONE',  ( -4.391654775818395251, 2.390265326283148806, -0.4999999972688171090 ) ) ;
#670=CARTESIAN_POINT ( 'NONE',  ( 4.276409079477644148, 1.261996585732577891, 0.4375000013655920839 ) ) ;
#679=VECTOR ( 'NONE', #15027, 1000.000000000000000 ) ;
#685=CARTESIAN_POINT ( 'NONE',  ( -0.5711823568785978633, -5.381735091635035495, -8.187499997268812280 ) ) ;
#708=ADVANCED_FACE ( 'NONE', ( #9143 ), #8603, .F. ) ;
#709=DIRECTION ( 'NONE',  ( -1.000000000000000000, 0.000000000000000000, 0.000000000000000000 ) ) ;
#710=ADVANCED_FACE ( 'NONE', ( #5496 ), #11549, .F. ) ;
#714=CARTESIAN_POINT ( 'NONE',  ( -3.033343224707664376, 3.753672977998667726, -0.9999999986344076941 ) ) ;
#725=CARTESIAN_POINT ( 'NONE',  ( 7.500000000000698996, -1.614186302713965571, -7.450236204328873235 ) ) ;
#726=CARTESIAN_POINT ( 'NONE',  ( 3.753672977998667726, 3.033343224707664820, -4.249999998634407028 ) ) ;
#729=CARTESIAN_POINT ( 'NONE',  ( -1.261996585732579224, 4.276409079477648589, -6.062499998634407028 ) ) ;
#748=CIRCLE ( 'NONE', #8495, 5.000000000000000888 ) ;
#750=CARTESIAN_POINT ( 'NONE',  ( -2.390265326283148806, -4.391654775818394363, -4.375000000000000000 ) ) ;
#752=CARTESIAN_POINT ( 'NONE',  ( 1.261996585732578113, -4.276409079477644148, -7.812499998634407916 ) ) ;
#753=CARTESIAN_POINT ( 'NONE',  ( -3.753672977998669946, -3.033343224707661712, 1.365593156898739876E-09 ) ) ;
#758=CARTESIAN_POINT ( 'NONE',  ( 0.04606493828582666761, 9.175055303659577888, -8.057411785091799672 ) ) ;
#766=CARTESIAN_POINT ( 'NONE',  ( -2.390265326283148806, -4.391654775818394363, -7.249999997268815832 ) ) ;
#767=CARTESIAN_POINT ( 'NONE',  ( -3.401574460001765221, 4.209348295687701302, -0.6875000000000015543 ) ) ;
#768=DIRECTION ( 'NONE',  ( 0.000000000000000000, 0.000000000000000000, 1.000000000000000000 ) ) ;
#777=CARTESIAN_POINT ( 'NONE',  ( 4.799145180956616130, -0.5093500532425063732, -0.6249999986344092484 ) ) ;
#789=( BOUNDED_CURVE ( )  B_SPLINE_CURVE ( 2, ( #4267, #640, #11924, #7022, #15271, #3296, #14367, #4503, #1998 ),
 .UNSPECIFIED., .F., .F. ) 
 B_SPLINE_CURVE_WITH_KNOTS ( ( 3, 2, 2, 2, 3 ),
 ( 0.9545872658012772849, 0.9625000000000000222, 0.9749999999999999778, 0.9875000000000000444, 1.000000000000000000 ),
 .UNSPECIFIED. ) 
 CURVE ( )  GEOMETRIC_REPRESENTATION_ITEM ( )  RATIONAL_B_SPLINE_CURVE ( ( 0.9646335149384808183, 0.9518143178943441196, 1.000000000000000000, 0.9238795325112867385, 1.000000000000000000, 0.9238795325112867385, 1.000000000000000000, 0.9238795325112867385, 1.000000000000000000 ) ) 
 REPRESENTATION_ITEM ( '' )  );
#791=CARTESIAN_POINT ( 'NONE',  ( -3.753672977998669946, -3.033343224707661712, -1.749999998634408360 ) ) ;
#795=ORIENTED_EDGE ( 'NONE', *, *, #12841, .F. ) ;
#799=EDGE_CURVE ( 'NONE', #3174, #2626, #1489, .T. ) ;
#801=CARTESIAN_POINT ( 'NONE',  ( 7.908230272949474227, -3.123266379892538858, -7.776722524729992259 ) ) ;
#802=CARTESIAN_POINT ( 'NONE',  ( -3.916244202832140253, 2.131511515620587272, -6.937499998634407916 ) ) ;
#805=CARTESIAN_POINT ( 'NONE',  ( 3.753672977998667726, 3.033343224707664376, -6.249999998634408804 ) ) ;
#812=ORIENTED_EDGE ( 'NONE', *, *, #2570, .F. ) ;
#814=LINE ( 'NONE', #5734, #2541 ) ;
#816=CARTESIAN_POINT ( 'NONE',  ( -0.5711823568785977523, -5.381735091635034607, -7.187499997268816720 ) ) ;
#830=CARTESIAN_POINT ( 'NONE',  ( -1.015826369458357803, 8.073766409984798997, -7.642786413620218156 ) ) ;
#838=CARTESIAN_POINT ( 'NONE',  ( -4.795541693661363958, -1.415196051561583790, -7.374999997268815832 ) ) ;
#859=CARTESIAN_POINT ( 'NONE',  ( -2.390265326283148806, -4.391654775818394363, -7.375000000000002665 ) ) ;
#861=B_SPLINE_CURVE_WITH_KNOTS ( 'NONE', 3,
 ( #8485, #2391, #13222, #14609, #9530, #8331, #9837, #7427, #1269, #12332, #13384, #7266, #6214, #11129, #2160, #7340, #3380, #7109, #14533, #10821, #14459, #12245, #12012, #5888, #15761, #12167, #2233, #4911, #9671, #1186, #4672, #7194, #6131, #1034 ),
 .UNSPECIFIED., .F., .F.,
 ( 4, 2, 2, 2, 2, 2, 2, 2, 2, 2, 2, 2, 2, 2, 2, 2, 4 ),
 ( 0.007748559620023459139, 0.008546605054884921782, 0.009344650489746383556, 0.01014269592460784707, 0.01094074135946930884, 0.01173878679433077235, 0.01253683222919223586, 0.01333487766405369590, 0.01413292309891515941, 0.01493096853377662292, 0.01572901396863808643, 0.01652705940349954994, 0.01732510483836101345, 0.01812315027322247696, 0.01892119570808394047, 0.01971924114294540398, 0.02051728657780686749 ),
 .UNSPECIFIED. ) ;
#864=CARTESIAN_POINT ( 'NONE',  ( 3.916244202832140253, -2.131511515620588160, -0.4374999986344086933 ) ) ;
#877=CARTESIAN_POINT ( 'NONE',  ( 7.922281120364393914, 4.573931137438269623, -8.047472243342932430 ) ) ;
#878=CARTESIAN_POINT ( 'NONE',  ( -3.033343224707664820, 3.753672977998667726, -4.999999998634407028 ) ) ;
#882=CARTESIAN_POINT ( 'NONE',  ( 4.795541693661363958, 1.415196051561583790, 0.9999999999999974465 ) ) ;
#884=DIRECTION ( 'NONE',  ( 0.000000000000000000, 0.000000000000000000, -1.000000000000000000 ) ) ;
#892=EDGE_CURVE ( 'NONE', #13370, #11577, #1632, .T. ) ;
#903=CARTESIAN_POINT ( 'NONE',  ( -5.000000000000002665, 1.292545281756915047E-15, -0.4202630448617610814 ) ) ;
#906=ORIENTED_EDGE ( 'NONE', *, *, #15328, .F. ) ;
#908=EDGE_CURVE ( 'NONE', #2200, #11431, #10878, .T. ) ;
#910=FACE_OUTER_BOUND ( 'NONE', #9958, .T. ) ;
#913=VECTOR ( 'NONE', #15309, 1000.000000000000114 ) ;
#915=CARTESIAN_POINT ( 'NONE',  ( -4.209348295687703079, -3.401574460001763445, -3.312499997268815832 ) ) ;
#916=CARTESIAN_POINT ( 'NONE',  ( -0.5093500532425060401, -4.799145180956616130, -0.6249999986344055847 ) ) ;
#919=CARTESIAN_POINT ( 'NONE',  ( 3.753672977998667726, 3.033343224707664376, -1.499999998634408138 ) ) ;
#937=CARTESIAN_POINT ( 'NONE',  ( 0.5711823568785989735, 5.381735091635026613, -0.6874999972688189409 ) ) ;
#941=CARTESIAN_POINT ( 'NONE',  ( -1.261996585732579224, 4.276409079477648589, 0.9375000013655925279 ) ) ;
#942=ORIENTED_EDGE ( 'NONE', *, *, #5179, .F. ) ;
#944=CARTESIAN_POINT ( 'NONE',  ( 1.060314165523342567, 8.048081368954365544, -7.659344964962869540 ) ) ;
#960=CARTESIAN_POINT ( 'NONE',  ( 0.5711823568785989735, 5.381735091635026613, -1.812500000000000888 ) ) ;
#965=CARTESIAN_POINT ( 'NONE',  ( 0.000000000000000000, 0.000000000000000000, 0.000000000000000000 ) ) ;
#969=CARTESIAN_POINT ( 'NONE',  ( -7.500000000000003553, -0.7583608255762881445, -7.446489218764575035 ) ) ;
#987=ORIENTED_EDGE ( 'NONE', *, *, #14160, .T. ) ;
#993=CARTESIAN_POINT ( 'NONE',  ( 3.753672977998667726, 3.033343224707664376, -1.249999998634407916 ) ) ;
#996=CARTESIAN_POINT ( 'NONE',  ( 1.261996585732578113, -4.276409079477644148, -0.8124999986344090264 ) ) ;
#1001=B_SPLINE_CURVE_WITH_KNOTS ( 'NONE', 3,
 ( #3864, #8803, #1524, #1431, #8726, #6461 ),
 .UNSPECIFIED., .F., .F.,
 ( 4, 2, 4 ),
 ( 0.000000000000000000, 0.002307655110370376069, 0.004615310220740751271 ),
 .UNSPECIFIED. ) ;
#1008=CARTESIAN_POINT ( 'NONE',  ( -3.916244202832140253, 2.131511515620587272, -1.187499998634405918 ) ) ;
#1009=AXIS2_PLACEMENT_3D ( 'NONE', #9184, #7818, #10391 ) ;
#1015=CARTESIAN_POINT ( 'NONE',  ( 4.795541693661363958, 1.415196051561583790, 0.1250000027311834461 ) ) ;
#1019=CARTESIAN_POINT ( 'NONE',  ( 4.799145180956616130, -0.5093500532425063732, -4.374999998634405252 ) ) ;
#1020=ORIENTED_EDGE ( 'NONE', *, *, #12841, .T. ) ;
#1032=CARTESIAN_POINT ( 'NONE',  ( 0.5711823568785989735, 5.381735091635026613, 0.1874999999999973355 ) ) ;
#1034=CARTESIAN_POINT ( 'NONE',  ( 4.391654732552941809, -2.390265405775130692, 0.000000000000000000 ) ) ;
#1036=CARTESIAN_POINT ( 'NONE',  ( -3.916244202832140253, 2.131511515620587272, 0.8125000013655924169 ) ) ;
#1041=CARTESIAN_POINT ( 'NONE',  ( -7.500000000000002665, 1.613867362005931172, -7.450195926347909392 ) ) ;
#1052=CARTESIAN_POINT ( 'NONE',  ( 5.000000000000004441, 3.034671531081452754E-15, -0.9202630448617579173 ) ) ;
#1054=CARTESIAN_POINT ( 'NONE',  ( -0.5711823568785977523, -5.381735091635034607, -6.187499997268815832 ) ) ;
#1061=( BOUNDED_CURVE ( )  B_SPLINE_CURVE ( 2, ( #5618, #15561, #3267, #4404, #15486, #8214, #11896, #9412, #14340, #13113, #10702 ),
 .UNSPECIFIED., .F., .F. ) 
 B_SPLINE_CURVE_WITH_KNOTS ( ( 3, 2, 2, 2, 2, 3 ),
 ( 0.3545872658012772516, 0.3624999999999999889, 0.3750000000000000000, 0.3875000000000000111, 0.4000000000000000222, 0.4045872658012772960 ),
 .UNSPECIFIED. ) 
 CURVE ( )  GEOMETRIC_REPRESENTATION_ITEM ( )  RATIONAL_B_SPLINE_CURVE ( ( 0.9646335149384808183, 0.9518143178943437865, 1.000000000000000000, 0.9238795325112867385, 1.000000000000000000, 0.9238795325112867385, 1.000000000000000000, 0.9238795325112867385, 1.000000000000000000, 0.9720652146169428409, 0.9646335149384805963 ) ) 
 REPRESENTATION_ITEM ( '' )  );
#1065=CARTESIAN_POINT ( 'NONE',  ( 2.131511515620586383, 3.916244202832140253, -1.187499998634405918 ) ) ;
#1067=CARTESIAN_POINT ( 'NONE',  ( 0.5093500532425063732, 4.799145180956616130, -2.374999998634407028 ) ) ;
#1078=CARTESIAN_POINT ( 'NONE',  ( 3.033343224707661712, -3.753672977998669502, -4.749999998634407028 ) ) ;
#1079=CONICAL_SURFACE ( 'NONE', #5723, 4.174999999999999822, 0.9599310885968795892 ) ;
#1081=CARTESIAN_POINT ( 'NONE',  ( -3.753672977998669502, -3.033343224707661712, -7.749999998634409692 ) ) ;
#1085=CARTESIAN_POINT ( 'NONE',  ( 2.484690871711851132E-16, -8.716842316802402735, -7.700127545397319473 ) ) ;
#1089=CARTESIAN_POINT ( 'NONE',  ( -4.276409079477644148, -1.261996585732578335, -3.812499998634404808 ) ) ;
#1103=CARTESIAN_POINT ( 'NONE',  ( -0.5711823568785978633, -5.381735091635035495, -2.312500000000001332 ) ) ;
#1107=CARTESIAN_POINT ( 'NONE',  ( -2.131511515620587272, -3.916244202832140253, -1.937499998634406584 ) ) ;
#1113=CARTESIAN_POINT ( 'NONE',  ( -7.500000000000004441, -1.545780083834020102, -7.491787297939580981 ) ) ;
#1116=CARTESIAN_POINT ( 'NONE',  ( 5.000000000000004441, 6.350331166892669572E-15, -1.920263044861758583 ) ) ;
#1128=CARTESIAN_POINT ( 'NONE',  ( -5.000000000000095035, -0.7223674278660573433, -6.396799362785969834 ) ) ;
#1131=ORIENTED_EDGE ( 'NONE', *, *, #15114, .T. ) ;
#1132=( NAMED_UNIT ( * ) SI_UNIT ( $, .STERADIAN. ) SOLID_ANGLE_UNIT ( ) );
#1144=CARTESIAN_POINT ( 'NONE',  ( 3.916244202832140253, -2.131511515620588160, -1.687499998634406362 ) ) ;
#1153=CARTESIAN_POINT ( 'NONE',  ( 3.916244202832140253, -2.131511515620588160, -2.687499998634407028 ) ) ;
#1160=CARTESIAN_POINT ( 'NONE',  ( -7.500000000000000000, -4.330127018922196314, -9.999999999999998224 ) ) ;
#1163=CARTESIAN_POINT ( 'NONE',  ( -5.381735091635034607, 0.5711823568785950878, -1.437499997268815832 ) ) ;
#1167=CARTESIAN_POINT ( 'NONE',  ( 3.753672977998667726, 3.033343224707664376, -6.249999998634408804 ) ) ;
#1178=CARTESIAN_POINT ( 'NONE',  ( 3.750000000000004441, -6.495190528383289141, 0.000000000000000000 ) ) ;
#1184=CARTESIAN_POINT ( 'NONE',  ( -2.390265326283148806, -4.391654775818394363, -2.375000000000002220 ) ) ;
#1185=CARTESIAN_POINT ( 'NONE',  ( -4.795541693661363958, -1.415196051561583790, -2.374999997268815388 ) ) ;
#1186=CARTESIAN_POINT ( 'NONE',  ( 3.585155863502412998, -3.448070198354993732, -0.02305246973459410681 ) ) ;
#1189=CARTESIAN_POINT ( 'NONE',  ( 2.131511515620586383, 3.916244202832140253, -3.437499998634407916 ) ) ;
#1190=EDGE_LOOP ( 'NONE', ( #4329, #9452, #7570 ) ) ;
#1201=CARTESIAN_POINT ( 'NONE',  ( 3.033343224707661712, -3.753672977998669946, -3.749999998634409692 ) ) ;
#1208=FACE_OUTER_BOUND ( 'NONE', #14300, .T. ) ;
#1209=AXIS2_PLACEMENT_3D ( 'NONE', #7335, #14454, #13290 ) ;
#1210=CARTESIAN_POINT ( 'NONE',  ( -2.390265326283148806, -4.391654775818394363, -1.249999997268814278 ) ) ;
#1222=CARTESIAN_POINT ( 'NONE',  ( 4.799145180956616130, -0.5093500532425063732, -2.374999998634407028 ) ) ;
#1224=CARTESIAN_POINT ( 'NONE',  ( 3.916244202832140253, -2.131511515620588160, -4.687499998634405252 ) ) ;
#1234=CARTESIAN_POINT ( 'NONE',  ( -3.753672977998669502, -3.033343224707661712, -3.999999998634410137 ) ) ;
#1236=EDGE_CURVE ( 'NONE', #10448, #4594, #4927, .T. ) ;
#1239=DIRECTION ( 'NONE',  ( 1.000000000000000000, 0.000000000000000000, 0.000000000000000000 ) ) ;
#1241=CARTESIAN_POINT ( 'NONE',  ( 4.391654775818395251, -2.390265326283149694, -2.125000000000001776 ) ) ;
#1245=CARTESIAN_POINT ( 'NONE',  ( 3.401574460001763001, -4.209348295687703967, -0.06249999726881655393 ) ) ;
#1247=CARTESIAN_POINT ( 'NONE',  ( -0.7119955712286091254, 4.450395979295969973, -0.3533432011777784543 ) ) ;
#1250=CARTESIAN_POINT ( 'NONE',  ( -3.753672977998669946, -3.033343224707661712, -2.749999998634409248 ) ) ;
#1267=CARTESIAN_POINT ( 'NONE',  ( -4.391654775818395251, 2.390265326283148806, -1.625000000000001332 ) ) ;
#1268=CARTESIAN_POINT ( 'NONE',  ( 4.391654775818395251, -2.390265326283149694, -1.999999997268814944 ) ) ;
#1269=CARTESIAN_POINT ( 'NONE',  ( -3.864322703872500764, -2.771540215593305323, -0.1764184119287106334 ) ) ;
#1271=CARTESIAN_POINT ( 'NONE',  ( -1.261996585732579224, 4.276409079477648589, -4.312499998634405252 ) ) ;
#1273=CARTESIAN_POINT ( 'NONE',  ( -7.500000000000000888, -4.330127018922199866, -1.000000000000000888 ) ) ;
#1274=ORIENTED_EDGE ( 'NONE', *, *, #11198, .T. ) ;
#1283=CARTESIAN_POINT ( 'NONE',  ( 4.613983237546154470, -6.452243898629821395, -7.591546097228405898 ) ) ;
#1302=CARTESIAN_POINT ( 'NONE',  ( 0.5093500532425063732, 4.799145180956616130, -4.124999998634405252 ) ) ;
#1304=CARTESIAN_POINT ( 'NONE',  ( 3.033343224707661712, -3.753672977998669946, -5.749999998634407916 ) ) ;
#1307=VERTEX_POINT ( 'NONE', #10989 ) ;
#1316=CARTESIAN_POINT ( 'NONE',  ( 3.916244202832140253, -2.131511515620588160, -1.687499998634406362 ) ) ;
#1322=CARTESIAN_POINT ( 'NONE',  ( -4.795541693661363958, -1.415196051561583790, -2.374999997268815388 ) ) ;
#1325=CARTESIAN_POINT ( 'NONE',  ( 5.000000000000003553, 1.275685995473128912E-14, -4.920263044861760804 ) ) ;
#1329=CARTESIAN_POINT ( 'NONE',  ( -3.753672977998669946, -3.033343224707661712, -3.749999998634409692 ) ) ;
#1339=CARTESIAN_POINT ( 'NONE',  ( -1.250000000000010436, 7.938566201357381225, -7.198902722707439139 ) ) ;
#1340=CARTESIAN_POINT ( 'NONE',  ( -5.000000000000004441, -7.530481206757679743E-15, -1.545263047592943861 ) ) ;
#1341=CARTESIAN_POINT ( 'NONE',  ( 4.391654775818395251, -2.390265326283149694, -4.125000000000000000 ) ) ;
#1342=CARTESIAN_POINT ( 'NONE',  ( 5.000000000000093259, 0.7223674278660628945, -4.021799365517152225 ) ) ;
#1347=CARTESIAN_POINT ( 'NONE',  ( 4.276409079477644148, 1.261996585732577891, -2.562499998634407028 ) ) ;
#1355=ORIENTED_EDGE ( 'NONE', *, *, #10703, .F. ) ;
#1357=CIRCLE ( 'NONE', #9608, 10.39117206796836079 ) ;
#1359=CARTESIAN_POINT ( 'NONE',  ( 0.5093500532425063732, 4.799145180956616130, -3.124999998634407472 ) ) ;
#1363=EDGE_CURVE ( 'NONE', #10448, #13539, #8407, .T. ) ;
#1367=CARTESIAN_POINT ( 'NONE',  ( 1.306442393143573577, 8.377108146505383601, -7.792327460285856766 ) ) ;
#1373=CARTESIAN_POINT ( 'NONE',  ( 7.500000000000001776, 4.330127018922190985, -7.564338275809340928 ) ) ;
#1379=CARTESIAN_POINT ( 'NONE',  ( -0.5093500532425060401, -4.799145180956616130, -4.624999998634405252 ) ) ;
#1382=( BOUNDED_CURVE ( )  B_SPLINE_CURVE ( 2, ( #3828, #7804, #6427, #8687, #12696, #2771, #8848, #12624, #13924, #7643, #2687 ),
 .UNSPECIFIED., .F., .F. ) 
 B_SPLINE_CURVE_WITH_KNOTS ( ( 3, 2, 2, 2, 2, 3 ),
 ( 0.5545872658012773737, 0.5625000000000000000, 0.5749999999999999556, 0.5875000000000000222, 0.5999999999999999778, 0.6045872658012773071 ),
 .UNSPECIFIED. ) 
 CURVE ( )  GEOMETRIC_REPRESENTATION_ITEM ( )  RATIONAL_B_SPLINE_CURVE ( ( 0.9646335149384803742, 0.9518143178943441196, 1.000000000000000000, 0.9238795325112867385, 1.000000000000000000, 0.9238795325112867385, 1.000000000000000000, 0.9238795325112867385, 1.000000000000000000, 0.9720652146169428409, 0.9646335149384808183 ) ) 
 REPRESENTATION_ITEM ( '' )  );
#1384=CARTESIAN_POINT ( 'NONE',  ( -0.5093500532425060401, -4.799145180956616130, -4.874999998634405252 ) ) ;
#1386=PLANE ( 'NONE',  #9760 ) ;
#1388=CARTESIAN_POINT ( 'NONE',  ( -7.500000000000003553, -1.084202172485504434E-15, -6.991905250253755533 ) ) ;
#1389=VERTEX_POINT ( 'NONE', #15196 ) ;
#1393=ORIENTED_EDGE ( 'NONE', *, *, #6464, .T. ) ;
#1394=CARTESIAN_POINT ( 'NONE',  ( -4.276409079477644148, -1.261996585732578335, -7.062499998634407916 ) ) ;
#1402=CARTESIAN_POINT ( 'NONE',  ( -0.5711823568785978633, -5.381735091635035495, -5.187499997268819385 ) ) ;
#1403=CARTESIAN_POINT ( 'NONE',  ( 2.390265326283148806, 4.391654775818395251, -8.749999997268814056 ) ) ;
#1404=CARTESIAN_POINT ( 'NONE',  ( 0.2565871882082941813, 4.472639628789296218, -0.3724480747979372897 ) ) ;
#1409=CARTESIAN_POINT ( 'NONE',  ( -0.5093500532425060401, -4.799145180956616130, -7.624999998634408804 ) ) ;
#1415=CARTESIAN_POINT ( 'NONE',  ( -5.276765049035074817, 6.073111908730299824, -7.634085501268424778 ) ) ;
#1421=CARTESIAN_POINT ( 'NONE',  ( -7.500000000000000000, -4.330127018922196314, -7.422398894150035176 ) ) ;
#1422=CARTESIAN_POINT ( 'NONE',  ( -5.147825380260984574, -5.688155668809796062, -7.450218641349908744 ) ) ;
#1423=DIRECTION ( 'NONE',  ( -1.000000000000000000, 0.000000000000000000, 0.000000000000000000 ) ) ;
#1424=CARTESIAN_POINT ( 'NONE',  ( 4.209348295687701302, 3.401574460001765665, -3.937500000000000888 ) ) ;
#1425=CARTESIAN_POINT ( 'NONE',  ( -5.000000000000004441, -7.530481206757679743E-15, -2.545263047592944972 ) ) ;
#1428=CARTESIAN_POINT ( 'NONE',  ( -3.916244202832140253, 2.131511515620587272, -2.187499998634407028 ) ) ;
#1431=CARTESIAN_POINT ( 'NONE',  ( -7.897836333153811950, -1.530409084195006653, -7.633857274177628938 ) ) ;
#1441=VECTOR ( 'NONE', #12812, 1000.000000000000000 ) ;
#1448=CARTESIAN_POINT ( 'NONE',  ( -10.12668159690567649, 1.256356190803088863E-15, -9.999999999999998224 ) ) ;
#1450=CARTESIAN_POINT ( 'NONE',  ( 4.391654775818395251, -2.390265326283149694, -3.125000000000002665 ) ) ;
#1463=ADVANCED_FACE ( 'NONE', ( #5722 ), #7027, .F. ) ;
#1470=CARTESIAN_POINT ( 'NONE',  ( -3.033343224707664376, 3.753672977998667726, -4.249999998634406140 ) ) ;
#1482=CARTESIAN_POINT ( 'NONE',  ( 3.916244202832140253, -2.131511515620588160, -6.687499998634407028 ) ) ;
#1485=EDGE_CURVE ( 'NONE', #14775, #15211, #14382, .T. ) ;
#1489=( BOUNDED_CURVE ( )  B_SPLINE_CURVE ( 2, ( #2657, #7609, #1450, #4196, #11466, #7779, #12749, #5423, #13805, #3955, #264 ),
 .UNSPECIFIED., .F., .F. ) 
 B_SPLINE_CURVE_WITH_KNOTS ( ( 3, 2, 2, 2, 2, 3 ),
 ( 0.5045872658012773293, 0.5124999999999999556, 0.5250000000000000222, 0.5374999999999999778, 0.5500000000000000444, 0.5545872658012773737 ),
 .UNSPECIFIED. ) 
 CURVE ( )  GEOMETRIC_REPRESENTATION_ITEM ( )  RATIONAL_B_SPLINE_CURVE ( ( 0.9646335149384803742, 0.9518143178943441196, 1.000000000000000000, 0.9238795325112867385, 1.000000000000000000, 0.9238795325112867385, 1.000000000000000000, 0.9238795325112867385, 1.000000000000000000, 0.9720652146169423968, 0.9646335149384803742 ) ) 
 REPRESENTATION_ITEM ( '' )  );
#1495=CARTESIAN_POINT ( 'NONE',  ( -1.415196051561583790, 4.795541693661363958, -4.624999997268817609 ) ) ;
#1507=CARTESIAN_POINT ( 'NONE',  ( -4.795541693661363958, -1.415196051561583790, -0.5000000000000004441 ) ) ;
#1514=CARTESIAN_POINT ( 'NONE',  ( -6.658902113225384944, -5.287118297634622266, -7.776713651266041971 ) ) ;
#1516=CARTESIAN_POINT ( 'NONE',  ( 4.209348295687701302, 3.401574460001765665, -4.937500000000001776 ) ) ;
#1517=CARTESIAN_POINT ( 'NONE',  ( 2.390265326283148806, 4.391654775818395251, -2.875000000000002665 ) ) ;
#1519=DIRECTION ( 'NONE',  ( 1.000000000000000000, 0.000000000000000000, 0.000000000000000000 ) ) ;
#1521=AXIS2_PLACEMENT_3D ( 'NONE', #3947, #13886, #15033 ) ;
#1522=CARTESIAN_POINT ( 'NONE',  ( -4.799145180956616130, 0.5093500532425063732, -5.124999998634405252 ) ) ;
#1524=CARTESIAN_POINT ( 'NONE',  ( -7.907996613752308335, -3.055722423191990611, -7.792112796859422374 ) ) ;
#1525=ORIENTED_EDGE ( 'NONE', *, *, #6203, .T. ) ;
#1532=CARTESIAN_POINT ( 'NONE',  ( -1.261996585732579224, 4.276409079477648589, -1.062499998634405696 ) ) ;
#1538=DIRECTION ( 'NONE',  ( 0.000000000000000000, 0.000000000000000000, 1.000000000000000000 ) ) ;
#1540=EDGE_CURVE ( 'NONE', #6438, #8156, #3851, .T. ) ;
#1543=ORIENTED_EDGE ( 'NONE', *, *, #6464, .F. ) ;
#1548=CARTESIAN_POINT ( 'NONE',  ( 7.922281120364393914, -4.573931137438281169, -8.047472243342932430 ) ) ;
#1549=CARTESIAN_POINT ( 'NONE',  ( -4.391654775818395251, 2.390265326283148806, -1.499999997268814500 ) ) ;
#1551=CARTESIAN_POINT ( 'NONE',  ( 5.000000000000095923, 0.7223674278660565662, -6.896799362785969834 ) ) ;
#1553=CARTESIAN_POINT ( 'NONE',  ( 1.261996585732578113, -4.276409079477644148, -4.812499998634405252 ) ) ;
#1564=CARTESIAN_POINT ( 'NONE',  ( 4.799145180956616130, -0.5093500532425063732, -5.624999998634405252 ) ) ;
#1569=CARTESIAN_POINT ( 'NONE',  ( 2.390265326283148806, 4.391654775818395251, -4.749999997268817609 ) ) ;
#1572=CARTESIAN_POINT ( 'NONE',  ( -4.662267971122446397, 0.3223875400172048211, -0.2364825125149292995 ) ) ;
#1581=CARTESIAN_POINT ( 'NONE',  ( -0.5711823568785977523, -5.381735091635034607, -0.3124999999999993339 ) ) ;
#1585=CARTESIAN_POINT ( 'NONE',  ( -2.621086668468696868, -7.606368536631369359, -7.634085501268423890 ) ) ;
#1586=CARTESIAN_POINT ( 'NONE',  ( -6.250000000000015987, 5.051814855409245020, -7.198902722707438251 ) ) ;
#1588=CARTESIAN_POINT ( 'NONE',  ( 4.209348295687701302, 3.401574460001765665, -5.937500000000002665 ) ) ;
#1594=CARTESIAN_POINT ( 'NONE',  ( 3.033343224707661712, -3.753672977998669946, -5.749999998634407916 ) ) ;
#1596=CARTESIAN_POINT ( 'NONE',  ( 3.749999999999999112, 6.495190528383289141, -6.991905250253754645 ) ) ;
#1601=VERTEX_POINT ( 'NONE', #1178 ) ;
#1626=AXIS2_PLACEMENT_3D ( 'NONE', #8984, #1538, #6552 ) ;
#1627=CARTESIAN_POINT ( 'NONE',  ( 0.5711823568785988625, 5.381735091635026613, -5.812500000000000000 ) ) ;
#1629=DIRECTION ( 'NONE',  ( 1.000000000000000000, 0.000000000000000000, 0.000000000000000000 ) ) ;
#1632=B_SPLINE_CURVE_WITH_KNOTS ( 'NONE', 3,
 ( #4131, #5190, #13910, #11635, #6410, #3965 ),
 .UNSPECIFIED., .F., .F.,
 ( 4, 2, 4 ),
 ( 0.000000000000000000, 0.002307655110370372166, 0.004615310220740744332 ),
 .UNSPECIFIED. ) ;
#1633=VERTEX_POINT ( 'NONE', #4983 ) ;
#1637=CARTESIAN_POINT ( 'NONE',  ( -3.033343224707664820, 3.753672977998667726, -6.249999998634408804 ) ) ;
#1639=EDGE_CURVE ( 'NONE', #2543, #5402, #1357, .T. ) ;
#1641=CARTESIAN_POINT ( 'NONE',  ( -2.390265326283148806, -4.391654775818394363, -5.249999997268817609 ) ) ;
#1642=CARTESIAN_POINT ( 'NONE',  ( 1.415196051561583790, -4.795541693661363958, -8.124999997268814056 ) ) ;
#1643=CARTESIAN_POINT ( 'NONE',  ( -4.209348295687703967, -3.401574460001763001, -4.312499997268816720 ) ) ;
#1653=ORIENTED_EDGE ( 'NONE', *, *, #7005, .F. ) ;
#1664=CARTESIAN_POINT ( 'NONE',  ( -4.391654775818395251, 2.390265326283148806, -4.625000000000000888 ) ) ;
#1668=CARTESIAN_POINT ( 'NONE',  ( -2.131511515620587272, -3.916244202832140253, -6.937499998634407916 ) ) ;
#1669=EDGE_LOOP ( 'NONE', ( #11062, #5715, #3885, #9341 ) ) ;
#1670=CARTESIAN_POINT ( 'NONE',  ( 4.999999999999999112, 5.773502691896254646, -7.063244554130000630 ) ) ;
#1680=DIRECTION ( 'NONE',  ( 0.000000000000000000, 0.000000000000000000, 1.000000000000000000 ) ) ;
#1685=CARTESIAN_POINT ( 'NONE',  ( 7.499999999998624212, 3.882635837268421763, -7.781684861373589612 ) ) ;
#1686=CARTESIAN_POINT ( 'NONE',  ( 4.799145180956616130, -0.5093500532425063732, -2.374999998634407028 ) ) ;
#1690=CARTESIAN_POINT ( 'NONE',  ( 4.799145180956616130, -0.5093500532425063732, -5.374999998634406140 ) ) ;
#1696=CARTESIAN_POINT ( 'NONE',  ( 4.599534470798633201, -6.460478697736662390, -7.590212325761508616 ) ) ;
#1697=ORIENTED_EDGE ( 'NONE', *, *, #4108, .T. ) ;
#1703=CARTESIAN_POINT ( 'NONE',  ( 7.897850199329718990, -1.533397866934080644, -7.634054012537967004 ) ) ;
#1705=ADVANCED_FACE ( 'NONE', ( #12327 ), #8721, .F. ) ;
#1710=CARTESIAN_POINT ( 'NONE',  ( 3.916244202832140253, -2.131511515620588160, -7.687499998634407916 ) ) ;
#1719=CARTESIAN_POINT ( 'NONE',  ( 5.000000000000004441, 3.034671531081452754E-15, -0.04526304759294640795 ) ) ;
#1723=CARTESIAN_POINT ( 'NONE',  ( -0.5093500532425060401, -4.799145180956616130, 1.125000001365592306 ) ) ;
#1725=VECTOR ( 'NONE', #10549, 1000.000000000000000 ) ;
#1728=ORIENTED_EDGE ( 'NONE', *, *, #9373, .F. ) ;
#1730=CARTESIAN_POINT ( 'NONE',  ( 7.500000000000000000, 2.886751345948125547, -7.198902722707428481 ) ) ;
#1733=ORIENTED_EDGE ( 'NONE', *, *, #8308, .F. ) ;
#1737=VECTOR ( 'NONE', #15330, 1000.000000000000000 ) ;
#1752=CARTESIAN_POINT ( 'NONE',  ( 3.916244202832140253, -2.131511515620588160, -6.687499998634407028 ) ) ;
#1753=ORIENTED_EDGE ( 'NONE', *, *, #4007, .F. ) ;
#1758=ORIENTED_EDGE ( 'NONE', *, *, #10314, .F. ) ;
#1766=CARTESIAN_POINT ( 'NONE',  ( 5.000000000000003553, 1.275685995473128912E-14, -4.045263047592942307 ) ) ;
#1767=CARTESIAN_POINT ( 'NONE',  ( 7.922798488042200660, -4.627419312545563379, -8.057411459260046982 ) ) ;
#1768=CARTESIAN_POINT ( 'NONE',  ( 4.799145180956616130, -0.5093500532425063732, -6.374999998634408804 ) ) ;
#1769=CARTESIAN_POINT ( 'NONE',  ( 2.982560088675708876, 3.325042182615861375, -0.3789984458506786558 ) ) ;
#1771=CARTESIAN_POINT ( 'NONE',  ( 4.276409079477644148, 1.261996585732577891, -5.312499998634406140 ) ) ;
#1773=FACE_OUTER_BOUND ( 'NONE', #13768, .T. ) ;
#1780=ORIENTED_EDGE ( 'NONE', *, *, #11942, .T. ) ;
#1782=EDGE_CURVE ( 'NONE', #13190, #7075, #6857, .T. ) ;
#1783=CARTESIAN_POINT ( 'NONE',  ( -7.500000000000001776, 4.651022038490038923, -7.928862870699877163 ) ) ;
#1787=VERTEX_POINT ( 'NONE', #386 ) ;
#1791=CARTESIAN_POINT ( 'NONE',  ( -4.999999999999848121, 1.272547481429012750, -0.4615974799134661688 ) ) ;
#1793=CARTESIAN_POINT ( 'NONE',  ( -2.131511515620587272, -3.916244202832140253, -7.937499998634408804 ) ) ;
#1794=CARTESIAN_POINT ( 'NONE',  ( 1.261996585732578113, -4.276409079477644148, 0.1875000013655918341 ) ) ;
#1800=ORIENTED_EDGE ( 'NONE', *, *, #9107, .F. ) ;
#1801=CARTESIAN_POINT ( 'NONE',  ( 4.209348295687701302, 3.401574460001766109, -4.937500000000000888 ) ) ;
#1804=CARTESIAN_POINT ( 'NONE',  ( 4.799145180956616130, -0.5093500532425063732, 1.375000001365592528 ) ) ;
#1807=LINE ( 'NONE', #10626, #4265 ) ;
#1812=CARTESIAN_POINT ( 'NONE',  ( 5.040301471719072168, 5.750234626350511746, -0.09933465333850965973 ) ) ;
#1814=CARTESIAN_POINT ( 'NONE',  ( 4.420982230657666712, -0.5789871446316176007, -0.3789984458506777676 ) ) ;
#1816=VERTEX_POINT ( 'NONE', #7825 ) ;
#1819=CARTESIAN_POINT ( 'NONE',  ( -7.500000000000005329, 0.3744244963005067262, -3.022637072276969577E-15 ) ) ;
#1824=CARTESIAN_POINT ( 'NONE',  ( -3.401574460001764777, 4.209348295687701302, -7.687500000000004441 ) ) ;
#1828=CARTESIAN_POINT ( 'NONE',  ( -2.131511515620587272, -3.916244202832140253, -4.937499998634406140 ) ) ;
#1830=CARTESIAN_POINT ( 'NONE',  ( 6.250000000000000888, 5.051814855409223703, -7.198902722707425816 ) ) ;
#1837=B_SPLINE_CURVE_WITH_KNOTS ( 'NONE', 3,
 ( #5625, #11908, #11598, #4165, #9422, #15333 ),
 .UNSPECIFIED., .F., .F.,
 ( 4, 2, 4 ),
 ( 2.475503369179729800E-07, 0.002222330217055626302, 0.004444412883774334112 ),
 .UNSPECIFIED. ) ;
#1840=CARTESIAN_POINT ( 'NONE',  ( -0.5093500532425060401, -4.799145180956616130, -3.624999998634407916 ) ) ;
#1844=CARTESIAN_POINT ( 'NONE',  ( 1.261996585732578113, -4.276409079477644148, -7.562499998634407916 ) ) ;
#1850=CARTESIAN_POINT ( 'NONE',  ( 4.209348295687701302, 3.401574460001766109, -6.937500000000003553 ) ) ;
#1864=CARTESIAN_POINT ( 'NONE',  ( 4.209348295687701302, 3.401574460001766109, -7.812499997268815832 ) ) ;
#1865=CARTESIAN_POINT ( 'NONE',  ( -5.000000000000003553, -1.404940523648820476E-14, -7.420263044861759028 ) ) ;
#1870=FACE_OUTER_BOUND ( 'NONE', #15786, .T. ) ;
#1874=CARTESIAN_POINT ( 'NONE',  ( -1.415196051561583790, 4.795541693661363958, -4.750000000000000888 ) ) ;
#1881=CARTESIAN_POINT ( 'NONE',  ( 0.5093500532425063732, 4.799145180956616130, 0.6250000013655918618 ) ) ;
#1883=CARTESIAN_POINT ( 'NONE',  ( 4.795541693661363958, 1.415196051561583790, -1.000000000000000888 ) ) ;
#1887=CARTESIAN_POINT ( 'NONE',  ( 7.500000000000000888, 0.3744244963005068927, 1.477225460011500186E-15 ) ) ;
#1891=ORIENTED_EDGE ( 'NONE', *, *, #625, .T. ) ;
#1901=CARTESIAN_POINT ( 'NONE',  ( 6.901579824520445605, -4.675625068323825850, -0.7022220667781389203 ) ) ;
#1903=FACE_OUTER_BOUND ( 'NONE', #4290, .T. ) ;
#1907=CARTESIAN_POINT ( 'NONE',  ( -3.753672977998669946, -3.033343224707661712, -0.7499999986344074721 ) ) ;
#1918=CARTESIAN_POINT ( 'NONE',  ( -4.276409079477644148, -1.261996585732578335, -3.812499998634404808 ) ) ;
#1921=CARTESIAN_POINT ( 'NONE',  ( 4.391654775818395251, -2.390265326283149694, 1.874999999999998224 ) ) ;
#1925=VERTEX_POINT ( 'NONE', #10482 ) ;
#1928=CARTESIAN_POINT ( 'NONE',  ( 5.088535779736900189, -5.722386535632459470, -7.491772860716841897 ) ) ;
#1934=CARTESIAN_POINT ( 'NONE',  ( 4.999999999999845457, -1.272547481429021854, -6.961597479913466557 ) ) ;
#1943=CARTESIAN_POINT ( 'NONE',  ( 5.000000000000003553, 1.275685995473128912E-14, -5.045263047592944083 ) ) ;
#1944=CARTESIAN_POINT ( 'NONE',  ( 3.401574460001763445, -4.209348295687703079, -0.06249999726881656087 ) ) ;
#1946=CARTESIAN_POINT ( 'NONE',  ( 2.500000000000000444, -7.216878364870333407, -7.063244554130006847 ) ) ;
#1947=CARTESIAN_POINT ( 'NONE',  ( -5.000000000000000888, 6.123233995736767268E-16, -25.03750572909317285 ) ) ;
#1952=CARTESIAN_POINT ( 'NONE',  ( -7.112481253774269874, 4.553861071372323543, -7.781689322728262859 ) ) ;
#1960=CARTESIAN_POINT ( 'NONE',  ( 3.401574460001763445, -4.209348295687703079, -8.062499997268812280 ) ) ;
#1962=CARTESIAN_POINT ( 'NONE',  ( -4.391654775818395251, 2.390265326283148806, -6.499999997268815832 ) ) ;
#1972=ORIENTED_EDGE ( 'NONE', *, *, #10703, .T. ) ;
#1977=CARTESIAN_POINT ( 'NONE',  ( 2.131511515620586383, 3.916244202832140253, -0.4374999986344086933 ) ) ;
#1980=CARTESIAN_POINT ( 'NONE',  ( -7.500000000000004441, 2.575910028905296301, -0.3641256808890121488 ) ) ;
#1990=CARTESIAN_POINT ( 'NONE',  ( -0.5093500532425060401, -4.799145180956616130, 1.375000001365592528 ) ) ;
#1998=CARTESIAN_POINT ( 'NONE',  ( 4.795541693661363958, 1.415196051561583790, -8.000000000000003553 ) ) ;
#2001=AXIS2_PLACEMENT_3D ( 'NONE', #431, #4458, #1629 ) ;
#2002=CYLINDRICAL_SURFACE ( 'NONE', #6173, 5.000000000000000888 ) ;
#2003=CARTESIAN_POINT ( 'NONE',  ( -2.131511515620587272, -3.916244202832140253, -4.687499998634405252 ) ) ;
#2004=CARTESIAN_POINT ( 'NONE',  ( 3.750000000000005773, 6.495190528383288253, 0.000000000000000000 ) ) ;
#2005=( BOUNDED_CURVE ( )  B_SPLINE_CURVE ( 2, ( #11690, #4431, #643, #12979, #5568, #15436, #3212, #15588, #11614, #565, #9294 ),
 .UNSPECIFIED., .F., .F. ) 
 B_SPLINE_CURVE_WITH_KNOTS ( ( 3, 2, 2, 2, 2, 3 ),
 ( 0.8045872658012773737, 0.8125000000000000000, 0.8249999999999999556, 0.8375000000000000222, 0.8499999999999999778, 0.8545872658012773071 ),
 .UNSPECIFIED. ) 
 CURVE ( )  GEOMETRIC_REPRESENTATION_ITEM ( )  RATIONAL_B_SPLINE_CURVE ( ( 0.9646335149384803742, 0.9518143178943441196, 1.000000000000000000, 0.9238795325112867385, 1.000000000000000000, 0.9238795325112867385, 1.000000000000000000, 0.9238795325112867385, 1.000000000000000000, 0.9720652146169428409, 0.9646335149384808183 ) ) 
 REPRESENTATION_ITEM ( '' )  );
#2007=CARTESIAN_POINT ( 'NONE',  ( -0.5711823568785978633, -5.381735091635035495, 1.687499999999998446 ) ) ;
#2018=EDGE_CURVE ( 'NONE', #12914, #3405, #5417, .T. ) ;
#2024=COLOUR_RGB ( '', 0.72549020, 0.75294118, 0.79215686) ;
#2038=ORIENTED_EDGE ( 'NONE', *, *, #13694, .F. ) ;
#2043=CARTESIAN_POINT ( 'NONE',  ( 3.753672977998667726, 3.033343224707664376, 0.7500000013655939712 ) ) ;
#2046=CARTESIAN_POINT ( 'NONE',  ( 4.795541693661363958, 1.415196051561583790, -8.874999997268814056 ) ) ;
#2054=ORIENTED_EDGE ( 'NONE', *, *, #4567, .T. ) ;
#2062=CARTESIAN_POINT ( 'NONE',  ( 4.999999999999848121, -1.272547481429015859, -5.086597482644648061 ) ) ;
#2064=ADVANCED_FACE ( 'NONE', ( #11108 ), #13198, .T. ) ;
#2068=CARTESIAN_POINT ( 'NONE',  ( -3.750000000000007550, -6.495190528383289141, 0.000000000000000000 ) ) ;
#2070=CARTESIAN_POINT ( 'NONE',  ( -4.276409079477644148, -1.261996585732578335, -0.8124999986344055847 ) ) ;
#2080=CARTESIAN_POINT ( 'NONE',  ( 0.5093500532425063732, 4.799145180956616130, -4.124999998634405252 ) ) ;
#2082=ADVANCED_FACE ( 'NONE', ( #13358 ), #2300, .T. ) ;
#2085=CARTESIAN_POINT ( 'NONE',  ( -4.799145180956616130, 0.5093500532425063732, -5.874999998634406140 ) ) ;
#2092=ORIENTED_EDGE ( 'NONE', *, *, #908, .F. ) ;
#2097=EDGE_LOOP ( 'NONE', ( #14132, #2475, #14126, #343 ) ) ;
#2098=CARTESIAN_POINT ( 'NONE',  ( 5.000000000000004441, 3.034671531081452754E-15, -0.04526304759294640795 ) ) ;
#2114=DIRECTION ( 'NONE',  ( 1.000000000000000000, 0.000000000000000000, 0.000000000000000000 ) ) ;
#2115=CARTESIAN_POINT ( 'NONE',  ( 3.033343224707661712, -3.753672977998669946, -0.4999999986344072500 ) ) ;
#2117=CARTESIAN_POINT ( 'NONE',  ( -3.033343224707664376, 3.753672977998667726, -0.2499999986344070280 ) ) ;
#2127=EDGE_CURVE ( 'NONE', #9146, #13099, #2187, .T. ) ;
#2132=AXIS2_PLACEMENT_3D ( 'NONE', #8014, #9139, #11311 ) ;
#2138=CARTESIAN_POINT ( 'NONE',  ( 4.391654775818395251, -2.390265326283149694, -0.9999999972688140559 ) ) ;
#2142=CARTESIAN_POINT ( 'NONE',  ( 2.131511515620586383, 3.916244202832140253, -2.187499998634407028 ) ) ;
#2157=DIRECTION ( 'NONE',  ( 1.000000000000000000, 0.000000000000000000, 0.000000000000000000 ) ) ;
#2158=CARTESIAN_POINT ( 'NONE',  ( -3.753672977998669946, -3.033343224707661712, -7.749999998634409692 ) ) ;
#2160=CARTESIAN_POINT ( 'NONE',  ( -2.086913300611921596, -4.342183829375121817, -0.1328488020282359572 ) ) ;
#2167=CARTESIAN_POINT ( 'NONE',  ( -7.500000000000003553, -0.7729939684939154398, -7.026407045654484484 ) ) ;
#2173=AXIS2_PLACEMENT_3D ( 'NONE', #11228, #9857, #14789 ) ;
#2185=ORIENTED_EDGE ( 'NONE', *, *, #5449, .T. ) ;
#2186=CARTESIAN_POINT ( 'NONE',  ( -2.558993250143184461, 7.638875775590766359, -7.593821156097443570 ) ) ;
#2187=( BOUNDED_CURVE ( )  B_SPLINE_CURVE ( 2, ( #12609, #6654, #11564, #3000, #11713, #11403, #9238, #8033, #15127, #1551, #12850 ),
 .UNSPECIFIED., .F., .F. ) 
 B_SPLINE_CURVE_WITH_KNOTS ( ( 3, 2, 2, 2, 2, 3 ),
 ( 0.7545872658012773293, 0.7624999999999999556, 0.7750000000000000222, 0.7874999999999999778, 0.8000000000000000444, 0.8045872658012773737 ),
 .UNSPECIFIED. ) 
 CURVE ( )  GEOMETRIC_REPRESENTATION_ITEM ( )  RATIONAL_B_SPLINE_CURVE ( ( 0.9646335149384803742, 0.9518143178943441196, 1.000000000000000000, 0.9238795325112867385, 1.000000000000000000, 0.9238795325112867385, 1.000000000000000000, 0.9238795325112867385, 1.000000000000000000, 0.9720652146169423968, 0.9646335149384803742 ) ) 
 REPRESENTATION_ITEM ( '' )  );
#2192=CARTESIAN_POINT ( 'NONE',  ( 0.000000000000000000, 0.000000000000000000, 0.000000000000000000 ) ) ;
#2194=CARTESIAN_POINT ( 'NONE',  ( -2.131511515620587272, -3.916244202832140253, -0.6874999986344054737 ) ) ;
#2197=CARTESIAN_POINT ( 'NONE',  ( -4.799145180956616130, 0.5093500532425063732, -3.124999998634407916 ) ) ;
#2200=VERTEX_POINT ( 'NONE', #10441 ) ;
#2208=CARTESIAN_POINT ( 'NONE',  ( -4.799145180956616130, 0.5093500532425063732, -3.124999998634407472 ) ) ;
#2215=CARTESIAN_POINT ( 'NONE',  ( 4.795541693661363958, 1.415196051561583790, 1.125000002731184390 ) ) ;
#2217=EDGE_CURVE ( 'NONE', #14425, #7414, #5929, .T. ) ;
#2219=CARTESIAN_POINT ( 'NONE',  ( 2.131511515620586383, 3.916244202832140253, -4.187499998634405252 ) ) ;
#2221=CARTESIAN_POINT ( 'NONE',  ( -0.04725809328185331254, 9.175759667312515688, -8.057670357645360326 ) ) ;
#2222=ORIENTED_EDGE ( 'NONE', *, *, #1236, .F. ) ;
#2233=CARTESIAN_POINT ( 'NONE',  ( 2.521252210804794114, -4.248023353278823855, -0.04711480227235904233 ) ) ;
#2236=CARTESIAN_POINT ( 'NONE',  ( 4.209348295687701302, 3.401574460001765665, -2.937500000000003109 ) ) ;
#2237=CARTESIAN_POINT ( 'NONE',  ( -5.000000000000000888, 6.123233995736767268E-16, -9.999999999999998224 ) ) ;
#2238=EDGE_CURVE ( 'NONE', #12516, #1307, #11996, .T. ) ;
#2242=CARTESIAN_POINT ( 'NONE',  ( -2.131511515620587272, -3.916244202832140253, 1.062500001365592528 ) ) ;
#2247=VERTEX_POINT ( 'NONE', #1943 ) ;
#2248=CARTESIAN_POINT ( 'NONE',  ( -7.908219015560236542, -3.084967917786102465, -7.795665562178456298 ) ) ;
#2251=ORIENTED_EDGE ( 'NONE', *, *, #8326, .F. ) ;
#2255=AXIS2_PLACEMENT_3D ( 'NONE', #2576, #7849, #2655 ) ;
#2263=ADVANCED_FACE ( 'NONE', ( #5824 ), #1079, .F. ) ;
#2278=CARTESIAN_POINT ( 'NONE',  ( -1.261996585732579224, 4.276409079477648589, -1.062499998634405696 ) ) ;
#2283=CARTESIAN_POINT ( 'NONE',  ( 3.033343224707661712, -3.753672977998669946, -1.749999998634408360 ) ) ;
#2294=CARTESIAN_POINT ( 'NONE',  ( 1.261996585732578113, -4.276409079477644148, -3.812499998634408360 ) ) ;
#2295=VECTOR ( 'NONE', #11312, 1000.000000000000000 ) ;
#2296=CIRCLE ( 'NONE', #1009, 10.12668159690567649 ) ;
#2300=PLANE ( 'NONE',  #7028 ) ;
#2303=CARTESIAN_POINT ( 'NONE',  ( 4.209348295687701302, 3.401574460001765665, -1.812499997268814278 ) ) ;
#2307=CARTESIAN_POINT ( 'NONE',  ( -1.261996585732579224, 4.276409079477648589, -3.062499998634407472 ) ) ;
#2312=ORIENTED_EDGE ( 'NONE', *, *, #383, .T. ) ;
#2320=CARTESIAN_POINT ( 'NONE',  ( 4.795541693661363958, 1.415196051561583790, -3.469446951953614189E-15 ) ) ;
#2324=CARTESIAN_POINT ( 'NONE',  ( 3.033343224707661712, -3.753672977998669946, -0.7499999986344074721 ) ) ;
#2347=ORIENTED_EDGE ( 'NONE', *, *, #5359, .F. ) ;
#2355=CARTESIAN_POINT ( 'NONE',  ( -3.753672977998669946, -3.033343224707661712, -1.999999998634408360 ) ) ;
#2363=CARTESIAN_POINT ( 'NONE',  ( 3.916244202832140253, -2.131511515620588160, -3.687499998634407916 ) ) ;
#2368=CYLINDRICAL_SURFACE ( 'NONE', #3075, 5.000000000000000888 ) ;
#2373=CARTESIAN_POINT ( 'NONE',  ( -5.381735091635034607, 0.5711823568785950878, 0.5625000027311820583 ) ) ;
#2376=CARTESIAN_POINT ( 'NONE',  ( -4.276409079477644148, -1.261996585732578335, -4.812499998634405252 ) ) ;
#2389=CARTESIAN_POINT ( 'NONE',  ( -4.391654775818395251, 2.390265326283148806, -0.6250000000000005551 ) ) ;
#2391=CARTESIAN_POINT ( 'NONE',  ( -4.678271028438514278, -0.2656286248631474223, -0.2252770511478082716 ) ) ;
#2393=CARTESIAN_POINT ( 'NONE',  ( -3.753672977998669946, -3.033343224707661712, -2.999999998634409248 ) ) ;
#2400=LINE ( 'NONE', #12258, #3251 ) ;
#2401=VERTEX_POINT ( 'NONE', #7526 ) ;
#2410=CARTESIAN_POINT ( 'NONE',  ( 4.276409079477644148, 1.261996585732577891, -8.562499998634409692 ) ) ;
#2423=CARTESIAN_POINT ( 'NONE',  ( 3.916244202832140253, -2.131511515620588160, -2.437499998634407028 ) ) ;
#2425=CARTESIAN_POINT ( 'NONE',  ( 0.5093500532425063732, 4.799145180956616130, -1.374999998634406140 ) ) ;
#2437=ORIENTED_EDGE ( 'NONE', *, *, #520, .F. ) ;
#2438=CARTESIAN_POINT ( 'NONE',  ( 3.753672977998667726, 3.033343224707664820, -2.499999998634408804 ) ) ;
#2445=CARTESIAN_POINT ( 'NONE',  ( -5.381735091635034607, 0.5711823568785950878, -0.4374999972688187744 ) ) ;
#2448=CARTESIAN_POINT ( 'NONE',  ( 0.5789871446316211534, 4.420982230657665824, -0.3789984458506777676 ) ) ;
#2452=CARTESIAN_POINT ( 'NONE',  ( -4.799145180956616130, 0.5093500532425063732, -4.874999998634405252 ) ) ;
#2454=VERTEX_POINT ( 'NONE', #9694 ) ;
#2460=FACE_OUTER_BOUND ( 'NONE', #13479, .T. ) ;
#2465=CARTESIAN_POINT ( 'NONE',  ( -4.209348295687703967, -3.401574460001763001, -2.437500000000003109 ) ) ;
#2470=ADVANCED_FACE ( 'NONE', ( #1208 ), #15864, .T. ) ;
#2471=CARTESIAN_POINT ( 'NONE',  ( 3.753672977998667726, 3.033343224707664376, -3.499999998634410137 ) ) ;
#2474=VERTEX_POINT ( 'NONE', #11146 ) ;
#2475=ORIENTED_EDGE ( 'NONE', *, *, #3082, .T. ) ;
#2489=CARTESIAN_POINT ( 'NONE',  ( 4.391654775818395251, -2.390265326283149694, -0.9999999972688140559 ) ) ;
#2492=CARTESIAN_POINT ( 'NONE',  ( 2.621086668468695979, 7.606368536631366695, -7.634085501268425666 ) ) ;
#2494=EDGE_LOOP ( 'NONE', ( #3249, #2943, #8099, #7599 ) ) ;
#2503=CARTESIAN_POINT ( 'NONE',  ( -4.276409079477644148, -1.261996585732578335, -3.812499998634404808 ) ) ;
#2505=( BOUNDED_CURVE ( )  B_SPLINE_CURVE ( 2, ( #2985, #9145, #12992, #4199, #15526, #657, #12916, #1850, #14058, #9224, #5582 ),
 .UNSPECIFIED., .F., .F. ) 
 B_SPLINE_CURVE_WITH_KNOTS ( ( 3, 2, 2, 2, 2, 3 ),
 ( 0.8545872658012773071, 0.8625000000000000444, 0.8750000000000000000, 0.8874999999999999556, 0.9000000000000000222, 0.9045872658012773515 ),
 .UNSPECIFIED. ) 
 CURVE ( )  GEOMETRIC_REPRESENTATION_ITEM ( )  RATIONAL_B_SPLINE_CURVE ( ( 0.9646335149384808183, 0.9518143178943441196, 1.000000000000000000, 0.9238795325112867385, 1.000000000000000000, 0.9238795325112867385, 1.000000000000000000, 0.9238795325112867385, 1.000000000000000000, 0.9720652146169423968, 0.9646335149384803742 ) ) 
 REPRESENTATION_ITEM ( '' )  );
#2506=CARTESIAN_POINT ( 'NONE',  ( 3.753672977998667726, 3.033343224707664376, -5.499999998634407916 ) ) ;
#2509=CARTESIAN_POINT ( 'NONE',  ( 4.276409079477644148, 1.261996585732577891, -8.437499998634409692 ) ) ;
#2517=VERTEX_POINT ( 'NONE', #2575 ) ;
#2518=CARTESIAN_POINT ( 'NONE',  ( -3.033343224707664820, 3.753672977998667726, -3.249999998634409692 ) ) ;
#2521=AXIS2_PLACEMENT_3D ( 'NONE', #7583, #12483, #1423 ) ;
#2522=ADVANCED_FACE ( 'NONE', ( #8896 ), #2898, .F. ) ;
#2524=CARTESIAN_POINT ( 'NONE',  ( 3.753672977998667726, 3.033343224707664820, -8.249999998634409692 ) ) ;
#2527=UNCERTAINTY_MEASURE_WITH_UNIT (LENGTH_MEASURE( 1.000000000000000082E-05 ), #14882, 'distance_accuracy_value', 'NONE');
#2530=CARTESIAN_POINT ( 'NONE',  ( -5.381735091635034607, 0.5711823568785950878, -2.437499997268816276 ) ) ;
#2536=CARTESIAN_POINT ( 'NONE',  ( 0.5093500532425063732, 4.799145180956616130, -4.124999998634405252 ) ) ;
#2541=VECTOR ( 'NONE', #14062, 1000.000000000000000 ) ;
#2543=VERTEX_POINT ( 'NONE', #14051 ) ;
#2553=CARTESIAN_POINT ( 'NONE',  ( 5.381735091635035495, -0.5711823568785978633, -1.062500000000000222 ) ) ;
#2557=CARTESIAN_POINT ( 'NONE',  ( -0.5093500532425060401, -4.799145180956616130, -3.874999998634408360 ) ) ;
#2570=EDGE_CURVE ( 'NONE', #4563, #14394, #14155, .T. ) ;
#2572=CARTESIAN_POINT ( 'NONE',  ( 3.753672977998667726, 3.033343224707664820, -1.249999998634407916 ) ) ;
#2575=CARTESIAN_POINT ( 'NONE',  ( 5.000000000000004441, -2.247904837838113790E-16, -3.920263044861760360 ) ) ;
#2576=CARTESIAN_POINT ( 'NONE',  ( 0.000000000000000000, 0.000000000000000000, 0.000000000000000000 ) ) ;
#2587=FACE_OUTER_BOUND ( 'NONE', #9380, .T. ) ;
#2590=CARTESIAN_POINT ( 'NONE',  ( -4.795541693661363958, -1.415196051561583790, -4.374999997268816720 ) ) ;
#2591=CARTESIAN_POINT ( 'NONE',  ( 3.033343224707661712, -3.753672977998669946, -4.499999998634407028 ) ) ;
#2593=CARTESIAN_POINT ( 'NONE',  ( 3.916244202832140253, -2.131511515620588160, -6.687499998634407028 ) ) ;
#2597=CARTESIAN_POINT ( 'NONE',  ( -7.500000000000003553, 1.443375672974063662, -7.063244554130003294 ) ) ;
#2602=DIRECTION ( 'NONE',  ( 0.000000000000000000, 0.000000000000000000, 1.000000000000000000 ) ) ;
#2605=CARTESIAN_POINT ( 'NONE',  ( -2.131511515620587272, -3.916244202832140253, -5.937499998634407028 ) ) ;
#2612=CARTESIAN_POINT ( 'NONE',  ( 3.401574460001763001, -4.209348295687703967, -5.062499997268816720 ) ) ;
#2616=VERTEX_POINT ( 'NONE', #12746 ) ;
#2618=CARTESIAN_POINT ( 'NONE',  ( -0.5093500532425060401, -4.799145180956616130, -6.624999998634407916 ) ) ;
#2626=VERTEX_POINT ( 'NONE', #5726 ) ;
#2631=CARTESIAN_POINT ( 'NONE',  ( -2.621328321947914208, -7.606199919102974327, -7.633618187056795179 ) ) ;
#2633=CARTESIAN_POINT ( 'NONE',  ( -5.381735091635034607, 0.5711823568785950878, -3.562499999999998224 ) ) ;
#2638=CARTESIAN_POINT ( 'NONE',  ( 4.276409079477644148, 1.261996585732577891, -1.562499998634406140 ) ) ;
#2652=CARTESIAN_POINT ( 'NONE',  ( 4.458734124999998549, -3.052311964297492742E-11, -0.3789984458506765463 ) ) ;
#2655=DIRECTION ( 'NONE',  ( 1.000000000000000000, -4.440892098500626162E-15, 0.000000000000000000 ) ) ;
#2657=CARTESIAN_POINT ( 'NONE',  ( 5.000000000000004441, -2.247904837838113790E-16, -3.045263047592945860 ) ) ;
#2661=ORIENTED_EDGE ( 'NONE', *, *, #14112, .F. ) ;
#2672=CARTESIAN_POINT ( 'NONE',  ( -4.799145180956616130, 0.5093500532425063732, -7.124999998634407916 ) ) ;
#2674=CARTESIAN_POINT ( 'NONE',  ( 7.500000000000001776, 0.000000000000000000, 0.000000000000000000 ) ) ;
#2677=EDGE_CURVE ( 'NONE', #4915, #3061, #10820, .T. ) ;
#2681=COLOUR_RGB ( '', 0.72549020, 0.75294118, 0.79215686) ;
#2682=ORIENTED_EDGE ( 'NONE', *, *, #12641, .T. ) ;
#2684=CARTESIAN_POINT ( 'NONE',  ( -1.261996585732579224, 4.276409079477648589, -5.312499998634406140 ) ) ;
#2687=CARTESIAN_POINT ( 'NONE',  ( 5.000000000000002665, 1.275685995473128912E-14, -4.920263044861760804 ) ) ;
#2690=PRODUCT_DEFINITION_CONTEXT ( 'detailed design', #15187, 'design' ) ;
#2693=CARTESIAN_POINT ( 'NONE',  ( -3.401574460001764777, 4.209348295687701302, -5.562499997268814056 ) ) ;
#2700=CARTESIAN_POINT ( 'NONE',  ( 3.916244202832140253, -2.131511515620588160, -6.437499998634407028 ) ) ;
#2706=( BOUNDED_SURFACE ( )  B_SPLINE_SURFACE ( 1, 2, ( 
 ( #6810, #15300, #8408, #6895, #7196, #13987, #2242, #12097, #14169, #3098, #1036, #11719, #12854, #5971, #10892, #10371, #670, #4135, #11801, #9083, #1794, #6742, #11642, #753, #10446, #15468, #4389, #2919, #6657, #9321, #14244, #10615, #15543, #9840, #8801, #2324, #15835, #15915, #9761, #9914, #14854, #4835, #7268, #153, #13705, #14698, #7342, #4753, #2638, #9674, #12169, #11132, #14945, #12488, #1107, #3532, #6048, #8564, #1428, #71, #13386, #6375, #7510, #13534, #1347, #13452, #14613, #3620, #6133, #8489, #10974, #2393, #7591, #3862, #10004, #12411, #3776, #12249, #1189, #2471, #12334, #11061, #7430, #1201, #6216, #2557, #4914, #6294, #14771, #3693, #8639, #4989, #1271, #8723, #13628, #11209, #5074, #15019, #11606, #12896, #13950, #4177, #1828, #14123, #11372, #1522, #2958, #4098, #9122, #11446, #11526, #7909, #5163, #9202, #2807, #1594, #10337, #5232, #557, #2717, #15263, #11293, #13873, #12653, #7834, #12810, #9047, #10168, #12729, #6459, #1752, #7996, #322, #3934, #1668, #15091, #245, #7762, #10092, #5477, #477, #6703, #6610, #3050, #7675, #8878, #10406, #4011, #13784, #12573, #8963, #392, #5401, #6532, #5313, #10256, #14032, #15342, #4258, #15180, #2881 ),
 ( #10803, #11916, #9582, #15743, #9285, #1990, #4346, #9432, #14360, #10723, #3433, #14206, #941, #4655, #6851, #3130, #4575, #8152, #11991, #14512, #11681, #13136, #5870, #8236, #8387, #13277, #6773, #15425, #3289, #11758, #634, #8314, #9510, #5555, #864, #10492, #8074, #12970, #6939, #1907, #2070, #7014, #15658, #714, #5637, #10580, #15505, #4421, #9356, #14442, #13049, #14281, #3203, #11842, #5785, #791, #3367, #5711, #10646, #15580, #4497, #13203, #2142, #7090, #3842, #14923, #7173, #11188, #6273, #12393, #9896, #1250, #5053, #13366, #10523, #14751, #2307, #4897, #7252, #8621, #4969, #12075, #8702, #12152, #8785, #14676, #7407, #1329, #1089, #6030, #6111, #15816, #5952, #2536, #2219, #9822, #11115, #1019, #9983, #10952, #8467, #14835, #11038, #53, #2376, #2452, #3753, #10872, #133, #9737, #8548, #6198, #15894, #7490, #9653, #13605, #4731, #4815, #3601, #3674, #14588, #13514, #13436, #12311, #7324, #3509, #12228, #1167, #6354, #15159, #2700, #4236, #10149, #2618, #14011, #13933, #15246, #4076, #5458, #5144, #13687, #2936, #8860, #12470, #10388, #7572, #2785, #7815, #5214, #1409, #12554, #10234, #5378, #12709, #15073, #7743, #12634, #6590, #11273, #541, #13766 ) ),
 .UNSPECIFIED., .F., .F., .F. ) 
 B_SPLINE_SURFACE_WITH_KNOTS ( ( 2, 2 ),
 ( 3, 2, 2, 2, 2, 2, 2, 2, 2, 2, 2, 2, 2, 2, 2, 2, 2, 2, 2, 2, 2, 2, 2, 2, 2, 2, 2, 2, 2, 2, 2, 2, 2, 2, 2, 2, 2, 2, 2, 2, 2, 2, 2, 2, 2, 2, 2, 2, 2, 2, 2, 2, 2, 2, 2, 2, 2, 2, 2, 2, 2, 2, 2, 2, 2, 2, 2, 2, 2, 2, 2, 2, 2, 2, 2, 2, 2, 2, 2, 2, 3 ),
 ( 0.000000000000000000, 1.000000000000000000 ),
 ( 0.000000000000000000, 0.01250000000000000069, 0.02500000000000000139, 0.03749999999999999861, 0.05000000000000000278, 0.06250000000000000000, 0.07499999999999999722, 0.08749999999999999445, 0.1000000000000000056, 0.1125000000000000028, 0.1250000000000000000, 0.1375000000000000111, 0.1499999999999999944, 0.1625000000000000056, 0.1749999999999999889, 0.1875000000000000000, 0.2000000000000000111, 0.2124999999999999944, 0.2250000000000000056, 0.2374999999999999889, 0.2500000000000000000, 0.2625000000000000111, 0.2750000000000000222, 0.2874999999999999778, 0.2999999999999999889, 0.3125000000000000000, 0.3250000000000000111, 0.3375000000000000222, 0.3499999999999999778, 0.3624999999999999889, 0.3750000000000000000, 0.3875000000000000111, 0.4000000000000000222, 0.4124999999999999778, 0.4249999999999999889, 0.4375000000000000000, 0.4500000000000000111, 0.4625000000000000222, 0.4749999999999999778, 0.4874999999999999889, 0.5000000000000000000, 0.5124999999999999556, 0.5250000000000000222, 0.5374999999999999778, 0.5500000000000000444, 0.5625000000000000000, 0.5749999999999999556, 0.5875000000000000222, 0.5999999999999999778, 0.6125000000000000444, 0.6250000000000000000, 0.6374999999999999556, 0.6500000000000000222, 0.6624999999999999778, 0.6750000000000000444, 0.6875000000000000000, 0.6999999999999999556, 0.7125000000000000222, 0.7249999999999999778, 0.7375000000000000444, 0.7500000000000000000, 0.7624999999999999556, 0.7750000000000000222, 0.7874999999999999778, 0.8000000000000000444, 0.8125000000000000000, 0.8249999999999999556, 0.8375000000000000222, 0.8499999999999999778, 0.8625000000000000444, 0.8750000000000000000, 0.8874999999999999556, 0.9000000000000000222, 0.9124999999999999778, 0.9250000000000000444, 0.9375000000000000000, 0.9499999999999999556, 0.9625000000000000222, 0.9749999999999999778, 0.9875000000000000444, 1.000000000000000000 ),
 .UNSPECIFIED. ) 
 GEOMETRIC_REPRESENTATION_ITEM ( )  RATIONAL_B_SPLINE_SURFACE ( (
 ( 1.000000000000000000, 0.9238795325112867385, 1.000000000000000000, 0.9238795325112867385, 1.000000000000000000, 0.9238795325112867385, 1.000000000000000000, 0.9238795325112867385, 1.000000000000000000, 0.9238795325112867385, 1.000000000000000000, 0.9238795325112867385, 1.000000000000000000, 0.9238795325112867385, 1.000000000000000000, 0.9238795325112867385, 1.000000000000000000, 0.9238795325112867385, 1.000000000000000000, 0.9238795325112867385, 1.000000000000000000, 0.9238795325112867385, 1.000000000000000000, 0.9238795325112867385, 1.000000000000000000, 0.9238795325112867385, 1.000000000000000000, 0.9238795325112867385, 1.000000000000000000, 0.9238795325112867385, 1.000000000000000000, 0.9238795325112867385, 1.000000000000000000, 0.9238795325112867385, 1.000000000000000000, 0.9238795325112867385, 1.000000000000000000, 0.9238795325112867385, 1.000000000000000000, 0.9238795325112867385, 1.000000000000000000, 0.9238795325112867385, 1.000000000000000000, 0.9238795325112867385, 1.000000000000000000, 0.9238795325112867385, 1.000000000000000000, 0.9238795325112867385, 1.000000000000000000, 0.9238795325112867385, 1.000000000000000000, 0.9238795325112867385, 1.000000000000000000, 0.9238795325112867385, 1.000000000000000000, 0.9238795325112867385, 1.000000000000000000, 0.9238795325112867385, 1.000000000000000000, 0.9238795325112867385, 1.000000000000000000, 0.9238795325112867385, 1.000000000000000000, 0.9238795325112867385, 1.000000000000000000, 0.9238795325112867385, 1.000000000000000000, 0.9238795325112867385, 1.000000000000000000, 0.9238795325112867385, 1.000000000000000000, 0.9238795325112867385, 1.000000000000000000, 0.9238795325112867385, 1.000000000000000000, 0.9238795325112867385, 1.000000000000000000, 0.9238795325112867385, 1.000000000000000000, 0.9238795325112867385, 1.000000000000000000, 0.9238795325112867385, 1.000000000000000000, 0.9238795325112867385, 1.000000000000000000, 0.9238795325112867385, 1.000000000000000000, 0.9238795325112867385, 1.000000000000000000, 0.9238795325112867385, 1.000000000000000000, 0.9238795325112867385, 1.000000000000000000, 0.9238795325112867385, 1.000000000000000000, 0.9238795325112867385, 1.000000000000000000, 0.9238795325112867385, 1.000000000000000000, 0.9238795325112867385, 1.000000000000000000, 0.9238795325112867385, 1.000000000000000000, 0.9238795325112867385, 1.000000000000000000, 0.9238795325112867385, 1.000000000000000000, 0.9238795325112867385, 1.000000000000000000, 0.9238795325112867385, 1.000000000000000000, 0.9238795325112867385, 1.000000000000000000, 0.9238795325112867385, 1.000000000000000000, 0.9238795325112867385, 1.000000000000000000, 0.9238795325112867385, 1.000000000000000000, 0.9238795325112867385, 1.000000000000000000, 0.9238795325112867385, 1.000000000000000000, 0.9238795325112867385, 1.000000000000000000, 0.9238795325112867385, 1.000000000000000000, 0.9238795325112867385, 1.000000000000000000, 0.9238795325112867385, 1.000000000000000000, 0.9238795325112867385, 1.000000000000000000, 0.9238795325112867385, 1.000000000000000000, 0.9238795325112867385, 1.000000000000000000, 0.9238795325112867385, 1.000000000000000000, 0.9238795325112867385, 1.000000000000000000, 0.9238795325112867385, 1.000000000000000000, 0.9238795325112867385, 1.000000000000000000, 0.9238795325112867385, 1.000000000000000000, 0.9238795325112867385, 1.000000000000000000, 0.9238795325112867385, 1.000000000000000000, 0.9238795325112867385, 1.000000000000000000, 0.9238795325112867385, 1.000000000000000000, 0.9238795325112867385, 1.000000000000000000, 0.9238795325112867385, 1.000000000000000000, 0.9238795325112867385, 1.000000000000000000),
 ( 1.000000000000000000, 0.9238795325112867385, 1.000000000000000000, 0.9238795325112867385, 1.000000000000000000, 0.9238795325112867385, 1.000000000000000000, 0.9238795325112867385, 1.000000000000000000, 0.9238795325112867385, 1.000000000000000000, 0.9238795325112867385, 1.000000000000000000, 0.9238795325112867385, 1.000000000000000000, 0.9238795325112867385, 1.000000000000000000, 0.9238795325112867385, 1.000000000000000000, 0.9238795325112867385, 1.000000000000000000, 0.9238795325112867385, 1.000000000000000000, 0.9238795325112867385, 1.000000000000000000, 0.9238795325112867385, 1.000000000000000000, 0.9238795325112867385, 1.000000000000000000, 0.9238795325112867385, 1.000000000000000000, 0.9238795325112867385, 1.000000000000000000, 0.9238795325112867385, 1.000000000000000000, 0.9238795325112867385, 1.000000000000000000, 0.9238795325112867385, 1.000000000000000000, 0.9238795325112867385, 1.000000000000000000, 0.9238795325112867385, 1.000000000000000000, 0.9238795325112867385, 1.000000000000000000, 0.9238795325112867385, 1.000000000000000000, 0.9238795325112867385, 1.000000000000000000, 0.9238795325112867385, 1.000000000000000000, 0.9238795325112867385, 1.000000000000000000, 0.9238795325112867385, 1.000000000000000000, 0.9238795325112867385, 1.000000000000000000, 0.9238795325112867385, 1.000000000000000000, 0.9238795325112867385, 1.000000000000000000, 0.9238795325112867385, 1.000000000000000000, 0.9238795325112867385, 1.000000000000000000, 0.9238795325112867385, 1.000000000000000000, 0.9238795325112867385, 1.000000000000000000, 0.9238795325112867385, 1.000000000000000000, 0.9238795325112867385, 1.000000000000000000, 0.9238795325112867385, 1.000000000000000000, 0.9238795325112867385, 1.000000000000000000, 0.9238795325112867385, 1.000000000000000000, 0.9238795325112867385, 1.000000000000000000, 0.9238795325112867385, 1.000000000000000000, 0.9238795325112867385, 1.000000000000000000, 0.9238795325112867385, 1.000000000000000000, 0.9238795325112867385, 1.000000000000000000, 0.9238795325112867385, 1.000000000000000000, 0.9238795325112867385, 1.000000000000000000, 0.9238795325112867385, 1.000000000000000000, 0.9238795325112867385, 1.000000000000000000, 0.9238795325112867385, 1.000000000000000000, 0.9238795325112867385, 1.000000000000000000, 0.9238795325112867385, 1.000000000000000000, 0.9238795325112867385, 1.000000000000000000, 0.9238795325112867385, 1.000000000000000000, 0.9238795325112867385, 1.000000000000000000, 0.9238795325112867385, 1.000000000000000000, 0.9238795325112867385, 1.000000000000000000, 0.9238795325112867385, 1.000000000000000000, 0.9238795325112867385, 1.000000000000000000, 0.9238795325112867385, 1.000000000000000000, 0.9238795325112867385, 1.000000000000000000, 0.9238795325112867385, 1.000000000000000000, 0.9238795325112867385, 1.000000000000000000, 0.9238795325112867385, 1.000000000000000000, 0.9238795325112867385, 1.000000000000000000, 0.9238795325112867385, 1.000000000000000000, 0.9238795325112867385, 1.000000000000000000, 0.9238795325112867385, 1.000000000000000000, 0.9238795325112867385, 1.000000000000000000, 0.9238795325112867385, 1.000000000000000000, 0.9238795325112867385, 1.000000000000000000, 0.9238795325112867385, 1.000000000000000000, 0.9238795325112867385, 1.000000000000000000, 0.9238795325112867385, 1.000000000000000000, 0.9238795325112867385, 1.000000000000000000, 0.9238795325112867385, 1.000000000000000000, 0.9238795325112867385, 1.000000000000000000, 0.9238795325112867385, 1.000000000000000000, 0.9238795325112867385, 1.000000000000000000, 0.9238795325112867385, 1.000000000000000000, 0.9238795325112867385, 1.000000000000000000) ) ) 
 REPRESENTATION_ITEM ( '' )  SURFACE ( )  );
#2711=CARTESIAN_POINT ( 'NONE',  ( 0.04725809328185395092, -9.175759667312529899, -8.057670357645365655 ) ) ;
#2713=CARTESIAN_POINT ( 'NONE',  ( 4.209348295687701302, 3.401574460001765665, -6.937500000000004441 ) ) ;
#2717=CARTESIAN_POINT ( 'NONE',  ( -3.753672977998669946, -3.033343224707661712, -5.999999998634407916 ) ) ;
#2724=AXIS2_PLACEMENT_3D ( 'NONE', #8341, #13233, #10676 ) ;
#2732=CARTESIAN_POINT ( 'NONE',  ( 4.313165601266488736, -1.402244460665938997, -0.4094021847041934281 ) ) ;
#2758=CARTESIAN_POINT ( 'NONE',  ( 1.415196051561583790, -4.795541693661363958, -0.2500000000000036637 ) ) ;
#2760=CARTESIAN_POINT ( 'NONE',  ( 4.276409079477644148, 1.261996585732577891, -4.562499998634405252 ) ) ;
#2770=CARTESIAN_POINT ( 'NONE',  ( -3.753672977998669502, -3.033343224707661712, -5.999999998634408804 ) ) ;
#2771=CARTESIAN_POINT ( 'NONE',  ( 0.5711823568785988625, 5.381735091635026613, -4.687499997268819385 ) ) ;
#2776=CARTESIAN_POINT ( 'NONE',  ( -3.750000000000007550, -6.495190528383289141, 0.000000000000000000 ) ) ;
#2778=CARTESIAN_POINT ( 'NONE',  ( -0.5711823568785978633, -5.381735091635035495, -2.187499997268816720 ) ) ;
#2785=CARTESIAN_POINT ( 'NONE',  ( 3.916244202832140253, -2.131511515620588160, -7.437499998634407916 ) ) ;
#2799=CARTESIAN_POINT ( 'NONE',  ( 0.2791032213812760232, -8.821394357840572908, -7.929128246061912577 ) ) ;
#2801=CARTESIAN_POINT ( 'NONE',  ( -2.390265326283148806, -4.391654775818394363, -4.375000000000000000 ) ) ;
#2807=CARTESIAN_POINT ( 'NONE',  ( 3.916244202832140253, -2.131511515620588160, -5.687499998634406140 ) ) ;
#2815=ORIENTED_EDGE ( 'NONE', *, *, #15378, .T. ) ;
#2819=CARTESIAN_POINT ( 'NONE',  ( 1.261996585732578113, -4.276409079477644148, -2.562499998634407028 ) ) ;
#2827=CARTESIAN_POINT ( 'NONE',  ( 6.625705691649768525, -5.306270977113037191, -7.795653906408973377 ) ) ;
#2830=B_SPLINE_CURVE_WITH_KNOTS ( 'NONE', 3,
 ( #15321, #13855, #12786, #6514, #11428, #375, #1730, #5293, #9030 ),
 .UNSPECIFIED., .F., .F.,
 ( 4, 2, 1, 2, 4 ),
 ( 0.000000000000000000, 0.002165063509461097498, 0.004330127018922194995, 0.006495190528383292493, 0.008660254037844389990 ),
 .UNSPECIFIED. ) ;
#2831=EDGE_CURVE ( 'NONE', #11431, #513, #7590, .T. ) ;
#2833=DIRECTION ( 'NONE',  ( 0.000000000000000000, 0.000000000000000000, 1.000000000000000000 ) ) ;
#2839=CARTESIAN_POINT ( 'NONE',  ( -1.415196051561583790, 4.795541693661363958, -5.750000000000001776 ) ) ;
#2840=CARTESIAN_POINT ( 'NONE',  ( -3.916244202832140253, 2.131511515620587272, -4.187499998634405252 ) ) ;
#2844=CARTESIAN_POINT ( 'NONE',  ( -5.000000000000002665, -1.404940523648820476E-14, -7.545263047592946748 ) ) ;
#2848=CARTESIAN_POINT ( 'NONE',  ( -0.5093500532425060401, -4.799145180956616130, -7.874999998634408804 ) ) ;
#2853=CARTESIAN_POINT ( 'NONE',  ( -4.209348295687703967, -3.401574460001763001, -3.312499997268815388 ) ) ;
#2854=CARTESIAN_POINT ( 'NONE',  ( -1.415196051561583790, 4.795541693661363958, -8.624999997268814056 ) ) ;
#2876=CARTESIAN_POINT ( 'NONE',  ( -7.549004593702465016, -4.358419834287842853, -7.700121441565846325 ) ) ;
#2877=CARTESIAN_POINT ( 'NONE',  ( -4.391654775818395251, 2.390265326283148806, -3.624999999999999556 ) ) ;
#2881=CARTESIAN_POINT ( 'NONE',  ( 4.276409079477644148, 1.261996585732577891, -8.562499998634409692 ) ) ;
#2882=VERTEX_POINT ( 'NONE', #2237 ) ;
#2887=EDGE_CURVE ( 'NONE', #2626, #13323, #3142, .T. ) ;
#2892=CARTESIAN_POINT ( 'NONE',  ( 0.000000000000000000, 0.000000000000000000, -25.03750572909317285 ) ) ;
#2897=CARTESIAN_POINT ( 'NONE',  ( -3.033343224707664376, 3.753672977998667726, -4.999999998634407028 ) ) ;
#2898=CYLINDRICAL_SURFACE ( 'NONE', #2132, 5.000000000000000888 ) ;
#2903=DIRECTION ( 'NONE',  ( 1.000000000000000000, 0.000000000000000000, 0.000000000000000000 ) ) ;
#2915=CARTESIAN_POINT ( 'NONE',  ( 2.390265326283148806, 4.391654775818395251, -0.7499999972688138339 ) ) ;
#2918=CARTESIAN_POINT ( 'NONE',  ( -0.5093500532425060401, -4.799145180956616130, -7.874999998634408804 ) ) ;
#2919=CARTESIAN_POINT ( 'NONE',  ( -3.033343224707664376, 3.753672977998667726, -0.2499999986344070280 ) ) ;
#2921=ORIENTED_EDGE ( 'NONE', *, *, #2127, .T. ) ;
#2926=CARTESIAN_POINT ( 'NONE',  ( -5.000000000000004441, -1.011557177027151181E-15, -5.420263044861760804 ) ) ;
#2930=CARTESIAN_POINT ( 'NONE',  ( 4.795541693661363958, 1.415196051561583790, -7.874999997268816720 ) ) ;
#2936=CARTESIAN_POINT ( 'NONE',  ( 0.5093500532425063732, 4.799145180956616130, -7.124999998634407916 ) ) ;
#2943=ORIENTED_EDGE ( 'NONE', *, *, #12398, .T. ) ;
#2954=CARTESIAN_POINT ( 'NONE',  ( 4.795541693661363958, 1.415196051561583790, -4.000000000000000000 ) ) ;
#2956=CARTESIAN_POINT ( 'NONE',  ( -5.040301471719076609, -5.750234626350518852, -0.09933465333851491941 ) ) ;
#2958=CARTESIAN_POINT ( 'NONE',  ( -3.916244202832140253, 2.131511515620587272, -5.187499998634406140 ) ) ;
#2969=ORIENTED_EDGE ( 'NONE', *, *, #4658, .T. ) ;
#2970=LINE ( 'NONE', #7919, #10951 ) ;
#2971=CARTESIAN_POINT ( 'NONE',  ( 7.500000000000000000, 3.160172554975060333, -7.231829826456837473 ) ) ;
#2972=CARTESIAN_POINT ( 'NONE',  ( 3.916244202832140253, -2.131511515620588160, -6.437499998634407028 ) ) ;
#2977=CARTESIAN_POINT ( 'NONE',  ( -1.261996585732579224, 4.276409079477648589, -5.062499998634406140 ) ) ;
#2979=DIRECTION ( 'NONE',  ( 0.000000000000000000, 0.000000000000000000, 1.000000000000000000 ) ) ;
#2985=CARTESIAN_POINT ( 'NONE',  ( -5.000000000000002665, -1.404940523648820476E-14, -6.545263047592945860 ) ) ;
#2990=CARTESIAN_POINT ( 'NONE',  ( 7.500000000000000000, 4.330127018922190096, -7.422398894150031623 ) ) ;
#2992=ORIENTED_EDGE ( 'NONE', *, *, #892, .F. ) ;
#3000=CARTESIAN_POINT ( 'NONE',  ( -3.401574460001765221, 4.209348295687701302, -6.562499997268814944 ) ) ;
#3007=ORIENTED_EDGE ( 'NONE', *, *, #7190, .F. ) ;
#3014=PRODUCT_DEFINITION_FORMATION_WITH_SPECIFIED_SOURCE ( 'ANY', '', #8362, .NOT_KNOWN. ) ;
#3015=CONICAL_SURFACE ( 'NONE', #3789, 7.500000000000001776, 0.8594454914424796144 ) ;
#3019=CARTESIAN_POINT ( 'NONE',  ( 0.5711823568785989735, 5.381735091635026613, -7.687499997268816720 ) ) ;
#3027=ORIENTED_EDGE ( 'NONE', *, *, #5041, .T. ) ;
#3036=CARTESIAN_POINT ( 'NONE',  ( -7.500000000000001776, 0.000000000000000000, 0.000000000000000000 ) ) ;
#3042=CARTESIAN_POINT ( 'NONE',  ( -7.808218555863024157, -4.508077085118360472, -7.999534413642737540 ) ) ;
#3050=CARTESIAN_POINT ( 'NONE',  ( 3.753672977998667726, 3.033343224707664376, -7.499999998634409692 ) ) ;
#3054=CARTESIAN_POINT ( 'NONE',  ( -4.240553267258006517E-16, 9.016154170237607346, -7.999534413642735764 ) ) ;
#3061=VERTEX_POINT ( 'NONE', #10404 ) ;
#3062=AXIS2_PLACEMENT_3D ( 'NONE', #4477, #4324, #8131 ) ;
#3065=CARTESIAN_POINT ( 'NONE',  ( -1.261996585732579224, 4.276409079477648589, -4.062499998634405252 ) ) ;
#3067=CONICAL_SURFACE ( 'NONE', #2521, 10.39117206796836079, 1.221730476396047926 ) ;
#3070=CARTESIAN_POINT ( 'NONE',  ( 2.131511515620586383, 3.916244202832140253, -8.187499998634407916 ) ) ;
#3075=AXIS2_PLACEMENT_3D ( 'NONE', #7314, #8612, #1239 ) ;
#3080=CARTESIAN_POINT ( 'NONE',  ( -7.922798540899434805, 4.627424769998857990, -8.057412477672054152 ) ) ;
#3082=EDGE_CURVE ( 'NONE', #3405, #3174, #7066, .T. ) ;
#3084=AXIS2_PLACEMENT_3D ( 'NONE', #8510, #89, #5006 ) ;
#3093=CARTESIAN_POINT ( 'NONE',  ( 5.000000000000004441, -2.247904837838113790E-16, -6.045263047592945860 ) ) ;
#3094=CARTESIAN_POINT ( 'NONE',  ( -4.795541693661363958, -1.415196051561583790, -0.3749999972688169980 ) ) ;
#3096=CARTESIAN_POINT ( 'NONE',  ( -4.999999999999847233, 1.272547481429013860, -7.461597479913464781 ) ) ;
#3098=CARTESIAN_POINT ( 'NONE',  ( -4.799145180956616130, 0.5093500532425063732, 0.8750000013655920839 ) ) ;
#3103=ORIENTED_EDGE ( 'NONE', *, *, #6192, .F. ) ;
#3106=CARTESIAN_POINT ( 'NONE',  ( -5.000000000000004441, -1.011557177027151181E-15, -4.545263047592944083 ) ) ;
#3109=CARTESIAN_POINT ( 'NONE',  ( -4.391654775818395251, 2.390265326283148806, -8.499999997268814056 ) ) ;
#3114=CARTESIAN_POINT ( 'NONE',  ( -7.922281120364393914, 4.573931137438272287, -8.047472243342932430 ) ) ;
#3121=CARTESIAN_POINT ( 'NONE',  ( -7.500000000000004441, 1.489914625144000304, -0.1187923833806791979 ) ) ;
#3130=CARTESIAN_POINT ( 'NONE',  ( 3.753672977998667726, 3.033343224707664376, 0.7500000013655939712 ) ) ;
#3136=DIRECTION ( 'NONE',  ( 0.9396926207859143121, 1.150791560227857665E-16, -0.3420201433256525592 ) ) ;
#3139=CARTESIAN_POINT ( 'NONE',  ( 7.499999999999999112, 4.652409454067510275, -7.929128589908465585 ) ) ;
#3140=CARTESIAN_POINT ( 'NONE',  ( 3.916244202832140253, -2.131511515620588160, -3.437499998634407916 ) ) ;
#3142=( BOUNDED_CURVE ( )  B_SPLINE_CURVE ( 2, ( #10889, #7193, #14851, #6130, #8717, #6044, #12093, #7507, #12408, #1342, #4750 ),
 .UNSPECIFIED., .F., .F. ) 
 B_SPLINE_CURVE_WITH_KNOTS ( ( 3, 2, 2, 2, 2, 3 ),
 ( 0.5545872658012773737, 0.5625000000000000000, 0.5749999999999999556, 0.5875000000000000222, 0.5999999999999999778, 0.6045872658012773071 ),
 .UNSPECIFIED. ) 
 CURVE ( )  GEOMETRIC_REPRESENTATION_ITEM ( )  RATIONAL_B_SPLINE_CURVE ( ( 0.9646335149384803742, 0.9518143178943441196, 1.000000000000000000, 0.9238795325112867385, 1.000000000000000000, 0.9238795325112867385, 1.000000000000000000, 0.9238795325112867385, 1.000000000000000000, 0.9720652146169428409, 0.9646335149384808183 ) ) 
 REPRESENTATION_ITEM ( '' )  );
#3144=CARTESIAN_POINT ( 'NONE',  ( -4.276409079477644148, -1.261996585732578335, -5.812499998634406140 ) ) ;
#3152=CARTESIAN_POINT ( 'NONE',  ( 1.249327701958355741, -8.410337540185093275, -7.776713651266290661 ) ) ;
#3155=CARTESIAN_POINT ( 'NONE',  ( -7.500000000000003553, 3.202583086486119779, -7.213046687579564242 ) ) ;
#3167=CARTESIAN_POINT ( 'NONE',  ( -4.276409079477644148, -1.261996585732578335, -8.062499998634407916 ) ) ;
#3173=SHAPE_REPRESENTATION ( 'hex flange nut gradea 1_iso_ISO - 4161 - M10 - N', ( #3223 ), #7084 ) ;
#3174=VERTEX_POINT ( 'NONE', #9508 ) ;
#3176=CARTESIAN_POINT ( 'NONE',  ( 0.5711823568785988625, 5.381735091635026613, -4.812500000000000000 ) ) ;
#3181=CARTESIAN_POINT ( 'NONE',  ( -2.390265326283148806, -4.391654775818394363, -8.249999997268814056 ) ) ;
#3184=CARTESIAN_POINT ( 'NONE',  ( 5.000000000000000888, 0.000000000000000000, -25.03750572909317285 ) ) ;
#3198=CARTESIAN_POINT ( 'NONE',  ( 4.458734124998676052, -0.1932007455631602477, -0.3789984458506766019 ) ) ;
#3203=CARTESIAN_POINT ( 'NONE',  ( 1.261996585732578113, -4.276409079477644148, -1.562499998634406140 ) ) ;
#3212=CARTESIAN_POINT ( 'NONE',  ( -2.390265326283148806, -4.391654775818394363, -6.375000000000001776 ) ) ;
#3216=CARTESIAN_POINT ( 'NONE',  ( 3.033343224707661712, -3.753672977998669502, -3.499999998634409692 ) ) ;
#3217=DIRECTION ( 'NONE',  ( 0.000000000000000000, 0.000000000000000000, 1.000000000000000000 ) ) ;
#3219=CARTESIAN_POINT ( 'NONE',  ( -3.401574460001764777, 4.209348295687701302, 1.312499999999996447 ) ) ;
#3223=AXIS2_PLACEMENT_3D ( 'NONE', #11897, #11972, #4638 ) ;
#3231=CARTESIAN_POINT ( 'NONE',  ( -4.999999999999849898, 1.272547481429008309, -3.461597479913464781 ) ) ;
#3245=CARTESIAN_POINT ( 'NONE',  ( -4.336808689942017736E-16, -8.660254037844399733, -7.422398894150038728 ) ) ;
#3249=ORIENTED_EDGE ( 'NONE', *, *, #2018, .T. ) ;
#3250=DIRECTION ( 'NONE',  ( 0.000000000000000000, 0.000000000000000000, 1.000000000000000000 ) ) ;
#3251=VECTOR ( 'NONE', #3540, 1000.000000000000000 ) ;
#3252=ORIENTED_EDGE ( 'NONE', *, *, #10570, .T. ) ;
#3257=CARTESIAN_POINT ( 'NONE',  ( -4.795541693661363958, -1.415196051561583790, -3.374999997268816276 ) ) ;
#3258=CARTESIAN_POINT ( 'NONE',  ( -3.753672977998669946, -3.033343224707661712, 1.250000001365594304 ) ) ;
#3260=CARTESIAN_POINT ( 'NONE',  ( -4.209348295687703967, -3.401574460001763001, -6.312499997268814056 ) ) ;
#3265=EDGE_LOOP ( 'NONE', ( #1274, #6914, #6984, #8682 ) ) ;
#3267=CARTESIAN_POINT ( 'NONE',  ( -4.391654775818395251, 2.390265326283148806, -2.499999997268815388 ) ) ;
#3273=ORIENTED_EDGE ( 'NONE', *, *, #2238, .T. ) ;
#3281=CARTESIAN_POINT ( 'NONE',  ( 1.415196051561583790, -4.795541693661363958, -5.250000000000000888 ) ) ;
#3287=CARTESIAN_POINT ( 'NONE',  ( -5.000000000000000888, 6.123233995736767268E-16, -25.03750572909317285 ) ) ;
#3289=CARTESIAN_POINT ( 'NONE',  ( -1.261996585732579224, 4.276409079477648589, -0.06249999863440838799 ) ) ;
#3296=CARTESIAN_POINT ( 'NONE',  ( 0.5711823568785988625, 5.381735091635026613, -7.812500000000005329 ) ) ;
#3301=CARTESIAN_POINT ( 'NONE',  ( 2.131511515620586383, 3.916244202832140253, -7.187499998634407916 ) ) ;
#3302=CARTESIAN_POINT ( 'NONE',  ( 3.093157300003885890, 6.874418838041284729, 2.320870275476782535E-15 ) ) ;
#3304=CARTESIAN_POINT ( 'NONE',  ( -4.209348295687703967, -3.401574460001763001, 1.562499999999996669 ) ) ;
#3317=CARTESIAN_POINT ( 'NONE',  ( -4.391654775818395251, 2.390265326283148806, -3.499999997268816276 ) ) ;
#3318=AXIS2_PLACEMENT_3D ( 'NONE', #6996, #10701, #8296 ) ;
#3322=DIRECTION ( 'NONE',  ( -1.000000000000000000, 0.000000000000000000, 0.000000000000000000 ) ) ;
#3341=CARTESIAN_POINT ( 'NONE',  ( -0.5093500532425060401, -4.799145180956616130, 1.375000001365592528 ) ) ;
#3343=CARTESIAN_POINT ( 'NONE',  ( 3.753672977998667726, 3.033343224707664376, -3.499999998634410137 ) ) ;
#3351=VERTEX_POINT ( 'NONE', #3505 ) ;
#3352=DIRECTION ( 'NONE',  ( 0.000000000000000000, 0.000000000000000000, 1.000000000000000000 ) ) ;
#3354=ORIENTED_EDGE ( 'NONE', *, *, #13324, .F. ) ;
#3355=CARTESIAN_POINT ( 'NONE',  ( -3.753672977998669502, -3.033343224707661712, -0.9999999986344076941 ) ) ;
#3357=FACE_OUTER_BOUND ( 'NONE', #6836, .T. ) ;
#3360=CARTESIAN_POINT ( 'NONE',  ( 0.000000000000000000, 0.000000000000000000, -25.03750572909317285 ) ) ;
#3363=DIRECTION ( 'NONE',  ( 1.000000000000000000, 0.000000000000000000, 0.000000000000000000 ) ) ;
#3367=CARTESIAN_POINT ( 'NONE',  ( -4.276409079477644148, -1.261996585732578335, -1.812499998634406584 ) ) ;
#3369=CARTESIAN_POINT ( 'NONE',  ( 0.3306966981844952636, 8.469326210127450238, -7.349897473154610950 ) ) ;
#3375=FACE_OUTER_BOUND ( 'NONE', #13788, .T. ) ;
#3376=CARTESIAN_POINT ( 'NONE',  ( 2.452879891156804160, 7.244083172395184178, -0.1007566405101766455 ) ) ;
#3378=CARTESIAN_POINT ( 'NONE',  ( 2.131511515620586383, 3.916244202832140253, -6.187499998634407028 ) ) ;
#3380=CARTESIAN_POINT ( 'NONE',  ( -1.344377895606795770, -4.647603660250892332, -0.1184410768129991742 ) ) ;
#3383=ORIENTED_EDGE ( 'NONE', *, *, #9107, .T. ) ;
#3392=CARTESIAN_POINT ( 'NONE',  ( 0.000000000000000000, 0.000000000000000000, 0.000000000000000000 ) ) ;
#3393=CARTESIAN_POINT ( 'NONE',  ( -1.211595439868048407, 7.960739084487649109, -0.4504974108211993733 ) ) ;
#3397=CARTESIAN_POINT ( 'NONE',  ( -4.209348295687703079, -3.401574460001763445, -0.3124999972688167760 ) ) ;
#3404=CARTESIAN_POINT ( 'NONE',  ( -0.9763930676191269198, 8.096533237419631490, -7.213065638944388347 ) ) ;
#3405=VERTEX_POINT ( 'NONE', #11347 ) ;
#3409=CARTESIAN_POINT ( 'NONE',  ( -3.916244202832140253, 2.131511515620587272, -0.9374999986344056957 ) ) ;
#3411=CARTESIAN_POINT ( 'NONE',  ( -2.131511515620587272, -3.916244202832140253, -1.937499998634406584 ) ) ;
#3422=CARTESIAN_POINT ( 'NONE',  ( 4.276409079477644148, 1.261996585732577891, -2.562499998634407028 ) ) ;
#3426=EDGE_CURVE ( 'NONE', #4597, #4915, #11486, .T. ) ;
#3427=DIRECTION ( 'NONE',  ( -1.000000000000000000, 0.000000000000000000, 0.000000000000000000 ) ) ;
#3430=CARTESIAN_POINT ( 'NONE',  ( 8.152940247294426498E-14, -9.016621985895911351, -7.999704684617491068 ) ) ;
#3433=CARTESIAN_POINT ( 'NONE',  ( -3.916244202832140253, 2.131511515620587272, 1.062500001365592528 ) ) ;
#3447=CARTESIAN_POINT ( 'NONE',  ( 0.000000000000000000, 0.000000000000000000, -8.499999999999996447 ) ) ;
#3449=CARTESIAN_POINT ( 'NONE',  ( -4.795541693661363958, -1.415196051561583790, -1.500000000000001332 ) ) ;
#3457=CARTESIAN_POINT ( 'NONE',  ( -7.500000000000003553, 1.644753667985980217, -7.029983668656051066 ) ) ;
#3475=SHAPE_REPRESENTATION_RELATIONSHIP ( 'NONE' , 'NONE' ,  #3173, #15834 ) ;
#3486=CARTESIAN_POINT ( 'NONE',  ( 4.276409079477644148, 1.261996585732577891, -0.5624999986344088043 ) ) ;
#3494=CARTESIAN_POINT ( 'NONE',  ( 4.999999999999849898, -1.272547481429010530, -1.086597482644648061 ) ) ;
#3497=CARTESIAN_POINT ( 'NONE',  ( 1.261996585732578113, -4.276409079477644148, -2.812499998634407472 ) ) ;
#3504=CARTESIAN_POINT ( 'NONE',  ( -4.391654775818395251, 2.390265326283148806, -1.499999997268814500 ) ) ;
#3505=CARTESIAN_POINT ( 'NONE',  ( -7.500000000000000888, -4.330127018922199866, -1.000000000000000888 ) ) ;
#3509=CARTESIAN_POINT ( 'NONE',  ( 0.5093500532425063732, 4.799145180956616130, -6.124999998634407916 ) ) ;
#3513=EDGE_LOOP ( 'NONE', ( #7034, #12791, #2347 ) ) ;
#3528=CARTESIAN_POINT ( 'NONE',  ( 0.5711823568785989735, 5.381735091635026613, -2.812500000000001332 ) ) ;
#3532=CARTESIAN_POINT ( 'NONE',  ( -3.753672977998669946, -3.033343224707661712, -1.999999998634408360 ) ) ;
#3540=DIRECTION ( 'NONE',  ( 0.8306121863236411995, 0.2451191463975535001, -0.4999999999999953371 ) ) ;
#3541=VERTEX_POINT ( 'NONE', #14997 ) ;
#3558=ORIENTED_EDGE ( 'NONE', *, *, #9039, .T. ) ;
#3568=CIRCLE ( 'NONE', #10559, 0.7733184030943203169 ) ;
#3569=DIRECTION ( 'NONE',  ( 0.000000000000000000, 0.000000000000000000, 1.000000000000000000 ) ) ;
#3571=CARTESIAN_POINT ( 'NONE',  ( -1.261996585732579224, 4.276409079477648589, -0.06249999863440838799 ) ) ;
#3576=CARTESIAN_POINT ( 'NONE',  ( -4.276409079477644148, -1.261996585732578335, -3.062499998634407472 ) ) ;
#3589=CARTESIAN_POINT ( 'NONE',  ( 0.5093500532425063732, 4.799145180956616130, -3.374999998634407916 ) ) ;
#3596=CARTESIAN_POINT ( 'NONE',  ( 3.401574460001763001, -4.209348295687703967, -1.062499997268813612 ) ) ;
#3598=( NAMED_UNIT ( * ) PLANE_ANGLE_UNIT ( ) SI_UNIT ( $, .RADIAN. ) );
#3601=CARTESIAN_POINT ( 'NONE',  ( -2.131511515620587272, -3.916244202832140253, -5.687499998634406140 ) ) ;
#3615=CARTESIAN_POINT ( 'NONE',  ( -2.390265326283148806, -4.391654775818394363, 0.6249999999999971134 ) ) ;
#3620=CARTESIAN_POINT ( 'NONE',  ( 3.033343224707661712, -3.753672977998669946, -2.749999998634409248 ) ) ;
#3625=CARTESIAN_POINT ( 'NONE',  ( -7.908228835406504231, 3.123118350879575456, -7.776694659841331791 ) ) ;
#3634=EDGE_CURVE ( 'NONE', #3976, #15838, #34, .T. ) ;
#3650=CARTESIAN_POINT ( 'NONE',  ( -4.799145180956616130, 0.5093500532425063732, -1.874999998634406584 ) ) ;
#3654=CARTESIAN_POINT ( 'NONE',  ( -1.261996585732579224, 4.276409079477648589, -0.3124999986344085823 ) ) ;
#3662=CARTESIAN_POINT ( 'NONE',  ( -0.5093500532425060401, -4.799145180956616130, -3.874999998634408360 ) ) ;
#3666=CARTESIAN_POINT ( 'NONE',  ( 4.276409079477644148, 1.261996585732577891, -8.312499998634407916 ) ) ;
#3667=CARTESIAN_POINT ( 'NONE',  ( -7.500000000000005329, 4.330127018922194537, -9.999999999999998224 ) ) ;
#3670=CARTESIAN_POINT ( 'NONE',  ( 4.209348295687701302, 3.401574460001765665, -0.8124999972688135008 ) ) ;
#3674=CARTESIAN_POINT ( 'NONE',  ( -3.753672977998669946, -3.033343224707661712, -5.749999998634407916 ) ) ;
#3685=AXIS2_PLACEMENT_3D ( 'NONE', #8899, #15040, #502 ) ;
#3689=CARTESIAN_POINT ( 'NONE',  ( 1.415196051561583790, -4.795541693661363958, -2.250000000000001776 ) ) ;
#3693=CARTESIAN_POINT ( 'NONE',  ( -4.799145180956616130, 0.5093500532425063732, -4.124999998634405252 ) ) ;
#3699=CARTESIAN_POINT ( 'NONE',  ( -7.500000000002755129, -3.882691789159864459, -7.781695678275425188 ) ) ;
#3710=CARTESIAN_POINT ( 'NONE',  ( -4.209348295687703079, -3.401574460001763445, -1.312499997268813834 ) ) ;
#3716=EDGE_LOOP ( 'NONE', ( #7241, #1780, #13245, #7331, #8705, #15659, #3805 ) ) ;
#3726=CARTESIAN_POINT ( 'NONE',  ( 4.999999999999845457, -1.272547481429021854, -3.961597479913466557 ) ) ;
#3727=CARTESIAN_POINT ( 'NONE',  ( 4.799145180956616130, -0.5093500532425063732, -3.374999998634407472 ) ) ;
#3728=CARTESIAN_POINT ( 'NONE',  ( -2.131511515620587272, -3.916244202832140253, -3.937499998634408360 ) ) ;
#3733=ADVANCED_FACE ( 'NONE', ( #13488 ), #11968, .F. ) ;
#3741=CARTESIAN_POINT ( 'NONE',  ( 3.916244202832140253, -2.131511515620588160, -4.687499998634405252 ) ) ;
#3744=CARTESIAN_POINT ( 'NONE',  ( -1.261996585732579224, 4.276409079477648589, -8.062499998634407916 ) ) ;
#3747=CARTESIAN_POINT ( 'NONE',  ( -4.795541693661363958, -1.415196051561583790, -3.374999997268816276 ) ) ;
#3753=CARTESIAN_POINT ( 'NONE',  ( -3.916244202832140253, 2.131511515620587272, -4.937499998634406140 ) ) ;
#3761=CONICAL_SURFACE ( 'NONE', #5586, 7.500000000000001776, 0.8594454914424796144 ) ;
#3765=VECTOR ( 'NONE', #329, 1000.000000000000000 ) ;
#3771=CARTESIAN_POINT ( 'NONE',  ( -0.5711823568785978633, -5.381735091635035495, -0.3124999999999993339 ) ) ;
#3772=CARTESIAN_POINT ( 'NONE',  ( 5.000000000000004441, 6.350331166892669572E-15, -1.920263044861758583 ) ) ;
#3776=CARTESIAN_POINT ( 'NONE',  ( -1.261996585732579224, 4.276409079477648589, -3.312499998634407916 ) ) ;
#3778=CARTESIAN_POINT ( 'NONE',  ( -7.500000000000007105, -1.486698507076798181, -0.09861472150524400182 ) ) ;
#3789=AXIS2_PLACEMENT_3D ( 'NONE', #3392, #4527, #3322 ) ;
#3790=CARTESIAN_POINT ( 'NONE',  ( 3.288228914120474133, -7.217643567644815406, -7.591235721156640359 ) ) ;
#3805=ORIENTED_EDGE ( 'NONE', *, *, #566, .T. ) ;
#3811=CARTESIAN_POINT ( 'NONE',  ( 4.276409079477644148, 1.261996585732577891, -4.312499998634405252 ) ) ;
#3814=CARTESIAN_POINT ( 'NONE',  ( -4.276409079477644148, -1.261996585732578335, -6.062499998634407028 ) ) ;
#3827=CARTESIAN_POINT ( 'NONE',  ( -3.916244202832140253, 2.131511515620587272, -8.187499998634407916 ) ) ;
#3828=CARTESIAN_POINT ( 'NONE',  ( -5.000000000000004441, -1.011557177027151181E-15, -4.420263044861760804 ) ) ;
#3836=CARTESIAN_POINT ( 'NONE',  ( 5.381735091635035495, -0.5711823568785978633, -3.937499997268818497 ) ) ;
#3838=CARTESIAN_POINT ( 'NONE',  ( -2.533142440694107655, 3.791257988497170661, -0.3164060562859182801 ) ) ;
#3842=CARTESIAN_POINT ( 'NONE',  ( 4.276409079477644148, 1.261996585732577891, -2.312499998634407028 ) ) ;
#3851=( BOUNDED_CURVE ( )  B_SPLINE_CURVE ( 2, ( #9369, #4273, #5490, #14138, #13217, #8165, #14293, #9445, #13148, #10507, #11693 ),
 .UNSPECIFIED., .F., .F. ) 
 B_SPLINE_CURVE_WITH_KNOTS ( ( 3, 2, 2, 2, 2, 3 ),
 ( 0.6545872658012773515, 0.6624999999999999778, 0.6750000000000000444, 0.6875000000000000000, 0.6999999999999999556, 0.7045872658012772849 ),
 .UNSPECIFIED. ) 
 CURVE ( )  GEOMETRIC_REPRESENTATION_ITEM ( )  RATIONAL_B_SPLINE_CURVE ( ( 0.9646335149384803742, 0.9518143178943441196, 1.000000000000000000, 0.9238795325112867385, 1.000000000000000000, 0.9238795325112867385, 1.000000000000000000, 0.9238795325112867385, 1.000000000000000000, 0.9720652146169428409, 0.9646335149384808183 ) ) 
 REPRESENTATION_ITEM ( '' )  );
#3855=CARTESIAN_POINT ( 'NONE',  ( -2.411464220262878655, -7.267994521134962582, -7.491772860716182869 ) ) ;
#3858=CARTESIAN_POINT ( 'NONE',  ( -4.795541693661363958, -1.415196051561583790, -4.500000000000000888 ) ) ;
#3862=CARTESIAN_POINT ( 'NONE',  ( -4.799145180956616130, 0.5093500532425063732, -3.124999998634407916 ) ) ;
#3863=ORIENTED_EDGE ( 'NONE', *, *, #14819, .F. ) ;
#3864=CARTESIAN_POINT ( 'NONE',  ( -7.922281120364393914, -4.573931137438277617, -8.047472243342932430 ) ) ;
#3866=ORIENTED_EDGE ( 'NONE', *, *, #5204, .T. ) ;
#3869=LINE ( 'NONE', #7597, #3765 ) ;
#3874=CARTESIAN_POINT ( 'NONE',  ( 4.799145180956616130, -0.5093500532425063732, -3.374999998634407916 ) ) ;
#3875=CARTESIAN_POINT ( 'NONE',  ( 2.337141007481793764, 3.806500215644827545, -0.3789984458506294174 ) ) ;
#3881=CARTESIAN_POINT ( 'NONE',  ( 4.999999999999848121, -1.272547481429015859, -5.961597479913463893 ) ) ;
#3883=ORIENTED_EDGE ( 'NONE', *, *, #7227, .T. ) ;
#3884=ORIENTED_EDGE ( 'NONE', *, *, #4510, .F. ) ;
#3885=ORIENTED_EDGE ( 'NONE', *, *, #11570, .T. ) ;
#3891=CARTESIAN_POINT ( 'NONE',  ( -0.5093500532425060401, -4.799145180956616130, -6.874999998634407916 ) ) ;
#3896=VERTEX_POINT ( 'NONE', #12372 ) ;
#3901=CARTESIAN_POINT ( 'NONE',  ( 3.753672977998667726, 3.033343224707664820, -7.499999998634409692 ) ) ;
#3908=CARTESIAN_POINT ( 'NONE',  ( 4.209348295687701302, 3.401574460001765665, -3.812499997268815832 ) ) ;
#3909=CARTESIAN_POINT ( 'NONE',  ( -3.401574460001765221, 4.209348295687701302, -8.562499997268812280 ) ) ;
#3911=CARTESIAN_POINT ( 'NONE',  ( -3.293006400480308127, 3.192677401847128671, -0.2974341898043406651 ) ) ;
#3925=CARTESIAN_POINT ( 'NONE',  ( 0.5789871446316211534, 4.420982230657665824, -0.3789984458506777676 ) ) ;
#3926=CARTESIAN_POINT ( 'NONE',  ( -5.274401269815138349, -6.074457022762090652, -7.633824513837112136 ) ) ;
#3929=CARTESIAN_POINT ( 'NONE',  ( 5.381735091635035495, -0.5711823568785978633, -5.062500000000000888 ) ) ;
#3934=CARTESIAN_POINT ( 'NONE',  ( -0.5093500532425060401, -4.799145180956616130, -6.874999998634407916 ) ) ;
#3938=ORIENTED_EDGE ( 'NONE', *, *, #100, .T. ) ;
#3947=CARTESIAN_POINT ( 'NONE',  ( 10.12668159690567649, 0.000000000000000000, -9.226681596905677907 ) ) ;
#3948=CARTESIAN_POINT ( 'NONE',  ( -4.799145180956616130, 0.5093500532425063732, -1.874999998634406584 ) ) ;
#3955=CARTESIAN_POINT ( 'NONE',  ( -5.000000000000095035, -0.7223674278660573433, -3.521799365517154001 ) ) ;
#3959=VERTEX_POINT ( 'NONE', #281 ) ;
#3963=VERTEX_POINT ( 'NONE', #1865 ) ;
#3965=CARTESIAN_POINT ( 'NONE',  ( 7.894787914004607998, 1.231001383561881556E-13, -7.591390474663423760 ) ) ;
#3967=STYLED_ITEM ( 'NONE', ( #6161 ), #15834 ) ;
#3968=CARTESIAN_POINT ( 'NONE',  ( 0.5093500532425063732, 4.799145180956616130, -7.374999998634408804 ) ) ;
#3971=DIRECTION ( 'NONE',  ( 0.000000000000000000, 0.000000000000000000, 1.000000000000000000 ) ) ;
#3976=VERTEX_POINT ( 'NONE', #15380 ) ;
#3977=CARTESIAN_POINT ( 'NONE',  ( -1.261996585732579224, 4.276409079477648589, -7.312499998634407916 ) ) ;
#3984=CARTESIAN_POINT ( 'NONE',  ( -2.390265326283148806, -4.391654775818394363, -4.249999997268816720 ) ) ;
#3989=EDGE_LOOP ( 'NONE', ( #2661, #5480, #10236, #6535, #8095, #97 ) ) ;
#4000=VECTOR ( 'NONE', #14821, 1000.000000000000000 ) ;
#4005=CARTESIAN_POINT ( 'NONE',  ( -2.390265326283148806, -4.391654775818394363, -6.375000000000001776 ) ) ;
#4007=EDGE_CURVE ( 'NONE', #2626, #7077, #14076, .T. ) ;
#4011=CARTESIAN_POINT ( 'NONE',  ( 3.033343224707661712, -3.753672977998669946, -7.749999998634409692 ) ) ;
#4022=CARTESIAN_POINT ( 'NONE',  ( 5.000000000000000888, 0.000000000000000000, -25.03750572909317285 ) ) ;
#4024=CARTESIAN_POINT ( 'NONE',  ( 0.6511518506208961998, -8.763486134561278007, -7.907570769506053310 ) ) ;
#4036=VERTEX_POINT ( 'NONE', #10533 ) ;
#4037=VECTOR ( 'NONE', #8113, 1000.000000000000000 ) ;
#4048=ADVANCED_FACE ( 'NONE', ( #7952 ), #2706, .F. ) ;
#4053=CARTESIAN_POINT ( 'NONE',  ( 3.753672977998667726, 3.033343224707664376, -6.499999998634407916 ) ) ;
#4058=CARTESIAN_POINT ( 'NONE',  ( -5.000000000000092371, -0.7223674278660636716, -7.521799365517158442 ) ) ;
#4063=CARTESIAN_POINT ( 'NONE',  ( 3.033343224707661712, -3.753672977998669502, -7.749999998634409692 ) ) ;
#4070=CARTESIAN_POINT ( 'NONE',  ( 3.401574460001763001, -4.209348295687703967, -2.062499997268814500 ) ) ;
#4072=CARTESIAN_POINT ( 'NONE',  ( -4.468245232710503778, 1.275674966182978265, -0.2551639277954672602 ) ) ;
#4076=CARTESIAN_POINT ( 'NONE',  ( -4.799145180956616130, 0.5093500532425063732, -6.874999998634407916 ) ) ;
#4077=VECTOR ( 'NONE', #7383, 1000.000000000000000 ) ;
#4083=CARTESIAN_POINT ( 'NONE',  ( -3.288228914120471913, 7.217643567644807412, -7.591235721156636806 ) ) ;
#4084=MECHANICAL_DESIGN_GEOMETRIC_PRESENTATION_REPRESENTATION('',(#11057),#13887);
#4092=CARTESIAN_POINT ( 'NONE',  ( -0.5711823568785978633, -5.381735091635035495, -5.312499999999999112 ) ) ;
#4098=CARTESIAN_POINT ( 'NONE',  ( -3.033343224707664376, 3.753672977998667726, -5.249999998634407028 ) ) ;
#4099=ORIENTED_EDGE ( 'NONE', *, *, #1782, .T. ) ;
#4105=CARTESIAN_POINT ( 'NONE',  ( -7.922281120364393914, -4.573931137438277617, -8.047472243342932430 ) ) ;
#4107=DIRECTION ( 'NONE',  ( 1.000000000000000000, 0.000000000000000000, 0.000000000000000000 ) ) ;
#4108=EDGE_CURVE ( 'NONE', #637, #1925, #2830, .T. ) ;
#4112=CARTESIAN_POINT ( 'NONE',  ( 4.420982230657666712, -0.5789871446316176007, -0.3789984458506777676 ) ) ;
#4115=CARTESIAN_POINT ( 'NONE',  ( -3.753672977998669946, -3.033343224707661712, -4.749999998634407028 ) ) ;
#4121=FACE_OUTER_BOUND ( 'NONE', #8533, .T. ) ;
#4124=EDGE_LOOP ( 'NONE', ( #9267, #6242, #15766 ) ) ;
#4128=ADVANCED_FACE ( 'NONE', ( #6681 ), #456, .T. ) ;
#4131=CARTESIAN_POINT ( 'NONE',  ( 7.922281120364393914, 4.573931137438269623, -8.047472243342932430 ) ) ;
#4135=CARTESIAN_POINT ( 'NONE',  ( 4.799145180956616130, -0.5093500532425063732, 0.3750000013655915843 ) ) ;
#4138=EDGE_LOOP ( 'NONE', ( #9106, #15622, #4269, #3027, #3558 ) ) ;
#4142=CARTESIAN_POINT ( 'NONE',  ( -3.033343224707664820, 3.753672977998667726, -5.249999998634407916 ) ) ;
#4147=CARTESIAN_POINT ( 'NONE',  ( -5.000000000000002665, -1.404940523648820476E-14, -8.420263044861757251 ) ) ;
#4149=CARTESIAN_POINT ( 'NONE',  ( 1.415196051561583790, -4.795541693661363958, -8.124999997268814056 ) ) ;
#4157=ORIENTED_EDGE ( 'NONE', *, *, #4658, .F. ) ;
#4162=EDGE_CURVE ( 'NONE', #3541, #7075, #13604, .T. ) ;
#4165=CARTESIAN_POINT ( 'NONE',  ( -5.047120108843201614, 5.746297884371392328, -0.1007566405101798096 ) ) ;
#4170=CARTESIAN_POINT ( 'NONE',  ( -4.209348295687703967, -3.401574460001763001, -4.437500000000000888 ) ) ;
#4171=CARTESIAN_POINT ( 'NONE',  ( -4.999999999999849898, 1.272547481429008309, -2.586597482644648949 ) ) ;
#4175=( BOUNDED_SURFACE ( )  B_SPLINE_SURFACE ( 3, 2, ( 
 ( #4286, #11701, #8020 ),
 ( #15452, #11627, #3152 ),
 ( #13972, #10429, #12751 ),
 ( #15364, #4373, #1696 ),
 ( #8097, #1928, #505 ),
 ( #5662, #10602, #2827 ),
 ( #15284, #5425, #13301 ),
 ( #5973, #14302, #6050 ) ),
 .UNSPECIFIED., .F., .F., .F. ) 
 B_SPLINE_SURFACE_WITH_KNOTS ( ( 4, 2, 2, 4 ),
 ( 3, 3 ),
 ( 0.03861844051980971304, 0.04325213341840643266, 0.04556897986770479247, 0.04788582631700314535 ),
 ( 0.000000000000000000, 1.000000000000000000 ),
 .UNSPECIFIED. ) 
 GEOMETRIC_REPRESENTATION_ITEM ( )  RATIONAL_B_SPLINE_SURFACE ( (
 ( 1.000000000000000000, 0.8047781759831919013, 1.000000000000000000),
 ( 1.000000000000000000, 0.8123762462801796813, 1.000000000000000000),
 ( 1.000000000000000000, 0.8190659850621079263, 1.000000000000000000),
 ( 1.000000000000000000, 0.8191937571011467245, 1.000000000000000000),
 ( 1.000000000000000000, 0.8176092952778544198, 1.000000000000000000),
 ( 1.000000000000000000, 0.8122962088598406627, 1.000000000000000000),
 ( 1.000000000000000000, 0.8086311330826504440, 1.000000000000000000),
 ( 1.000000000000000000, 0.8047712282214325441, 1.000000000000000000) ) ) 
 REPRESENTATION_ITEM ( '' )  SURFACE ( )  );
#4177=CARTESIAN_POINT ( 'NONE',  ( -0.5093500532425060401, -4.799145180956616130, -4.874999998634405252 ) ) ;
#4192=CARTESIAN_POINT ( 'NONE',  ( -4.276409079477644148, -1.261996585732578335, -4.812499998634405252 ) ) ;
#4193=CARTESIAN_POINT ( 'NONE',  ( -1.250000000000000444, -7.938566201357371455, -7.198902722707432922 ) ) ;
#4196=CARTESIAN_POINT ( 'NONE',  ( 3.401574460001763445, -4.209348295687703079, -3.187500000000003553 ) ) ;
#4199=CARTESIAN_POINT ( 'NONE',  ( -3.401574460001765221, 4.209348295687701302, -6.687500000000003553 ) ) ;
#4201=EDGE_LOOP ( 'NONE', ( #12815, #7497, #12056, #14443 ) ) ;
#4214=CARTESIAN_POINT ( 'NONE',  ( 3.750000000000001776, -6.495190528383298911, -6.991905250253755533 ) ) ;
#4228=CARTESIAN_POINT ( 'NONE',  ( 4.391654775818395251, -2.390265326283149694, -5.999999997268814944 ) ) ;
#4231=CARTESIAN_POINT ( 'NONE',  ( -5.000000000000004441, -7.530481206757679743E-15, -1.545263047592943861 ) ) ;
#4233=EDGE_CURVE ( 'NONE', #513, #9050, #1061, .T. ) ;
#4234=EDGE_LOOP ( 'NONE', ( #15251, #1543, #9230, #14107, #6886 ) ) ;
#4236=CARTESIAN_POINT ( 'NONE',  ( 3.033343224707661712, -3.753672977998669946, -6.499999998634407916 ) ) ;
#4258=CARTESIAN_POINT ( 'NONE',  ( 2.131511515620586383, 3.916244202832140253, -8.437499998634409692 ) ) ;
#4265=VECTOR ( 'NONE', #11818, 1000.000000000000000 ) ;
#4267=CARTESIAN_POINT ( 'NONE',  ( -5.000000000000002665, -1.404940523648820476E-14, -7.545263047592946748 ) ) ;
#4269=ORIENTED_EDGE ( 'NONE', *, *, #5223, .T. ) ;
#4271=CARTESIAN_POINT ( 'NONE',  ( 7.500000000000346390, 1.545478204151935930, -7.491761935629074109 ) ) ;
#4272=CARTESIAN_POINT ( 'NONE',  ( -3.033343224707664820, 3.753672977998667726, -3.999999998634406584 ) ) ;
#4273=CARTESIAN_POINT ( 'NONE',  ( -4.999999999999844569, 1.272547481429019856, -5.461597479913463893 ) ) ;
#4277=CARTESIAN_POINT ( 'NONE',  ( 3.401574460001763001, -4.209348295687703967, 1.812499999999996669 ) ) ;
#4283=ORIENTED_EDGE ( 'NONE', *, *, #9373, .T. ) ;
#4286=CARTESIAN_POINT ( 'NONE',  ( -0.3470952277635217520, -8.860649561028104415, -7.493596212620246888 ) ) ;
#4289=FACE_OUTER_BOUND ( 'NONE', #4234, .T. ) ;
#4290=EDGE_LOOP ( 'NONE', ( #12529, #95, #5463 ) ) ;
#4293=ADVANCED_FACE ( 'NONE', ( #3375 ), #11123, .F. ) ;
#4294=CARTESIAN_POINT ( 'NONE',  ( 0.000000000000000000, 0.000000000000000000, 0.000000000000000000 ) ) ;
#4296=EDGE_CURVE ( 'NONE', #13728, #15071, #11518, .T. ) ;
#4299=CARTESIAN_POINT ( 'NONE',  ( 5.000000000000091482, 0.7223674278660666692, -0.8967993627859682793 ) ) ;
#4300=CARTESIAN_POINT ( 'NONE',  ( 3.401574460001763445, -4.209348295687703079, -4.187500000000000888 ) ) ;
#4307=CARTESIAN_POINT ( 'NONE',  ( -7.848314987057863235, 4.129027267381583322, -7.493854785173818200 ) ) ;
#4311=ORIENTED_EDGE ( 'NONE', *, *, #13694, .T. ) ;
#4318=CARTESIAN_POINT ( 'NONE',  ( -3.033343224707664376, 3.753672977998667726, 0.7500000013655939712 ) ) ;
#4321=CARTESIAN_POINT ( 'NONE',  ( -3.401574460001765221, 4.209348295687701302, -1.687500000000002442 ) ) ;
#4324=DIRECTION ( 'NONE',  ( 0.000000000000000000, 0.000000000000000000, 1.000000000000000000 ) ) ;
#4325=CARTESIAN_POINT ( 'NONE',  ( -7.808218555861950350, 4.508077085120202554, -7.999534413642741093 ) ) ;
#4329=ORIENTED_EDGE ( 'NONE', *, *, #11388, .F. ) ;
#4346=CARTESIAN_POINT ( 'NONE',  ( -2.131511515620587272, -3.916244202832140253, 1.312500001365592750 ) ) ;
#4348=CARTESIAN_POINT ( 'NONE',  ( 0.6250000000000025535, 8.299410119600878488, -7.298562697733109061 ) ) ;
#4349=ORIENTED_EDGE ( 'NONE', *, *, #10158, .F. ) ;
#4350=EDGE_LOOP ( 'NONE', ( #9606, #7636, #8059, #6743, #9250, #12755, #6033, #5360 ) ) ;
#4361=CARTESIAN_POINT ( 'NONE',  ( 7.897825807688668043, 1.532833846124465271, -7.633607627188378153 ) ) ;
#4362=CARTESIAN_POINT ( 'NONE',  ( 2.131511515620586383, 3.916244202832140253, -6.187499998634407028 ) ) ;
#4366=CARTESIAN_POINT ( 'NONE',  ( 3.753672977998667726, 3.033343224707664376, -7.249999998634409692 ) ) ;
#4371=VECTOR ( 'NONE', #11419, 1000.000000000000000 ) ;
#4373=CARTESIAN_POINT ( 'NONE',  ( 4.406466114818385904, -6.116179640278937235, -7.446478553995120819 ) ) ;
#4376=CARTESIAN_POINT ( 'NONE',  ( -1.415196051561583790, 4.795541693661363958, -3.624999997268816276 ) ) ;
#4379=ORIENTED_EDGE ( 'NONE', *, *, #8182, .T. ) ;
#4384=DIRECTION ( 'NONE',  ( 0.000000000000000000, 0.000000000000000000, 1.000000000000000000 ) ) ;
#4389=CARTESIAN_POINT ( 'NONE',  ( -3.916244202832140253, 2.131511515620587272, -0.1874999986344084990 ) ) ;
#4392=EDGE_LOOP ( 'NONE', ( #10584, #1758 ) ) ;
#4399=CARTESIAN_POINT ( 'NONE',  ( 3.916244202832140253, -2.131511515620588160, 1.312500001365592750 ) ) ;
#4403=CARTESIAN_POINT ( 'NONE',  ( 7.500000000000000888, 1.489914625144004523, -0.1187923833806749097 ) ) ;
#4404=CARTESIAN_POINT ( 'NONE',  ( -3.401574460001765221, 4.209348295687701302, -2.562499997268814944 ) ) ;
#4414=CARTESIAN_POINT ( 'NONE',  ( -4.795541693661363958, -1.415196051561583790, -5.500000000000001776 ) ) ;
#4417=CARTESIAN_POINT ( 'NONE',  ( -4.391654775818395251, 2.390265326283148806, -7.625000000000003553 ) ) ;
#4421=CARTESIAN_POINT ( 'NONE',  ( 3.753672977998667726, 3.033343224707664376, -1.249999998634407916 ) ) ;
#4431=CARTESIAN_POINT ( 'NONE',  ( 4.999999999999845457, -1.272547481429021854, -6.086597482644649837 ) ) ;
#4433=CARTESIAN_POINT ( 'NONE',  ( -0.5093500532425060401, -4.799145180956616130, -4.624999998634405252 ) ) ;
#4436=CARTESIAN_POINT ( 'NONE',  ( -4.795541693661363958, -1.415196051561583790, 1.499999999999997780 ) ) ;
#4448=CARTESIAN_POINT ( 'NONE',  ( 7.499999999999999112, -2.930060224340428121, -0.4701183149080244705 ) ) ;
#4449=DIRECTION ( 'NONE',  ( 1.000000000000000000, 0.000000000000000000, 0.000000000000000000 ) ) ;
#4451=CARTESIAN_POINT ( 'NONE',  ( 5.000000000000004441, -2.247904837838113790E-16, -2.045263047592944528 ) ) ;
#4458=DIRECTION ( 'NONE',  ( 0.000000000000000000, 0.000000000000000000, 1.000000000000000000 ) ) ;
#4464=CARTESIAN_POINT ( 'NONE',  ( -4.419133455864435511, 6.108866147516203604, -7.026396753507444082 ) ) ;
#4465=B_SPLINE_CURVE_WITH_KNOTS ( 'NONE', 3,
 ( #6614, #9049, #13952, #10339, #15265, #9124 ),
 .UNSPECIFIED., .F., .F.,
 ( 4, 2, 4 ),
 ( 0.000000000000000000, 0.0004189869898914129693, 0.0008379739797828259385 ),
 .UNSPECIFIED. ) ;
#4471=DIRECTION ( 'NONE',  ( 1.000000000000000000, 0.000000000000000000, 0.000000000000000000 ) ) ;
#4472=CARTESIAN_POINT ( 'NONE',  ( -5.381735091635034607, 0.5711823568785950878, -6.437499997268815832 ) ) ;
#4477=CARTESIAN_POINT ( 'NONE',  ( 0.000000000000000000, 0.000000000000000000, 0.000000000000000000 ) ) ;
#4486=DIRECTION ( 'NONE',  ( 0.000000000000000000, 0.000000000000000000, 1.000000000000000000 ) ) ;
#4489=CARTESIAN_POINT ( 'NONE',  ( -0.5711823568785977523, -5.381735091635034607, -5.312499999999999112 ) ) ;
#4492=( GEOMETRIC_REPRESENTATION_CONTEXT ( 3 ) GLOBAL_UNCERTAINTY_ASSIGNED_CONTEXT ( ( #2527 ) ) GLOBAL_UNIT_ASSIGNED_CONTEXT ( ( #14882, #14554, #1132 ) ) REPRESENTATION_CONTEXT ( 'NONE', 'WORKASPACE' ) );
#4497=CARTESIAN_POINT ( 'NONE',  ( -1.261996585732579224, 4.276409079477648589, -2.062499998634406584 ) ) ;
#4499=CARTESIAN_POINT ( 'NONE',  ( 6.484173630540333910, 4.916614646778451281, -7.642786413620781261 ) ) ;
#4503=CARTESIAN_POINT ( 'NONE',  ( 4.209348295687701302, 3.401574460001766109, -7.937500000000003553 ) ) ;
#4505=AXIS2_PLACEMENT_3D ( 'NONE', #4825, #9829, #4905 ) ;
#4508=CARTESIAN_POINT ( 'NONE',  ( -3.033343224707664820, 3.753672977998667726, -6.999999998634409692 ) ) ;
#4510=EDGE_CURVE ( 'NONE', #11190, #11803, #13982, .T. ) ;
#4512=CARTESIAN_POINT ( 'NONE',  ( -3.916244202832140253, 2.131511515620587272, -6.937499998634407916 ) ) ;
#4525=CARTESIAN_POINT ( 'NONE',  ( -4.795541693661363958, -1.415196051561583790, -7.374999997268815832 ) ) ;
#4527=DIRECTION ( 'NONE',  ( 0.000000000000000000, 0.000000000000000000, -1.000000000000000000 ) ) ;
#4541=CARTESIAN_POINT ( 'NONE',  ( 0.000000000000000000, 0.000000000000000000, -9.226681596905677907 ) ) ;
#4549=CARTESIAN_POINT ( 'NONE',  ( 4.276409079477644148, 1.261996585732577891, 0.6875000013655923059 ) ) ;
#4551=AXIS2_PLACEMENT_3D ( 'NONE', #6245, #14974, #11158 ) ;
#4552=CARTESIAN_POINT ( 'NONE',  ( 0.5093500532425063732, 4.799145180956616130, -3.374999998634407472 ) ) ;
#4553=CARTESIAN_POINT ( 'NONE',  ( -1.415196051561583790, 4.795541693661363958, -0.7500000000000006661 ) ) ;
#4554=CARTESIAN_POINT ( 'NONE',  ( 7.922281120364393914, -4.573931137438281169, -8.047472243342932430 ) ) ;
#4557=DIRECTION ( 'NONE',  ( -0.5000000000000004441, 0.8660254037844383745, 0.000000000000000000 ) ) ;
#4563=VERTEX_POINT ( 'NONE', #1421 ) ;
#4564=CARTESIAN_POINT ( 'NONE',  ( 1.261996585732578113, -4.276409079477644148, -0.8124999986344090264 ) ) ;
#4567=EDGE_CURVE ( 'NONE', #7493, #3963, #6451, .T. ) ;
#4572=CARTESIAN_POINT ( 'NONE',  ( 2.390265326283148806, 4.391654775818395251, -7.875000000000003553 ) ) ;
#4575=CARTESIAN_POINT ( 'NONE',  ( 4.276409079477644148, 1.261996585732577891, 0.6875000013655923059 ) ) ;
#4577=CARTESIAN_POINT ( 'NONE',  ( 2.387978478800976134, 7.281554020289609852, -7.069802615102036114 ) ) ;
#4580=ORIENTED_EDGE ( 'NONE', *, *, #14027, .T. ) ;
#4584=AXIS2_PLACEMENT_3D ( 'NONE', #3360, #8617, #13274 ) ;
#4587=CARTESIAN_POINT ( 'NONE',  ( 4.799145180956616130, -0.5093500532425063732, -7.374999998634407916 ) ) ;
#4590=CARTESIAN_POINT ( 'NONE',  ( -2.131511515620587272, -3.916244202832140253, -7.687499998634407916 ) ) ;
#4594=VERTEX_POINT ( 'NONE', #10160 ) ;
#4597=VERTEX_POINT ( 'NONE', #12961 ) ;
#4606=DIRECTION ( 'NONE',  ( 0.000000000000000000, 0.000000000000000000, 1.000000000000000000 ) ) ;
#4625=CARTESIAN_POINT ( 'NONE',  ( -5.112021521198794716, 5.708827036477132744, -7.069802615102390497 ) ) ;
#4629=DIRECTION ( 'NONE',  ( -1.000000000000000000, 1.224646799147354686E-16, 0.000000000000000000 ) ) ;
#4631=FACE_OUTER_BOUND ( 'NONE', #14557, .T. ) ;
#4633=CARTESIAN_POINT ( 'NONE',  ( -4.799145180956616130, 0.5093500532425063732, -2.124999998634406584 ) ) ;
#4638=DIRECTION ( 'NONE',  ( 1.000000000000000000, 0.000000000000000000, 0.000000000000000000 ) ) ;
#4651=CARTESIAN_POINT ( 'NONE',  ( 5.381735091635035495, -0.5711823568785978633, -0.9374999972688153882 ) ) ;
#4655=CARTESIAN_POINT ( 'NONE',  ( 0.5093500532425063732, 4.799145180956616130, 0.8750000013655920839 ) ) ;
#4658=EDGE_CURVE ( 'NONE', #2247, #14425, #13142, .T. ) ;
#4670=CARTESIAN_POINT ( 'NONE',  ( 0.5711823568785989735, 5.381735091635026613, -0.8124999999999997780 ) ) ;
#4672=CARTESIAN_POINT ( 'NONE',  ( 3.768577604424125038, -3.256865806044285439, -0.01833770324489448003 ) ) ;
#4688=DIRECTION ( 'NONE',  ( 1.000000000000000000, 0.000000000000000000, 0.000000000000000000 ) ) ;
#4706=CARTESIAN_POINT ( 'NONE',  ( 3.033343224707661712, -3.753672977998669946, -1.499999998634408138 ) ) ;
#4709=CARTESIAN_POINT ( 'NONE',  ( -4.276409079477644148, -1.261996585732578335, -1.062499998634405696 ) ) ;
#4716=EDGE_LOOP ( 'NONE', ( #8704, #3884, #9460, #812 ) ) ;
#4720=CARTESIAN_POINT ( 'NONE',  ( -1.261996585732579224, 4.276409079477648589, -3.312499998634407916 ) ) ;
#4727=CARTESIAN_POINT ( 'NONE',  ( -3.401574460001764777, 4.209348295687701302, -0.5624999972688170535 ) ) ;
#4731=CARTESIAN_POINT ( 'NONE',  ( 1.261996585732578113, -4.276409079477644148, -5.562499998634406140 ) ) ;
#4733=CARTESIAN_POINT ( 'NONE',  ( -4.336808689942017736E-16, 9.147862274876558786, -8.047472243342932430 ) ) ;
#4749=CARTESIAN_POINT ( 'NONE',  ( -0.5711823568785978633, -5.381735091635035495, -1.312500000000000444 ) ) ;
#4750=CARTESIAN_POINT ( 'NONE',  ( 5.000000000000002665, 1.275685995473128912E-14, -4.045263047592942307 ) ) ;
#4753=CARTESIAN_POINT ( 'NONE',  ( 3.753672977998667726, 3.033343224707664376, -1.499999998634408138 ) ) ;
#4757=ORIENTED_EDGE ( 'NONE', *, *, #1485, .T. ) ;
#4771=CARTESIAN_POINT ( 'NONE',  ( -5.000000000000091482, -0.7223674278660691117, -1.396799362785968501 ) ) ;
#4778=SURFACE_STYLE_USAGE ( .BOTH. , #9702 ) ;
#4785=CARTESIAN_POINT ( 'NONE',  ( 4.391654775818395251, -2.390265326283149694, -3.999999997268816720 ) ) ;
#4786=CARTESIAN_POINT ( 'NONE',  ( -4.276409079477644148, -1.261996585732578335, 0.1875000013655918341 ) ) ;
#4789=AXIS2_PLACEMENT_3D ( 'NONE', #965, #5892, #6135 ) ;
#4790=CARTESIAN_POINT ( 'NONE',  ( -3.753672977998669946, -3.033343224707661712, -2.999999998634409248 ) ) ;
#4800=CARTESIAN_POINT ( 'NONE',  ( -2.131511515620587272, -3.916244202832140253, -3.937499998634408360 ) ) ;
#4802=ADVANCED_FACE ( 'NONE', ( #3357 ), #15650, .T. ) ;
#4807=CARTESIAN_POINT ( 'NONE',  ( -7.894787914004613327, -1.222495057920810896E-13, -7.591390474663425536 ) ) ;
#4810=CARTESIAN_POINT ( 'NONE',  ( 0.5711823568785989735, 5.381735091635026613, 0.3125000027311818918 ) ) ;
#4813=( LENGTH_UNIT ( ) NAMED_UNIT ( * ) SI_UNIT ( .MILLI., .METRE. ) );
#4815=CARTESIAN_POINT ( 'NONE',  ( -0.5093500532425060401, -4.799145180956616130, -5.624999998634406140 ) ) ;
#4818=ORIENTED_EDGE ( 'NONE', *, *, #6863, .T. ) ;
#4825=CARTESIAN_POINT ( 'NONE',  ( 0.000000000000000000, 0.000000000000000000, -25.03750572909317285 ) ) ;
#4831=CARTESIAN_POINT ( 'NONE',  ( -4.209348295687703967, -3.401574460001763001, -1.437500000000001998 ) ) ;
#4835=CARTESIAN_POINT ( 'NONE',  ( -4.799145180956616130, 0.5093500532425063732, -1.124999998634405918 ) ) ;
#4847=EDGE_LOOP ( 'NONE', ( #3938, #9513, #6010, #14921, #1131, #12632 ) ) ;
#4867=EDGE_CURVE ( 'NONE', #7219, #3541, #15551, .T. ) ;
#4873=CARTESIAN_POINT ( 'NONE',  ( -0.5093500532425060401, -4.799145180956616130, 0.3750000013655915843 ) ) ;
#4877=CARTESIAN_POINT ( 'NONE',  ( -3.916244202832140253, 2.131511515620587272, -1.187499998634405918 ) ) ;
#4882=EDGE_LOOP ( 'NONE', ( #9583, #6616, #2038 ) ) ;
#4884=CARTESIAN_POINT ( 'NONE',  ( -0.5093500532425060401, -4.799145180956616130, -1.874999998634406584 ) ) ;
#4891=CARTESIAN_POINT ( 'NONE',  ( -4.209348295687703967, -3.401574460001763001, -1.312499997268813834 ) ) ;
#4897=CARTESIAN_POINT ( 'NONE',  ( 0.5093500532425063732, 4.799145180956616130, -3.124999998634407916 ) ) ;
#4905=DIRECTION ( 'NONE',  ( 1.000000000000000000, 0.000000000000000000, 0.000000000000000000 ) ) ;
#4909=CARTESIAN_POINT ( 'NONE',  ( -4.795541693661363958, -1.415196051561583790, 0.4999999999999970024 ) ) ;
#4911=CARTESIAN_POINT ( 'NONE',  ( 2.971083655575039728, -3.963652976736657507, -0.03751319233342364362 ) ) ;
#4914=CARTESIAN_POINT ( 'NONE',  ( -2.131511515620587272, -3.916244202832140253, -3.937499998634408360 ) ) ;
#4915=VERTEX_POINT ( 'NONE', #13270 ) ;
#4916=CARTESIAN_POINT ( 'NONE',  ( -7.500000000000007105, -0.7512838658081422150, -2.971391578968086378E-15 ) ) ;
#4917=ORIENTED_EDGE ( 'NONE', *, *, #6093, .F. ) ;
#4919=CARTESIAN_POINT ( 'NONE',  ( -7.500000000000003553, -3.948305025207483610, -7.349903712355165375 ) ) ;
#4927=LINE ( 'NONE', #10907, #15566 ) ;
#4931=CYLINDRICAL_SURFACE ( 'NONE', #3084, 5.000000000000000888 ) ;
#4945=CARTESIAN_POINT ( 'NONE',  ( -1.261996585732579224, 4.276409079477648589, -3.062499998634407472 ) ) ;
#4948=CARTESIAN_POINT ( 'NONE',  ( -3.753672977998669946, -3.033343224707661712, -3.999999998634410137 ) ) ;
#4956=CARTESIAN_POINT ( 'NONE',  ( 2.131511515620586383, 3.916244202832140253, -4.437499998634405252 ) ) ;
#4960=CARTESIAN_POINT ( 'NONE',  ( -4.795541693661363958, -1.415196051561583790, -2.500000000000002220 ) ) ;
#4964=CARTESIAN_POINT ( 'NONE',  ( 4.391654775818395251, -2.390265326283149694, 1.000000002731184168 ) ) ;
#4966=CARTESIAN_POINT ( 'NONE',  ( -4.081282237088195153, 2.167655003740347475, -0.2732678705139793274 ) ) ;
#4969=CARTESIAN_POINT ( 'NONE',  ( 4.276409079477644148, 1.261996585732577891, -3.312499998634407916 ) ) ;
#4971=ORIENTED_EDGE ( 'NONE', *, *, #2238, .F. ) ;
#4983=CARTESIAN_POINT ( 'NONE',  ( 4.391654732552941809, -2.390265405775130692, 0.000000000000000000 ) ) ;
#4985=CARTESIAN_POINT ( 'NONE',  ( 1.415196051561583790, -4.795541693661363958, -1.250000000000001110 ) ) ;
#4989=CARTESIAN_POINT ( 'NONE',  ( -3.033343224707664376, 3.753672977998667726, -4.249999998634406140 ) ) ;
#5006=DIRECTION ( 'NONE',  ( 1.000000000000000000, 0.000000000000000000, 0.000000000000000000 ) ) ;
#5008=CARTESIAN_POINT ( 'NONE',  ( 3.753672977998667726, 3.033343224707664820, -8.499999998634411469 ) ) ;
#5014=( NAMED_UNIT ( * ) SI_UNIT ( $, .STERADIAN. ) SOLID_ANGLE_UNIT ( ) );
#5023=CARTESIAN_POINT ( 'NONE',  ( -3.753672977998669946, -3.033343224707661712, -3.749999998634409692 ) ) ;
#5025=CARTESIAN_POINT ( 'NONE',  ( -3.033343224707664376, 3.753672977998667726, -5.249999998634407028 ) ) ;
#5038=CARTESIAN_POINT ( 'NONE',  ( -4.276409079477644148, -1.261996585732578335, -2.062499998634406584 ) ) ;
#5041=EDGE_CURVE ( 'NONE', #2454, #5622, #14763, .T. ) ;
#5047=CARTESIAN_POINT ( 'NONE',  ( -5.381735091635034607, 0.5711823568785950878, -4.437499997268819385 ) ) ;
#5053=CARTESIAN_POINT ( 'NONE',  ( -4.276409079477644148, -1.261996585732578335, -2.812499998634407472 ) ) ;
#5066=CARTESIAN_POINT ( 'NONE',  ( -5.000000000000015987, 5.773502691896279515, -7.063244554130010400 ) ) ;
#5069=CARTESIAN_POINT ( 'NONE',  ( 0.5711823568785989735, 5.381735091635026613, -3.812499999999998668 ) ) ;
#5071=FACE_BOUND ( 'NONE', #9706, .T. ) ;
#5074=CARTESIAN_POINT ( 'NONE',  ( 4.276409079477644148, 1.261996585732577891, -4.562499998634405252 ) ) ;
#5087=CARTESIAN_POINT ( 'NONE',  ( 2.623433461001182909, -7.604994000793865006, -7.633824513837115688 ) ) ;
#5088=CARTESIAN_POINT ( 'NONE',  ( 2.131511515620586383, 3.916244202832140253, -1.187499998634405918 ) ) ;
#5111=CARTESIAN_POINT ( 'NONE',  ( 2.131511515620586383, 3.916244202832140253, -5.437499998634406140 ) ) ;
#5113=CONICAL_SURFACE ( 'NONE', #6670, 7.500000000000001776, 0.8594454914424796144 ) ;
#5118=CARTESIAN_POINT ( 'NONE',  ( -7.500000000000000000, -4.330127018922196314, -7.422398894150035176 ) ) ;
#5121=EDGE_LOOP ( 'NONE', ( #9152, #2682, #10393, #11784, #8317, #10873, #3383 ) ) ;
#5123=DIRECTION ( 'NONE',  ( 1.000000000000000000, 0.000000000000000000, 0.000000000000000000 ) ) ;
#5127=CARTESIAN_POINT ( 'NONE',  ( 3.753672977998667726, 3.033343224707664820, -6.499999998634408804 ) ) ;
#5130=VECTOR ( 'NONE', #5585, 1000.000000000000000 ) ;
#5136=CARTESIAN_POINT ( 'NONE',  ( -4.795541693661363958, -1.415196051561583790, -5.374999997268817609 ) ) ;
#5139=CARTESIAN_POINT ( 'NONE',  ( -3.912039780753109763, 2.444181052284501110, -0.2789798816695437944 ) ) ;
#5143=CARTESIAN_POINT ( 'NONE',  ( -5.000000000000004441, -1.011557177027151181E-15, -4.545263047592944083 ) ) ;
#5144=CARTESIAN_POINT ( 'NONE',  ( -3.033343224707664376, 3.753672977998667726, -6.999999998634408804 ) ) ;
#5158=CARTESIAN_POINT ( 'NONE',  ( -5.381735091635034607, 0.5711823568785950878, -6.562500000000004441 ) ) ;
#5163=CARTESIAN_POINT ( 'NONE',  ( 4.276409079477644148, 1.261996585732577891, -5.562499998634406140 ) ) ;
#5173=CARTESIAN_POINT ( 'NONE',  ( -2.131511515620587272, -3.916244202832140253, -0.6874999986344054737 ) ) ;
#5174=CARTESIAN_POINT ( 'NONE',  ( 1.620853800412707768, 4.162292401171781897, -0.3789984458506779896 ) ) ;
#5179=EDGE_CURVE ( 'NONE', #10281, #2882, #11535, .T. ) ;
#5190=CARTESIAN_POINT ( 'NONE',  ( 7.914973979435151463, 3.817460047930444134, -7.907502498112419786 ) ) ;
#5193=CARTESIAN_POINT ( 'NONE',  ( 1.261996585732578113, -4.276409079477644148, -5.812499998634406140 ) ) ;
#5195=DIRECTION ( 'NONE',  ( 0.000000000000000000, 0.000000000000000000, -1.000000000000000000 ) ) ;
#5200=CARTESIAN_POINT ( 'NONE',  ( 4.391654775818395251, -2.390265326283149694, -7.125000000000002665 ) ) ;
#5202=CARTESIAN_POINT ( 'NONE',  ( -0.5093500532425060401, -4.799145180956616130, -6.874999998634407916 ) ) ;
#5204=EDGE_CURVE ( 'NONE', #1816, #4597, #6018, .T. ) ;
#5208=CARTESIAN_POINT ( 'NONE',  ( 2.390265326283148806, 4.391654775818395251, -5.749999997268814944 ) ) ;
#5210=CARTESIAN_POINT ( 'NONE',  ( -1.502104865711912707, 4.262924311968062874, -0.3382386524005038808 ) ) ;
#5214=CARTESIAN_POINT ( 'NONE',  ( 1.261996585732578113, -4.276409079477644148, -7.562499998634407916 ) ) ;
#5223=EDGE_CURVE ( 'NONE', #14394, #2454, #6907, .T. ) ;
#5224=CARTESIAN_POINT ( 'NONE',  ( -6.602753909532900423, -5.319290460493544259, -7.792447862505331280 ) ) ;
#5225=CARTESIAN_POINT ( 'NONE',  ( -0.3306966981844624009, -8.469326210127480437, -7.349897473154090477 ) ) ;
#5228=CARTESIAN_POINT ( 'NONE',  ( -2.390265326283148806, -4.391654775818394363, -3.375000000000003109 ) ) ;
#5232=CARTESIAN_POINT ( 'NONE',  ( -0.5093500532425060401, -4.799145180956616130, -5.874999998634406140 ) ) ;
#5234=CARTESIAN_POINT ( 'NONE',  ( 5.000000000000000888, 0.000000000000000000, -25.03750572909317285 ) ) ;
#5246=CARTESIAN_POINT ( 'NONE',  ( 7.922281120364393914, -4.573931137438281169, -8.047472243342932430 ) ) ;
#5247=CARTESIAN_POINT ( 'NONE',  ( 4.276409079477644148, 1.261996585732577891, -2.312499998634407028 ) ) ;
#5264=CARTESIAN_POINT ( 'NONE',  ( 5.000000000000091482, 0.7223674278660682235, -1.896799362785968945 ) ) ;
#5266=CARTESIAN_POINT ( 'NONE',  ( -5.000000000000004441, -1.011557177027151181E-15, -5.545263047592944972 ) ) ;
#5268=CARTESIAN_POINT ( 'NONE',  ( -1.261996585732579224, 4.276409079477648589, -5.312499998634406140 ) ) ;
#5270=ORIENTED_EDGE ( 'NONE', *, *, #6700, .F. ) ;
#5274=CARTESIAN_POINT ( 'NONE',  ( -5.000000000000004441, -7.530481206757679743E-15, -1.545263047592943861 ) ) ;
#5279=CARTESIAN_POINT ( 'NONE',  ( 0.5093500532425063732, 4.799145180956616130, -6.374999998634408804 ) ) ;
#5286=CARTESIAN_POINT ( 'NONE',  ( 3.401574460001763001, -4.209348295687703967, -4.062499997268816720 ) ) ;
#5288=CARTESIAN_POINT ( 'NONE',  ( -4.671041856245029322, -9.682850088987660890E-14, -0.2303389720127052009 ) ) ;
#5293=CARTESIAN_POINT ( 'NONE',  ( 7.500000000000001776, 3.608439182435154269, -7.298562697733103732 ) ) ;
#5299=ORIENTED_EDGE ( 'NONE', *, *, #6961, .F. ) ;
#5300=CARTESIAN_POINT ( 'NONE',  ( -5.000000000000004441, -7.530481206757679743E-15, -0.5452630475929430842 ) ) ;
#5304=AXIS2_PLACEMENT_3D ( 'NONE', #531, #15233, #8044 ) ;
#5308=CARTESIAN_POINT ( 'NONE',  ( 3.401574460001763001, -4.209348295687703967, -7.187500000000003553 ) ) ;
#5309=CARTESIAN_POINT ( 'NONE',  ( 4.795541693661363958, 1.415196051561583790, -3.000000000000002665 ) ) ;
#5313=CARTESIAN_POINT ( 'NONE',  ( -3.916244202832140253, 2.131511515620587272, -8.187499998634407916 ) ) ;
#5317=ADVANCED_FACE ( 'NONE', ( #4631 ), #13657, .F. ) ;
#5330=CARTESIAN_POINT ( 'NONE',  ( 3.916244202832140253, -2.131511515620588160, -0.4374999986344086933 ) ) ;
#5331=CARTESIAN_POINT ( 'NONE',  ( 3.175402709531165435, 3.141463792224340690, -0.3789984458506759912 ) ) ;
#5334=CARTESIAN_POINT ( 'NONE',  ( -3.916244202832140253, 2.131511515620587272, -1.937499998634406584 ) ) ;
#5352=CARTESIAN_POINT ( 'NONE',  ( -5.000000000000004441, -7.530481206757679743E-15, -1.420263044861758361 ) ) ;
#5354=CARTESIAN_POINT ( 'NONE',  ( 0.5711823568785988625, 5.381735091635026613, -0.6874999972688190519 ) ) ;
#5356=CARTESIAN_POINT ( 'NONE',  ( -1.415196051561583790, 4.795541693661363958, -7.624999997268816720 ) ) ;
#5359=EDGE_CURVE ( 'NONE', #3959, #1601, #9920, .T. ) ;
#5360=ORIENTED_EDGE ( 'NONE', *, *, #3426, .F. ) ;
#5363=CARTESIAN_POINT ( 'NONE',  ( 3.401574460001763445, -4.209348295687703079, -7.187500000000003553 ) ) ;
#5366=EDGE_LOOP ( 'NONE', ( #14016, #14928, #1525, #9554 ) ) ;
#5367=CARTESIAN_POINT ( 'NONE',  ( -3.916244202832140253, 2.131511515620587272, -7.187499998634407916 ) ) ;
#5369=CARTESIAN_POINT ( 'NONE',  ( 3.401574460001763445, -4.209348295687703079, -5.062499997268816720 ) ) ;
#5372=CARTESIAN_POINT ( 'NONE',  ( 4.209348295687701302, 3.401574460001765665, -2.812499997268815388 ) ) ;
#5378=CARTESIAN_POINT ( 'NONE',  ( -4.276409079477644148, -1.261996585732578335, -7.812499998634407916 ) ) ;
#5386=LINE ( 'NONE', #7749, #1737 ) ;
#5395=CARTESIAN_POINT ( 'NONE',  ( 5.381735091635035495, -0.5711823568785978633, -6.062500000000000000 ) ) ;
#5401=CARTESIAN_POINT ( 'NONE',  ( -4.276409079477644148, -1.261996585732578335, -8.062499998634407916 ) ) ;
#5402=VERTEX_POINT ( 'NONE', #5633 ) ;
#5411=VECTOR ( 'NONE', #3352, 1000.000000000000000 ) ;
#5412=CARTESIAN_POINT ( 'NONE',  ( 7.915340744419800068, 3.857466640755369713, -7.913699667208869748 ) ) ;
#5414=CARTESIAN_POINT ( 'NONE',  ( -4.799145180956616130, 0.5093500532425063732, -2.874999998634407472 ) ) ;
#5417=( BOUNDED_CURVE ( )  B_SPLINE_CURVE ( 2, ( #14668, #12304, #1241, #6190, #11983, #15886, #13271, #9646, #4960, #46, #8307 ),
 .UNSPECIFIED., .F., .F. ) 
 B_SPLINE_CURVE_WITH_KNOTS ( ( 3, 2, 2, 2, 2, 3 ),
 ( 0.4045872658012772960, 0.4124999999999999778, 0.4249999999999999889, 0.4375000000000000000, 0.4500000000000000111, 0.4545872658012772849 ),
 .UNSPECIFIED. ) 
 CURVE ( )  GEOMETRIC_REPRESENTATION_ITEM ( )  RATIONAL_B_SPLINE_CURVE ( ( 0.9646335149384805963, 0.9518143178943438976, 1.000000000000000000, 0.9238795325112867385, 1.000000000000000000, 0.9238795325112867385, 1.000000000000000000, 0.9238795325112867385, 1.000000000000000000, 0.9720652146169430630, 0.9646335149384808183 ) ) 
 REPRESENTATION_ITEM ( '' )  );
#5419=CARTESIAN_POINT ( 'NONE',  ( 1.261996585732578113, -4.276409079477644148, -5.562499998634406140 ) ) ;
#5423=CARTESIAN_POINT ( 'NONE',  ( -4.209348295687703079, -3.401574460001763445, -3.437500000000003553 ) ) ;
#5425=CARTESIAN_POINT ( 'NONE',  ( 7.112481253774558532, -4.553861071371746227, -7.781689322726583313 ) ) ;
#5430=CARTESIAN_POINT ( 'NONE',  ( 7.549006887134069643, 4.358421158401189821, -7.700127545397313256 ) ) ;
#5446=CARTESIAN_POINT ( 'NONE',  ( 5.000000000000002665, 1.275685995473128912E-14, -5.045263047592944083 ) ) ;
#5449=EDGE_CURVE ( 'NONE', #14394, #11190, #10960, .T. ) ;
#5450=CARTESIAN_POINT ( 'NONE',  ( -5.000000000000095035, -0.7223674278660573433, -5.396799362785971610 ) ) ;
#5452=CARTESIAN_POINT ( 'NONE',  ( 0.5711823568785989735, 5.381735091635026613, -6.687499997268816720 ) ) ;
#5458=CARTESIAN_POINT ( 'NONE',  ( -3.916244202832140253, 2.131511515620587272, -6.937499998634407916 ) ) ;
#5463=ORIENTED_EDGE ( 'NONE', *, *, #9039, .F. ) ;
#5464=CARTESIAN_POINT ( 'NONE',  ( -7.264118654998712010, 4.945491722146219793, -7.907633014911223945 ) ) ;
#5467=ADVANCED_FACE ( 'NONE', ( #11034 ), #10800, .F. ) ;
#5477=CARTESIAN_POINT ( 'NONE',  ( -3.033343224707664376, 3.753672977998667726, -7.249999998634409692 ) ) ;
#5480=ORIENTED_EDGE ( 'NONE', *, *, #9158, .F. ) ;
#5484=ADVANCED_FACE ( 'NONE', ( #5866 ), #15332, .F. ) ;
#5489=CARTESIAN_POINT ( 'NONE',  ( -4.276409079477644148, -1.261996585732578335, -4.812499998634405252 ) ) ;
#5490=CARTESIAN_POINT ( 'NONE',  ( -4.391654775818395251, 2.390265326283148806, -5.499999997268814944 ) ) ;
#5492=CARTESIAN_POINT ( 'NONE',  ( -2.131511515620587272, -3.916244202832140253, -6.687499998634407028 ) ) ;
#5496=FACE_OUTER_BOUND ( 'NONE', #14570, .T. ) ;
#5498=DIRECTION ( 'NONE',  ( 0.000000000000000000, 0.000000000000000000, 1.000000000000000000 ) ) ;
#5506=DIRECTION ( 'NONE',  ( 0.000000000000000000, 0.000000000000000000, 1.000000000000000000 ) ) ;
#5509=CARTESIAN_POINT ( 'NONE',  ( 7.908030677224555660, -3.059924800338350792, -7.792662696733365202 ) ) ;
#5512=CARTESIAN_POINT ( 'NONE',  ( -5.000000000000002665, 1.292545281756915047E-15, -0.4202630448617610814 ) ) ;
#5521=CARTESIAN_POINT ( 'NONE',  ( -7.169303301815265428, 4.521054846639298574, -7.349897473155284189 ) ) ;
#5527=CARTESIAN_POINT ( 'NONE',  ( -4.276409079477644148, -1.261996585732578335, 0.9375000013655925279 ) ) ;
#5529=CARTESIAN_POINT ( 'NONE',  ( -4.999999999999849898, 1.272547481429008309, -1.586597482644648505 ) ) ;
#5532=CARTESIAN_POINT ( 'NONE',  ( 7.500000000000000000, 2.932633423934446260, -0.4709827563909316783 ) ) ;
#5540=EDGE_CURVE ( 'NONE', #14394, #637, #10587, .T. ) ;
#5545=CARTESIAN_POINT ( 'NONE',  ( -7.500000000000006217, 0.7513028741560140444, -0.02472015219303315067 ) ) ;
#5555=CARTESIAN_POINT ( 'NONE',  ( 4.799145180956616130, -0.5093500532425063732, -0.3749999986344090264 ) ) ;
#5561=ADVANCED_FACE ( 'NONE', ( #15542 ), #8036, .F. ) ;
#5568=CARTESIAN_POINT ( 'NONE',  ( 1.415196051561583790, -4.795541693661363958, -6.250000000000001776 ) ) ;
#5570=CARTESIAN_POINT ( 'NONE',  ( -1.261996585732579224, 4.276409079477648589, -6.062499998634407028 ) ) ;
#5571=CARTESIAN_POINT ( 'NONE',  ( 2.602085213965210642E-15, 8.660254037844392627, -1.000000000000000888 ) ) ;
#5574=CARTESIAN_POINT ( 'NONE',  ( -3.753672977998669946, -3.033343224707661712, -6.749999998634408804 ) ) ;
#5582=CARTESIAN_POINT ( 'NONE',  ( 5.000000000000004441, -2.247904837838113790E-16, -7.045263047592947636 ) ) ;
#5585=DIRECTION ( 'NONE',  ( 0.000000000000000000, 0.000000000000000000, 1.000000000000000000 ) ) ;
#5586=AXIS2_PLACEMENT_3D ( 'NONE', #11296, #247, #8880 ) ;
#5593=EDGE_CURVE ( 'NONE', #3963, #1816, #14286, .T. ) ;
#5601=CARTESIAN_POINT ( 'NONE',  ( 0.2779000157839381924, 8.820699686765076208, -7.928862157988310955 ) ) ;
#5611=CARTESIAN_POINT ( 'NONE',  ( 3.401574460001763001, -4.209348295687703967, -7.062499997268814944 ) ) ;
#5614=CARTESIAN_POINT ( 'NONE',  ( 4.795541693661363958, 1.415196051561583790, -2.000000000000001776 ) ) ;
#5618=CARTESIAN_POINT ( 'NONE',  ( -5.000000000000004441, -7.530481206757679743E-15, -2.420263044861759472 ) ) ;
#5622=VERTEX_POINT ( 'NONE', #8349 ) ;
#5625=CARTESIAN_POINT ( 'NONE',  ( -7.500000000000005329, 4.330127018922194537, -0.9999999999999974465 ) ) ;
#5633=CARTESIAN_POINT ( 'NONE',  ( -10.39117206796836079, 1.272551561242683567E-15, -8.499999999999996447 ) ) ;
#5637=CARTESIAN_POINT ( 'NONE',  ( -1.261996585732579224, 4.276409079477648589, -1.062499998634405696 ) ) ;
#5643=VECTOR ( 'NONE', #5195, 1000.000000000000000 ) ;
#5650=CARTESIAN_POINT ( 'NONE',  ( 4.799145180956616130, -0.5093500532425063732, -4.374999998634405252 ) ) ;
#5655=CARTESIAN_POINT ( 'NONE',  ( 4.276409079477644148, 1.261996585732577891, -6.312499998634407028 ) ) ;
#5662=CARTESIAN_POINT ( 'NONE',  ( 6.486836893983276120, -4.915077010913956101, -7.231838333420564702 ) ) ;
#5675=CARTESIAN_POINT ( 'NONE',  ( -5.000000000000004441, -1.011557177027151181E-15, -4.545263047592944083 ) ) ;
#5677=CARTESIAN_POINT ( 'NONE',  ( 6.874999999999997335, -4.690970937165719334, -7.298562697733109061 ) ) ;
#5684=CARTESIAN_POINT ( 'NONE',  ( -4.999999999999844569, 1.272547481429019856, -4.586597482644648949 ) ) ;
#5685=CARTESIAN_POINT ( 'NONE',  ( -5.000000000000004441, -7.530481206757679743E-15, -3.420263044861759916 ) ) ;
#5687=CARTESIAN_POINT ( 'NONE',  ( 3.753672977998667726, 3.033343224707664376, 0.5000000013655936382 ) ) ;
#5692=CARTESIAN_POINT ( 'NONE',  ( 7.500000000000000000, 0.7513028741560167090, -0.02472015219302843916 ) ) ;
#5698=ORIENTED_EDGE ( 'NONE', *, *, #9017, .F. ) ;
#5711=CARTESIAN_POINT ( 'NONE',  ( -4.799145180956616130, 0.5093500532425063732, -1.874999998634406584 ) ) ;
#5713=FACE_OUTER_BOUND ( 'NONE', #3265, .T. ) ;
#5715=ORIENTED_EDGE ( 'NONE', *, *, #9553, .T. ) ;
#5721=CARTESIAN_POINT ( 'NONE',  ( 4.799145180956616130, -0.5093500532425063732, -5.374999998634405252 ) ) ;
#5722=FACE_OUTER_BOUND ( 'NONE', #15453, .T. ) ;
#5723=AXIS2_PLACEMENT_3D ( 'NONE', #13317, #4384, #4688 ) ;
#5725=CARTESIAN_POINT ( 'NONE',  ( -0.5093500532425060401, -4.799145180956616130, -7.624999998634408804 ) ) ;
#5726=CARTESIAN_POINT ( 'NONE',  ( -5.000000000000004441, -1.011557177027151181E-15, -3.545263047592942307 ) ) ;
#5734=CARTESIAN_POINT ( 'NONE',  ( -7.500000000000005329, 4.330127018922194537, -9.999999999999998224 ) ) ;
#5741=ORIENTED_EDGE ( 'NONE', *, *, #15328, .T. ) ;
#5752=CARTESIAN_POINT ( 'NONE',  ( -5.276498195232070643, 6.073236878018064111, -7.633618187056732118 ) ) ;
#5758=CARTESIAN_POINT ( 'NONE',  ( 3.916244202832140253, -2.131511515620588160, 1.562500001365592972 ) ) ;
#5760=CARTESIAN_POINT ( 'NONE',  ( -4.799145180956616130, 0.5093500532425063732, -0.1249999986344088321 ) ) ;
#5762=CARTESIAN_POINT ( 'NONE',  ( 5.000000000000092371, 0.7223674278660651149, -2.021799365517154889 ) ) ;
#5764=VERTEX_POINT ( 'NONE', #10998 ) ;
#5779=CARTESIAN_POINT ( 'NONE',  ( -4.209348295687703967, -3.401574460001763001, -7.437500000000004441 ) ) ;
#5785=CARTESIAN_POINT ( 'NONE',  ( -2.131511515620587272, -3.916244202832140253, -1.687499998634406362 ) ) ;
#5787=CARTESIAN_POINT ( 'NONE',  ( 3.080866544135724361, 6.881514909250313394, -7.026396753507434312 ) ) ;
#5797=CARTESIAN_POINT ( 'NONE',  ( -1.261996585732579224, 4.276409079477648589, -7.062499998634407916 ) ) ;
#5798=CARTESIAN_POINT ( 'NONE',  ( 1.206569728928466034, 7.963640680051485177, -0.4524126574264489831 ) ) ;
#5800=CARTESIAN_POINT ( 'NONE',  ( 0.5093500532425063732, 4.799145180956616130, -7.124999998634407916 ) ) ;
#5816=CARTESIAN_POINT ( 'NONE',  ( -5.000000000000002665, -1.404940523648820476E-14, -7.420263044861759028 ) ) ;
#5824=FACE_OUTER_BOUND ( 'NONE', #507, .T. ) ;
#5826=CARTESIAN_POINT ( 'NONE',  ( 4.391654732552941809, -2.390265405775130692, 0.000000000000000000 ) ) ;
#5830=( BOUNDED_SURFACE ( )  B_SPLINE_SURFACE ( 3, 2, ( 
 ( #13139, #10648, #8239 ),
 ( #15582, #4499, #11918 ),
 ( #9434, #14362, #7016 ),
 ( #5787, #15661, #13205 ),
 ( #4577, #9512, #12077 ),
 ( #10874, #944, #7176 ),
 ( #3369, #8316, #5872 ),
 ( #10805, #8389, #2221 ) ),
 .UNSPECIFIED., .F., .F., .F. ) 
 B_SPLINE_SURFACE_WITH_KNOTS ( ( 4, 2, 2, 4 ),
 ( 3, 3 ),
 ( 0.03861844051980969222, 0.04325213341840641185, 0.04556897986770477166, 0.04788582631700313147 ),
 ( 0.000000000000000000, 1.000000000000000000 ),
 .UNSPECIFIED. ) 
 GEOMETRIC_REPRESENTATION_ITEM ( )  RATIONAL_B_SPLINE_SURFACE ( (
 ( 1.000000000000000000, 0.8047781759831917903, 1.000000000000000000),
 ( 1.000000000000000000, 0.8123762462806505269, 1.000000000000000000),
 ( 1.000000000000000000, 0.8190659850614816495, 1.000000000000000000),
 ( 1.000000000000000000, 0.8191937571014599184, 1.000000000000000000),
 ( 1.000000000000000000, 0.8176092952781195411, 1.000000000000000000),
 ( 1.000000000000000000, 0.8122962088595742092, 1.000000000000000000),
 ( 1.000000000000000000, 0.8086311330828503952, 1.000000000000000000),
 ( 1.000000000000000000, 0.8047712282214323221, 1.000000000000000000) ) ) 
 REPRESENTATION_ITEM ( '' )  SURFACE ( )  );
#5837=DIRECTION ( 'NONE',  ( 1.000000000000000000, 0.000000000000000000, 0.000000000000000000 ) ) ;
#5839=CARTESIAN_POINT ( 'NONE',  ( -5.000000000000091482, -0.7223674278660691117, -3.396799362785969834 ) ) ;
#5841=CARTESIAN_POINT ( 'NONE',  ( -2.131511515620587272, -3.916244202832140253, 1.312500001365592750 ) ) ;
#5845=CARTESIAN_POINT ( 'NONE',  ( 3.916244202832140253, -2.131511515620588160, 0.3125000013655919728 ) ) ;
#5846=CIRCLE ( 'NONE', #15412, 7.500000000000001776 ) ;
#5849=EDGE_LOOP ( 'NONE', ( #942, #5299 ) ) ;
#5866=FACE_OUTER_BOUND ( 'NONE', #14171, .T. ) ;
#5868=FILL_AREA_STYLE ('',( #7171 ) ) ;
#5870=CARTESIAN_POINT ( 'NONE',  ( -2.131511515620587272, -3.916244202832140253, 0.3125000013655919728 ) ) ;
#5872=CARTESIAN_POINT ( 'NONE',  ( 0.6169862416621371137, 8.783631307151244627, -7.913704048099939214 ) ) ;
#5885=CARTESIAN_POINT ( 'NONE',  ( 2.390265326283148806, 4.391654775818395251, -2.875000000000002665 ) ) ;
#5888=CARTESIAN_POINT ( 'NONE',  ( 1.540890760463220044, -4.665335934641420934, -0.06581821247642098693 ) ) ;
#5892=DIRECTION ( 'NONE',  ( 0.000000000000000000, 0.000000000000000000, 1.000000000000000000 ) ) ;
#5917=CIRCLE ( 'NONE', #2255, 5.000000000000000000 ) ;
#5925=CARTESIAN_POINT ( 'NONE',  ( 1.415196051561583790, -4.795541693661363958, -4.124999997268816720 ) ) ;
#5927=CARTESIAN_POINT ( 'NONE',  ( 4.276409079477644148, 1.261996585732577891, -1.312499998634406140 ) ) ;
#5929=( BOUNDED_CURVE ( )  B_SPLINE_CURVE ( 2, ( #5266, #6736, #9001, #13912, #2839, #1627, #589, #6565, #7790, #13984, #3093 ),
 .UNSPECIFIED., .F., .F. ) 
 B_SPLINE_CURVE_WITH_KNOTS ( ( 3, 2, 2, 2, 2, 3 ),
 ( 0.7545872658012773293, 0.7624999999999999556, 0.7750000000000000222, 0.7874999999999999778, 0.8000000000000000444, 0.8045872658012773737 ),
 .UNSPECIFIED. ) 
 CURVE ( )  GEOMETRIC_REPRESENTATION_ITEM ( )  RATIONAL_B_SPLINE_CURVE ( ( 0.9646335149384803742, 0.9518143178943441196, 1.000000000000000000, 0.9238795325112867385, 1.000000000000000000, 0.9238795325112867385, 1.000000000000000000, 0.9238795325112867385, 1.000000000000000000, 0.9720652146169423968, 0.9646335149384803742 ) ) 
 REPRESENTATION_ITEM ( '' )  );
#5930=CARTESIAN_POINT ( 'NONE',  ( 2.131511515620586383, 3.916244202832140253, -0.4374999986344086933 ) ) ;
#5937=VERTEX_POINT ( 'NONE', #5143 ) ;
#5939=CARTESIAN_POINT ( 'NONE',  ( 2.131511515620586383, 3.916244202832140253, -1.437499998634406140 ) ) ;
#5942=ADVANCED_FACE ( 'NONE', ( #15001 ), #13606, .T. ) ;
#5945=CARTESIAN_POINT ( 'NONE',  ( -7.894787914004613327, 0.7647108141804107584, -7.591390474663421095 ) ) ;
#5948=CARTESIAN_POINT ( 'NONE',  ( -0.5711823568785978633, -5.381735091635035495, -0.1874999972688185246 ) ) ;
#5952=CARTESIAN_POINT ( 'NONE',  ( -1.261996585732579224, 4.276409079477648589, -4.062499998634405252 ) ) ;
#5967=CARTESIAN_POINT ( 'NONE',  ( -5.381735091635034607, 0.5711823568785950878, -0.5624999999999995559 ) ) ;
#5971=CARTESIAN_POINT ( 'NONE',  ( 0.5093500532425063732, 4.799145180956616130, 0.6250000013655918618 ) ) ;
#5973=CARTESIAN_POINT ( 'NONE',  ( 7.848314987057847247, -4.129027267381571775, -7.493854785173811983 ) ) ;
#5975=ORIENTED_EDGE ( 'NONE', *, *, #11336, .F. ) ;
#5976=CARTESIAN_POINT ( 'NONE',  ( -7.894955577759749765, 1.603085139987818764, -7.593799241562204649 ) ) ;
#5981=CARTESIAN_POINT ( 'NONE',  ( -3.750000000000004885, 6.495190528383289141, 0.000000000000000000 ) ) ;
#5986=CARTESIAN_POINT ( 'NONE',  ( 3.401574460001763445, -4.209348295687703079, -1.062499997268813612 ) ) ;
#5988=CARTESIAN_POINT ( 'NONE',  ( -5.000000000000003553, -1.404940523648820476E-14, -6.545263047592945860 ) ) ;
#5997=LINE ( 'NONE', #12126, #10460 ) ;
#6001=CARTESIAN_POINT ( 'NONE',  ( -2.131511515620587272, -3.916244202832140253, 0.3125000013655919728 ) ) ;
#6003=CARTESIAN_POINT ( 'NONE',  ( 2.131511515620586383, 3.916244202832140253, -2.437499998634407028 ) ) ;
#6008=CARTESIAN_POINT ( 'NONE',  ( 0.000000000000000000, 0.000000000000000000, 0.000000000000000000 ) ) ;
#6010=ORIENTED_EDGE ( 'NONE', *, *, #11388, .T. ) ;
#6015=CARTESIAN_POINT ( 'NONE',  ( 1.261996585732578113, -4.276409079477644148, -4.812499998634405252 ) ) ;
#6018=( BOUNDED_CURVE ( )  B_SPLINE_CURVE ( 2, ( #6822, #11581, #533, #1960, #1642, #6749, #15239, #10312, #14000, #7881, #4147 ),
 .UNSPECIFIED., .F., .F. ) 
 B_SPLINE_CURVE_WITH_KNOTS ( ( 3, 2, 2, 2, 2, 3 ),
 ( 0.9045872658012773515, 0.9124999999999999778, 0.9250000000000000444, 0.9375000000000000000, 0.9499999999999999556, 0.9545872658012772849 ),
 .UNSPECIFIED. ) 
 CURVE ( )  GEOMETRIC_REPRESENTATION_ITEM ( )  RATIONAL_B_SPLINE_CURVE ( ( 0.9646335149384803742, 0.9518143178943441196, 1.000000000000000000, 0.9238795325112867385, 1.000000000000000000, 0.9238795325112867385, 1.000000000000000000, 0.9238795325112867385, 1.000000000000000000, 0.9720652146169428409, 0.9646335149384808183 ) ) 
 REPRESENTATION_ITEM ( '' )  );
#6019=CARTESIAN_POINT ( 'NONE',  ( 2.131511515620586383, 3.916244202832140253, -8.187499998634407916 ) ) ;
#6024=CARTESIAN_POINT ( 'NONE',  ( -8.673617379884035472E-16, -9.147862274876560562, -8.047472243342939535 ) ) ;
#6026=PRODUCT_DEFINITION ( 'UNKNOWN', '', #3014, #2690 ) ;
#6030=CARTESIAN_POINT ( 'NONE',  ( -4.799145180956616130, 0.5093500532425063732, -3.874999998634404363 ) ) ;
#6033=ORIENTED_EDGE ( 'NONE', *, *, #2677, .F. ) ;
#6043=CARTESIAN_POINT ( 'NONE',  ( 4.391654775818395251, -2.390265326283149694, -3.125000000000002665 ) ) ;
#6044=CARTESIAN_POINT ( 'NONE',  ( 0.5711823568785988625, 5.381735091635026613, -3.812499999999998668 ) ) ;
#6048=CARTESIAN_POINT ( 'NONE',  ( -4.276409079477644148, -1.261996585732578335, -2.062499998634406584 ) ) ;
#6050=CARTESIAN_POINT ( 'NONE',  ( 7.970070017554209407, -4.546953124339768060, -8.057670357645360326 ) ) ;
#6053=CARTESIAN_POINT ( 'NONE',  ( -7.500000000000003553, -1.572902445675431471, -7.069816568113128419 ) ) ;
#6068=CARTESIAN_POINT ( 'NONE',  ( -5.000000000000004441, -1.011557177027151181E-15, -6.420263044861759028 ) ) ;
#6081=CARTESIAN_POINT ( 'NONE',  ( -4.276409079477644148, -1.261996585732578335, 1.187500001365592750 ) ) ;
#6084=CARTESIAN_POINT ( 'NONE',  ( 4.276409079477644148, 1.261996585732577891, 0.4375000013655920839 ) ) ;
#6086=AXIS2_PLACEMENT_3D ( 'NONE', #271, #2833, #185 ) ;
#6093=EDGE_CURVE ( 'NONE', #4594, #10386, #10771, .T. ) ;
#6095=CARTESIAN_POINT ( 'NONE',  ( -0.5093500532425060401, -4.799145180956616130, -2.874999998634407472 ) ) ;
#6105=CARTESIAN_POINT ( 'NONE',  ( 4.795541693661363958, 1.415196051561583790, -1.874999997268814944 ) ) ;
#6111=CARTESIAN_POINT ( 'NONE',  ( -3.916244202832140253, 2.131511515620587272, -3.937499998634404808 ) ) ;
#6112=CARTESIAN_POINT ( 'NONE',  ( -3.750000000000004885, 6.495190528383289141, 0.000000000000000000 ) ) ;
#6124=ADVANCED_FACE ( 'NONE', ( #540 ), #10387, .T. ) ;
#6127=DIRECTION ( 'NONE',  ( 0.000000000000000000, 0.000000000000000000, 1.000000000000000000 ) ) ;
#6129=CARTESIAN_POINT ( 'NONE',  ( 3.401574460001763001, -4.209348295687703967, -1.187500000000001998 ) ) ;
#6130=CARTESIAN_POINT ( 'NONE',  ( -3.401574460001765221, 4.209348295687701302, -3.687500000000000444 ) ) ;
#6131=CARTESIAN_POINT ( 'NONE',  ( 4.257627111623017768, -2.623238587170121594, -0.004444259227768714363 ) ) ;
#6133=CARTESIAN_POINT ( 'NONE',  ( 1.261996585732578113, -4.276409079477644148, -2.812499998634407472 ) ) ;
#6135=DIRECTION ( 'NONE',  ( 1.000000000000000000, 0.000000000000000000, 0.000000000000000000 ) ) ;
#6154=FACE_OUTER_BOUND ( 'NONE', #7747, .T. ) ;
#6161=PRESENTATION_STYLE_ASSIGNMENT (( #4778 ) ) ;
#6170=CARTESIAN_POINT ( 'NONE',  ( -3.753672977998669946, -3.033343224707661712, -2.749999998634409248 ) ) ;
#6173=AXIS2_PLACEMENT_3D ( 'NONE', #14136, #15193, #11771 ) ;
#6174=CARTESIAN_POINT ( 'NONE',  ( -2.131511515620587272, -3.916244202832140253, -4.937499998634406140 ) ) ;
#6179=EDGE_CURVE ( 'NONE', #9532, #2616, #12100, .T. ) ;
#6181=CARTESIAN_POINT ( 'NONE',  ( 1.415196051561583790, -4.795541693661363958, -1.250000000000001110 ) ) ;
#6183=ORIENTED_EDGE ( 'NONE', *, *, #10103, .T. ) ;
#6185=CARTESIAN_POINT ( 'NONE',  ( -4.799145180956616130, 0.5093500532425063732, -4.124999998634405252 ) ) ;
#6190=CARTESIAN_POINT ( 'NONE',  ( 3.401574460001763445, -4.209348295687703079, -2.187500000000002665 ) ) ;
#6192=EDGE_CURVE ( 'NONE', #15071, #1633, #10543, .T. ) ;
#6193=CARTESIAN_POINT ( 'NONE',  ( -4.336808689942017736E-16, -8.660254037844399733, -7.422398894150038728 ) ) ;
#6198=CARTESIAN_POINT ( 'NONE',  ( 3.753672977998667726, 3.033343224707664376, -5.249999998634407028 ) ) ;
#6203=EDGE_CURVE ( 'NONE', #7414, #8156, #8213, .T. ) ;
#6212=CARTESIAN_POINT ( 'NONE',  ( 5.381735091635035495, -0.5711823568785978633, -0.06250000000000287270 ) ) ;
#6213=CARTESIAN_POINT ( 'NONE',  ( -5.000000000000091482, -0.7223674278660691117, -2.396799362785969389 ) ) ;
#6214=CARTESIAN_POINT ( 'NONE',  ( -2.762894178058169725, -3.922440002897376932, -0.1467115563401084066 ) ) ;
#6216=CARTESIAN_POINT ( 'NONE',  ( 1.261996585732578113, -4.276409079477644148, -3.812499998634408360 ) ) ;
#6217=ORIENTED_EDGE ( 'NONE', *, *, #7024, .T. ) ;
#6218=CARTESIAN_POINT ( 'NONE',  ( -7.500000000000004441, -3.988190556646204588, -0.8526458641284350159 ) ) ;
#6219=ORIENTED_EDGE ( 'NONE', *, *, #8065, .T. ) ;
#6235=CARTESIAN_POINT ( 'NONE',  ( -4.795541693661363958, -1.415196051561583790, -6.374999997268815832 ) ) ;
#6242=ORIENTED_EDGE ( 'NONE', *, *, #5041, .F. ) ;
#6245=CARTESIAN_POINT ( 'NONE',  ( 0.000000000000000000, 0.000000000000000000, -25.03750572909317285 ) ) ;
#6247=CARTESIAN_POINT ( 'NONE',  ( -2.131511515620587272, -3.916244202832140253, -2.687499998634407028 ) ) ;
#6250=CARTESIAN_POINT ( 'NONE',  ( 3.916244202832140253, -2.131511515620588160, -5.687499998634406140 ) ) ;
#6260=CARTESIAN_POINT ( 'NONE',  ( 3.033343224707661712, -3.753672977998669502, -1.749999998634408360 ) ) ;
#6261=( BOUNDED_CURVE ( )  B_SPLINE_CURVE ( 2, ( #5826, #1944, #11877, #13169, #13091, #3397, #3094, #590, #903 ),
 .UNSPECIFIED., .F., .F. ) 
 B_SPLINE_CURVE_WITH_KNOTS ( ( 3, 2, 2, 2, 3 ),
 ( 0.1125000002956211415, 0.1250000000000000000, 0.1375000000000000111, 0.1499999999999999944, 0.1545872658012772960 ),
 .UNSPECIFIED. ) 
 CURVE ( )  GEOMETRIC_REPRESENTATION_ITEM ( )  RATIONAL_B_SPLINE_CURVE ( ( 1.000000000000000000, 0.9238795325112867385, 1.000000000000000000, 0.9238795325112867385, 1.000000000000000000, 0.9238795325112867385, 1.000000000000000000, 0.9720652146169428409, 0.9646335149384808183 ) ) 
 REPRESENTATION_ITEM ( '' )  );
#6264=CARTESIAN_POINT ( 'NONE',  ( -1.908195823574487804E-14, -8.660254037844392627, -1.000000000000000888 ) ) ;
#6267=CARTESIAN_POINT ( 'NONE',  ( 1.415196051561583790, -4.795541693661363958, -2.124999997268814944 ) ) ;
#6269=CARTESIAN_POINT ( 'NONE',  ( -5.000000000000004441, -1.011557177027151181E-15, -6.420263044861759028 ) ) ;
#6273=CARTESIAN_POINT ( 'NONE',  ( 1.261996585732578113, -4.276409079477644148, -2.562499998634407028 ) ) ;
#6288=CARTESIAN_POINT ( 'NONE',  ( -7.968863443239230016, -4.547634245050486967, -8.057411785091790790 ) ) ;
#6290=CARTESIAN_POINT ( 'NONE',  ( 2.390265326283148806, 4.391654775818395251, -4.875000000000000888 ) ) ;
#6294=CARTESIAN_POINT ( 'NONE',  ( -3.753672977998669946, -3.033343224707661712, -3.999999998634410137 ) ) ;
#6304=CARTESIAN_POINT ( 'NONE',  ( 2.602085213965210642E-15, 8.660254037844392627, -7.422398894150035176 ) ) ;
#6307=CARTESIAN_POINT ( 'NONE',  ( 2.131511515620586383, 3.916244202832140253, -3.187499998634407916 ) ) ;
#6314=CARTESIAN_POINT ( 'NONE',  ( 4.606548227981507537, 6.456511556909250160, -7.591235721156634142 ) ) ;
#6328=CARTESIAN_POINT ( 'NONE',  ( -3.033343224707664376, 3.753672977998667726, -1.999999998634408360 ) ) ;
#6329=CARTESIAN_POINT ( 'NONE',  ( -4.276409079477644148, -1.261996585732578335, -5.062499998634406140 ) ) ;
#6331=CARTESIAN_POINT ( 'NONE',  ( 4.535975386569504053, 1.338596318647080397, -8.156249999317205734 ) ) ;
#6333=CARTESIAN_POINT ( 'NONE',  ( -7.500000000000003553, -1.443375672974066770, -7.063244554130003294 ) ) ;
#6340=CARTESIAN_POINT ( 'NONE',  ( -1.261996585732579224, 4.276409079477648589, -8.312499998634407916 ) ) ;
#6345=VECTOR ( 'NONE', #14723, 1000.000000000000000 ) ;
#6348=CARTESIAN_POINT ( 'NONE',  ( 2.390265326283148806, 4.391654775818395251, -3.749999997268816720 ) ) ;
#6354=CARTESIAN_POINT ( 'NONE',  ( 4.276409079477644148, 1.261996585732577891, -6.312499998634407028 ) ) ;
#6358=( BOUNDED_CURVE ( )  B_SPLINE_CURVE ( 2, ( #4112, #2732, #5330, #8816, #258, #15195, #5173, #13718, #13795, #7690, #12587, #6543, #1532, #11540, #5088, #2572, #7602, #11307, #11460, #407, #10101, #9060, #11382, #15034, #8976, #3948, #13962, #15275, #6470, #11224, #13888, #333, #5247, #1686, #6627, #10183, #2819, #490, #10269, #10348, #10022, #5414, #9135, #7523, #12426, #1359, #6307, #169, #14959, #3874, #3140, #3216, #12906, #1840, #13147, #12824, #1918, #10419, #568, #4272, #3065, #2080, #8164, #726, #10506, #5650, #10593, #11617, #15517, #4433, #2003, #10734, #5489, #8253, #7026, #878, #10657, #15354, #9213, #8009, #11927, #5721, #14137, #6715, #14047, #9368, #6784, #15440, #11692, #14372, #14292, #647, #5570, #15590, #4362, #9297, #6952, #1768, #2972, #14220, #8087, #11772, #13065, #12982, #11854, #6866, #802, #4508, #5797, #9444, #3301, #7926, #15672, #4587, #12383, #9813, #13677, #7561, #14911, #1081, #15147, #14371, #12459, #7396, #3744, #10942, #6019, #2524, #3666 ),
 .UNSPECIFIED., .F., .F. ) 
 B_SPLINE_CURVE_WITH_KNOTS ( ( 3, 2, 2, 2, 2, 2, 2, 2, 2, 2, 2, 2, 2, 2, 2, 2, 2, 2, 2, 2, 2, 2, 2, 2, 2, 2, 2, 2, 2, 2, 2, 2, 2, 2, 2, 2, 2, 2, 2, 2, 2, 2, 2, 2, 2, 2, 2, 2, 2, 2, 2, 2, 2, 2, 2, 2, 2, 2, 2, 2, 2, 2, 2, 2, 3 ),
 ( 0.2066346841896726794, 0.2124999999999999944, 0.2250000000000000056, 0.2374999999999999889, 0.2500000000000000000, 0.2625000000000000111, 0.2750000000000000222, 0.2874999999999999778, 0.2999999999999999889, 0.3125000000000000000, 0.3250000000000000111, 0.3375000000000000222, 0.3499999999999999778, 0.3624999999999999889, 0.3750000000000000000, 0.3875000000000000666, 0.4000000000000000222, 0.4124999999999999778, 0.4249999999999999889, 0.4375000000000000000, 0.4500000000000000666, 0.4625000000000000222, 0.4749999999999999778, 0.4874999999999999889, 0.5000000000000000000, 0.5124999999999999556, 0.5250000000000000222, 0.5374999999999998668, 0.5500000000000000444, 0.5625000000000000000, 0.5749999999999999556, 0.5875000000000000222, 0.5999999999999999778, 0.6125000000000000444, 0.6250000000000000000, 0.6374999999999999556, 0.6500000000000000222, 0.6624999999999998668, 0.6750000000000000444, 0.6875000000000000000, 0.6999999999999999556, 0.7125000000000000222, 0.7249999999999999778, 0.7375000000000000444, 0.7500000000000000000, 0.7624999999999999556, 0.7750000000000000222, 0.7874999999999999778, 0.8000000000000000444, 0.8125000000000000000, 0.8249999999999999556, 0.8375000000000000222, 0.8499999999999999778, 0.8625000000000000444, 0.8749999999999998890, 0.8874999999999999556, 0.9000000000000000222, 0.9124999999999999778, 0.9250000000000000444, 0.9375000000000000000, 0.9499999999999999556, 0.9625000000000000222, 0.9749999999999998668, 0.9875000000000001554, 1.000000000000000000 ),
 .UNSPECIFIED. ) 
 CURVE ( )  GEOMETRIC_REPRESENTATION_ITEM ( )  RATIONAL_B_SPLINE_CURVE ( ( 0.9620839512587866516, 0.9642823534839154442, 1.000000000000000000, 0.9238795325112867385, 1.000000000000000000, 0.9238795325112867385, 1.000000000000000000, 0.9238795325112867385, 1.000000000000000000, 0.9238795325112867385, 1.000000000000000000, 0.9238795325112867385, 1.000000000000000000, 0.9238795325112867385, 1.000000000000000000, 0.9238795325112867385, 1.000000000000000000, 0.9238795325112867385, 1.000000000000000000, 0.9238795325112867385, 1.000000000000000000, 0.9238795325112867385, 1.000000000000000000, 0.9238795325112867385, 1.000000000000000000, 0.9238795325112867385, 1.000000000000000000, 0.9238795325112867385, 1.000000000000000000, 0.9238795325112867385, 1.000000000000000000, 0.9238795325112867385, 1.000000000000000000, 0.9238795325112867385, 1.000000000000000000, 0.9238795325112867385, 1.000000000000000000, 0.9238795325112867385, 1.000000000000000000, 0.9238795325112867385, 1.000000000000000000, 0.9238795325112867385, 1.000000000000000000, 0.9238795325112867385, 1.000000000000000000, 0.9238795325112867385, 1.000000000000000000, 0.9238795325112867385, 1.000000000000000000, 0.9238795325112867385, 1.000000000000000000, 0.9238795325112867385, 1.000000000000000000, 0.9238795325112867385, 1.000000000000000000, 0.9238795325112867385, 1.000000000000000000, 0.9238795325112867385, 1.000000000000000000, 0.9238795325112867385, 1.000000000000000000, 0.9238795325112867385, 1.000000000000000000, 0.9238795325112867385, 1.000000000000000000, 0.9238795325112867385, 1.000000000000000000, 0.9238795325112867385, 1.000000000000000000, 0.9238795325112867385, 1.000000000000000000, 0.9238795325112867385, 1.000000000000000000, 0.9238795325112867385, 1.000000000000000000, 0.9238795325112867385, 1.000000000000000000, 0.9238795325112867385, 1.000000000000000000, 0.9238795325112867385, 1.000000000000000000, 0.9238795325112867385, 1.000000000000000000, 0.9238795325112867385, 1.000000000000000000, 0.9238795325112867385, 1.000000000000000000, 0.9238795325112867385, 1.000000000000000000, 0.9238795325112867385, 1.000000000000000000, 0.9238795325112867385, 1.000000000000000000, 0.9238795325112867385, 1.000000000000000000, 0.9238795325112867385, 1.000000000000000000, 0.9238795325112867385, 1.000000000000000000, 0.9238795325112867385, 1.000000000000000000, 0.9238795325112867385, 1.000000000000000000, 0.9238795325112867385, 1.000000000000000000, 0.9238795325112867385, 1.000000000000000000, 0.9238795325112867385, 1.000000000000000000, 0.9238795325112867385, 1.000000000000000000, 0.9238795325112867385, 1.000000000000000000, 0.9238795325112867385, 1.000000000000000000, 0.9238795325112867385, 1.000000000000000000, 0.9238795325112867385, 1.000000000000000000, 0.9238795325112867385, 1.000000000000000000, 0.9238795325112867385, 1.000000000000000000, 0.9238795325112867385, 1.000000000000000000, 0.9238795325112867385, 1.000000000000000000, 0.9238795325112867385, 1.000000000000000000 ) ) 
 REPRESENTATION_ITEM ( '' )  );
#6362=CARTESIAN_POINT ( 'NONE',  ( 5.000000000000004441, 3.034671531081452754E-15, -0.04526304759294640795 ) ) ;
#6369=CARTESIAN_POINT ( 'NONE',  ( -0.3875187462258835036, -8.436519985396071064, -7.781689322727316060 ) ) ;
#6371=CARTESIAN_POINT ( 'NONE',  ( -4.209348295687703967, -3.401574460001763001, -3.437500000000003553 ) ) ;
#6373=DIRECTION ( 'NONE',  ( 0.000000000000000000, 0.000000000000000000, 1.000000000000000000 ) ) ;
#6375=CARTESIAN_POINT ( 'NONE',  ( 0.5093500532425063732, 4.799145180956616130, -2.374999998634407028 ) ) ;
#6385=ORIENTED_EDGE ( 'NONE', *, *, #3426, .T. ) ;
#6402=ADVANCED_FACE ( 'NONE', ( #15955 ), #6412, .T. ) ;
#6410=CARTESIAN_POINT ( 'NONE',  ( 7.894787914004607998, 0.7661396099416303285, -7.591390474663427312 ) ) ;
#6412=CONICAL_SURFACE ( 'NONE', #7202, 7.500000000000001776, 0.8594454914424796144 ) ;
#6413=CARTESIAN_POINT ( 'NONE',  ( -3.753672977998669946, -3.033343224707661712, -4.999999998634407028 ) ) ;
#6426=CARTESIAN_POINT ( 'NONE',  ( 1.261996585732578113, -4.276409079477644148, -7.812499998634407916 ) ) ;
#6427=CARTESIAN_POINT ( 'NONE',  ( -4.391654775818395251, 2.390265326283148806, -4.499999997268817609 ) ) ;
#6435=CARTESIAN_POINT ( 'NONE',  ( 0.5711823568785989735, 5.381735091635026613, -4.687499997268819385 ) ) ;
#6438=VERTEX_POINT ( 'NONE', #7719 ) ;
#6451=LINE ( 'NONE', #11363, #6639 ) ;
#6452=CARTESIAN_POINT ( 'NONE',  ( -2.387978478801059179, -7.281554020289573437, -7.069802615102041443 ) ) ;
#6454=CARTESIAN_POINT ( 'NONE',  ( -4.795541693661363958, -1.415196051561583790, -5.500000000000001776 ) ) ;
#6455=CARTESIAN_POINT ( 'NONE',  ( 5.000000000000095923, 0.7223674278660565662, -3.021799365517156666 ) ) ;
#6458=( BOUNDED_CURVE ( )  B_SPLINE_CURVE ( 2, ( #8768, #3494, #8452, #8531, #6181, #13348, #7239, #7309, #10303, #13993, #5274 ),
 .UNSPECIFIED., .F., .F. ) 
 B_SPLINE_CURVE_WITH_KNOTS ( ( 3, 2, 2, 2, 2, 3 ),
 ( 0.3045872658012772627, 0.3125000000000000000, 0.3250000000000000111, 0.3375000000000000222, 0.3499999999999999778, 0.3545872658012772516 ),
 .UNSPECIFIED. ) 
 CURVE ( )  GEOMETRIC_REPRESENTATION_ITEM ( )  RATIONAL_B_SPLINE_CURVE ( ( 0.9646335149384808183, 0.9518143178943437865, 1.000000000000000000, 0.9238795325112867385, 1.000000000000000000, 0.9238795325112867385, 1.000000000000000000, 0.9238795325112867385, 1.000000000000000000, 0.9720652146169430630, 0.9646335149384808183 ) ) 
 REPRESENTATION_ITEM ( '' )  );
#6459=CARTESIAN_POINT ( 'NONE',  ( 4.799145180956616130, -0.5093500532425063732, -6.624999998634407916 ) ) ;
#6460=EDGE_LOOP ( 'NONE', ( #8530, #13959, #2992, #9314, #15800 ) ) ;
#6461=CARTESIAN_POINT ( 'NONE',  ( -7.894787914004613327, -1.222495057920810896E-13, -7.591390474663425536 ) ) ;
#6464=EDGE_CURVE ( 'NONE', #7075, #4563, #157, .T. ) ;
#6470=CARTESIAN_POINT ( 'NONE',  ( -1.261996585732579224, 4.276409079477648589, -2.062499998634406584 ) ) ;
#6473=CARTESIAN_POINT ( 'NONE',  ( -6.250000000000000888, -5.051814855409232585, -7.198902722707430257 ) ) ;
#6487=CARTESIAN_POINT ( 'NONE',  ( -1.415196051561583790, 4.795541693661363958, -1.624999997268814722 ) ) ;
#6493=CARTESIAN_POINT ( 'NONE',  ( -1.261996585732579224, 4.276409079477648589, -6.312499998634407028 ) ) ;
#6498=CARTESIAN_POINT ( 'NONE',  ( -2.390265326283148806, -4.391654775818394363, -7.375000000000002665 ) ) ;
#6502=CARTESIAN_POINT ( 'NONE',  ( 2.131511515620586383, 3.916244202832140253, -7.437499998634407916 ) ) ;
#6504=CARTESIAN_POINT ( 'NONE',  ( 4.762271716570388058, 0.4578986391487566143, -0.1664591361020693883 ) ) ;
#6507=ADVANCED_FACE ( 'NONE', ( #10127 ), #15058, .F. ) ;
#6508=CARTESIAN_POINT ( 'NONE',  ( 4.795541693661363958, 1.415196051561583790, -2.874999997268815832 ) ) ;
#6514=CARTESIAN_POINT ( 'NONE',  ( 7.499999999999999112, -1.443375672974070101, -7.063244554130002406 ) ) ;
#6523=CARTESIAN_POINT ( 'NONE',  ( -4.606548227981508425, -6.456511556909257266, -7.591235721156635918 ) ) ;
#6524=CARTESIAN_POINT ( 'NONE',  ( -6.874999999999997335, 4.690970937165711341, -7.298562697733101956 ) ) ;
#6527=CARTESIAN_POINT ( 'NONE',  ( 4.795541693661363958, 1.415196051561583790, -5.000000000000000888 ) ) ;
#6528=CARTESIAN_POINT ( 'NONE',  ( 0.5711823568785988625, 5.381735091635026613, -2.812500000000001776 ) ) ;
#6532=CARTESIAN_POINT ( 'NONE',  ( -4.799145180956616130, 0.5093500532425063732, -8.124999998634409692 ) ) ;
#6535=ORIENTED_EDGE ( 'NONE', *, *, #1236, .T. ) ;
#6542=CARTESIAN_POINT ( 'NONE',  ( 7.264118654998711122, -4.945491722146229563, -7.907633014911222169 ) ) ;
#6543=CARTESIAN_POINT ( 'NONE',  ( -3.033343224707664820, 3.753672977998667726, -0.9999999986344076941 ) ) ;
#6551=B_SPLINE_CURVE_WITH_KNOTS ( 'NONE', 3,
 ( #6967, #14305, #9457, #4448, #11787, #6796, #10521, #508 ),
 .UNSPECIFIED., .F., .F.,
 ( 4, 2, 2, 4 ),
 ( 0.006061689441712458590, 0.007174127271521684238, 0.008286565101330909885, 0.01051144076094936118 ),
 .UNSPECIFIED. ) ;
#6552=DIRECTION ( 'NONE',  ( 1.000000000000000000, 0.000000000000000000, 0.000000000000000000 ) ) ;
#6554=CARTESIAN_POINT ( 'NONE',  ( -14.99999999999998934, -1.734723475976807094E-15, -9.999999999999998224 ) ) ;
#6563=CARTESIAN_POINT ( 'NONE',  ( -4.209348295687703079, -3.401574460001763445, -4.312499997268815832 ) ) ;
#6565=CARTESIAN_POINT ( 'NONE',  ( 4.209348295687701302, 3.401574460001766109, -5.937500000000003553 ) ) ;
#6576=CARTESIAN_POINT ( 'NONE',  ( -4.799145180956616130, 0.5093500532425063732, -7.124999998634407916 ) ) ;
#6578=AXIS2_PLACEMENT_3D ( 'NONE', #12085, #15754, #14761 ) ;
#6581=UNCERTAINTY_MEASURE_WITH_UNIT (LENGTH_MEASURE( 1.000000000000000082E-05 ), #9620, 'distance_accuracy_value', 'NONE');
#6584=CARTESIAN_POINT ( 'NONE',  ( -4.795541693661363958, -1.415196051561583790, -4.374999997268816720 ) ) ;
#6590=CARTESIAN_POINT ( 'NONE',  ( 0.5093500532425063732, 4.799145180956616130, -8.124999998634409692 ) ) ;
#6598=LINE ( 'NONE', #13036, #15410 ) ;
#6599=ADVANCED_FACE ( 'NONE', ( #7125 ), #14868, .F. ) ;
#6604=CARTESIAN_POINT ( 'NONE',  ( -3.080866544137487395, -6.881514909249307088, -7.026396753507437865 ) ) ;
#6606=CARTESIAN_POINT ( 'NONE',  ( -4.391654775818395251, 2.390265326283148806, -6.625000000000002665 ) ) ;
#6610=CARTESIAN_POINT ( 'NONE',  ( 2.131511515620586383, 3.916244202832140253, -7.437499998634407916 ) ) ;
#6613=UNCERTAINTY_MEASURE_WITH_UNIT (LENGTH_MEASURE( 1.000000000000000082E-05 ), #4813, 'distance_accuracy_value', 'NONE');
#6614=CARTESIAN_POINT ( 'NONE',  ( 7.500000000000003553, -4.330127018922199866, -7.422398894150035176 ) ) ;
#6616=ORIENTED_EDGE ( 'NONE', *, *, #12795, .F. ) ;
#6627=CARTESIAN_POINT ( 'NONE',  ( 3.916244202832140253, -2.131511515620588160, -2.437499998634407028 ) ) ;
#6631=CARTESIAN_POINT ( 'NONE',  ( 3.916244202832140253, -2.131511515620588160, -5.437499998634406140 ) ) ;
#6639=VECTOR ( 'NONE', #313, 1000.000000000000000 ) ;
#6646=CIRCLE ( 'NONE', #14894, 7.500000000000001776 ) ;
#6654=CARTESIAN_POINT ( 'NONE',  ( -4.999999999999844569, 1.272547481429019856, -6.461597479913464781 ) ) ;
#6657=CARTESIAN_POINT ( 'NONE',  ( -1.261996585732579224, 4.276409079477648589, -0.3124999986344085823 ) ) ;
#6670=AXIS2_PLACEMENT_3D ( 'NONE', #6849, #11679, #709 ) ;
#6672=DIRECTION ( 'NONE',  ( -0.000000000000000000, -0.000000000000000000, -1.000000000000000000 ) ) ;
#6674=CARTESIAN_POINT ( 'NONE',  ( -3.753672977998669946, -3.033343224707661712, 1.000000001365594082 ) ) ;
#6681=FACE_OUTER_BOUND ( 'NONE', #14537, .T. ) ;
#6688=CARTESIAN_POINT ( 'NONE',  ( 4.391654775818395251, -2.390265326283149694, -0.1250000000000035805 ) ) ;
#6700=EDGE_CURVE ( 'NONE', #10386, #11169, #6358, .T. ) ;
#6703=CARTESIAN_POINT ( 'NONE',  ( 0.5093500532425063732, 4.799145180956616130, -7.374999998634408804 ) ) ;
#6705=CARTESIAN_POINT ( 'NONE',  ( 1.249999999999999556, 7.938566201357357244, -7.198902722707428481 ) ) ;
#6706=ORIENTED_EDGE ( 'NONE', *, *, #6933, .T. ) ;
#6712=FACE_OUTER_BOUND ( 'NONE', #13055, .T. ) ;
#6715=CARTESIAN_POINT ( 'NONE',  ( 3.033343224707661712, -3.753672977998669502, -5.499999998634407916 ) ) ;
#6716=CARTESIAN_POINT ( 'NONE',  ( 0.8467517840721383582, 4.385914846095951170, -0.3789984458506778786 ) ) ;
#6718=CARTESIAN_POINT ( 'NONE',  ( 3.753672977998667726, 3.033343224707664376, -5.249999998634407028 ) ) ;
#6731=CARTESIAN_POINT ( 'NONE',  ( -5.000000000000092371, -0.7223674278660636716, -7.396799362785970722 ) ) ;
#6736=CARTESIAN_POINT ( 'NONE',  ( -4.999999999999844569, 1.272547481429019856, -5.586597482644649837 ) ) ;
#6742=CARTESIAN_POINT ( 'NONE',  ( -0.5093500532425060401, -4.799145180956616130, 0.1250000013655913900 ) ) ;
#6743=ORIENTED_EDGE ( 'NONE', *, *, #5593, .F. ) ;
#6748=CARTESIAN_POINT ( 'NONE',  ( 1.415196051561583790, -4.795541693661363958, -3.124999997268815832 ) ) ;
#6749=CARTESIAN_POINT ( 'NONE',  ( -0.5711823568785977523, -5.381735091635034607, -8.187499997268814056 ) ) ;
#6751=CARTESIAN_POINT ( 'NONE',  ( -5.381735091635034607, 0.5711823568785950878, -7.437499997268817609 ) ) ;
#6757=DIRECTION ( 'NONE',  ( -0.8660254037844383745, -0.5000000000000004441, 0.000000000000000000 ) ) ;
#6761=VERTEX_POINT ( 'NONE', #13591 ) ;
#6766=CARTESIAN_POINT ( 'NONE',  ( 5.000000000000002665, 1.275685995473128912E-14, -5.045263047592944083 ) ) ;
#6773=CARTESIAN_POINT ( 'NONE',  ( -3.916244202832140253, 2.131511515620587272, 0.06250000136559172303 ) ) ;
#6780=CARTESIAN_POINT ( 'NONE',  ( 0.000000000000000000, 0.000000000000000000, -0.5776712190230133270 ) ) ;
#6781=ADVANCED_FACE ( 'NONE', ( #9887 ), #2368, .F. ) ;
#6784=CARTESIAN_POINT ( 'NONE',  ( -2.131511515620587272, -3.916244202832140253, -5.687499998634406140 ) ) ;
#6787=CARTESIAN_POINT ( 'NONE',  ( -4.276409079477644148, -1.261996585732578335, -7.812499998634407916 ) ) ;
#6788=DIRECTION ( 'NONE',  ( 0.000000000000000000, 0.000000000000000000, 1.000000000000000000 ) ) ;
#6796=CARTESIAN_POINT ( 'NONE',  ( 7.500000000000000000, -1.486698507076799070, -0.09861472150523925562 ) ) ;
#6809=CARTESIAN_POINT ( 'NONE',  ( 4.795541693661363958, 1.415196051561583790, -7.874999997268816720 ) ) ;
#6810=CARTESIAN_POINT ( 'NONE',  ( 4.276409079477644148, 1.261996585732577891, 1.437500001365592972 ) ) ;
#6819=EDGE_CURVE ( 'NONE', #13728, #4594, #13238, .T. ) ;
#6822=CARTESIAN_POINT ( 'NONE',  ( 5.000000000000004441, -2.247904837838113790E-16, -7.920263044861759028 ) ) ;
#6823=CARTESIAN_POINT ( 'NONE',  ( 5.381735091635035495, -0.5711823568785978633, -5.937499997268815832 ) ) ;
#6824=CARTESIAN_POINT ( 'NONE',  ( 5.000000000000091482, 0.7223674278660682235, -1.021799365517154223 ) ) ;
#6832=LINE ( 'NONE', #14497, #5411 ) ;
#6836=EDGE_LOOP ( 'NONE', ( #4349, #1393, #302, #9070, #7746 ) ) ;
#6846=CARTESIAN_POINT ( 'NONE',  ( -7.500000000000000000, -4.330127018922196314, -7.422398894150035176 ) ) ;
#6847=CARTESIAN_POINT ( 'NONE',  ( 6.293430271071538407, -5.026740376715105540, -0.4524126574264555334 ) ) ;
#6849=CARTESIAN_POINT ( 'NONE',  ( 0.000000000000000000, 0.000000000000000000, 0.000000000000000000 ) ) ;
#6851=CARTESIAN_POINT ( 'NONE',  ( 2.131511515620586383, 3.916244202832140253, 0.8125000013655924169 ) ) ;
#6852=ORIENTED_EDGE ( 'NONE', *, *, #14294, .F. ) ;
#6857=B_SPLINE_CURVE_WITH_KNOTS ( 'NONE', 3,
 ( #12722, #12404, #1339, #147, #12647, #5066, #1586, #6524, #12481 ),
 .UNSPECIFIED., .F., .F.,
 ( 4, 2, 1, 2, 4 ),
 ( 0.000000000000000000, 0.002165063509461100100, 0.004330127018922199332, 0.006495190528383298564, 0.008660254037844396929 ),
 .UNSPECIFIED. ) ;
#6863=EDGE_CURVE ( 'NONE', #2882, #4597, #7880, .T. ) ;
#6866=CARTESIAN_POINT ( 'NONE',  ( -4.799145180956616130, 0.5093500532425063732, -6.874999998634407916 ) ) ;
#6870=CARTESIAN_POINT ( 'NONE',  ( 1.415196051561583790, -4.795541693661363958, 1.749999999999998002 ) ) ;
#6879=PLANE ( 'NONE',  #14856 ) ;
#6882=LINE ( 'NONE', #10605, #5130 ) ;
#6883=CARTESIAN_POINT ( 'NONE',  ( -2.390265326283148806, -4.391654775818394363, -7.249999997268815832 ) ) ;
#6886=ORIENTED_EDGE ( 'NONE', *, *, #15194, .F. ) ;
#6893=CARTESIAN_POINT ( 'NONE',  ( 4.391654775818395251, -2.390265326283149694, -4.125000000000000000 ) ) ;
#6894=CARTESIAN_POINT ( 'NONE',  ( 6.250000000000002665, -5.051814855409234362, -7.198902722707431145 ) ) ;
#6895=CARTESIAN_POINT ( 'NONE',  ( 3.033343224707661712, -3.753672977998669946, 1.250000001365594304 ) ) ;
#6899=CLOSED_SHELL ( 'NONE', ( #13377, #1463, #10027, #6781, #6507, #13478, #8268, #12502, #8216, #7329, #2522, #710, #3733, #5561, #13154, #12540, #6599, #2263, #708, #7567, #2470, #4128, #2064, #4293, #6124, #2082, #4802, #8813, #14878, #10945, #15477, #15237, #5942, #9072, #12817, #6402, #8524, #1705, #14965, #10197, #9942, #10926, #15534, #13322, #5467, #9581, #5317, #4048, #5484 ) ) ;
#6903=AXIS2_PLACEMENT_3D ( 'NONE', #9752, #7104, #64 ) ;
#6906=CARTESIAN_POINT ( 'NONE',  ( -0.5711823568785977523, -5.381735091635034607, -3.187499997268817609 ) ) ;
#6907=LINE ( 'NONE', #11728, #1725 ) ;
#6908=CARTESIAN_POINT ( 'NONE',  ( -5.381735091635034607, 0.5711823568785950878, -8.437499997268814056 ) ) ;
#6914=ORIENTED_EDGE ( 'NONE', *, *, #566, .F. ) ;
#6923=CARTESIAN_POINT ( 'NONE',  ( 3.753672977998667726, 3.033343224707664820, -0.4999999986344072500 ) ) ;
#6925=CARTESIAN_POINT ( 'NONE',  ( -7.500000000000005329, 2.932633423934443151, -0.4709827563909335657 ) ) ;
#6933=EDGE_CURVE ( 'NONE', #9162, #6438, #9744, .T. ) ;
#6939=CARTESIAN_POINT ( 'NONE',  ( -2.131511515620587272, -3.916244202832140253, -0.6874999986344054737 ) ) ;
#6952=CARTESIAN_POINT ( 'NONE',  ( 4.276409079477644148, 1.261996585732577891, -6.312499998634407028 ) ) ;
#6955=CIRCLE ( 'NONE', #1521, 0.7733184030943203169 ) ;
#6957=CARTESIAN_POINT ( 'NONE',  ( 4.391654775818395251, -2.390265326283149694, 0.8749999999999973355 ) ) ;
#6961=EDGE_CURVE ( 'NONE', #2882, #10281, #748, .T. ) ;
#6967=CARTESIAN_POINT ( 'NONE',  ( 7.500000000000004441, -4.330127018922205195, -1.000000000000000888 ) ) ;
#6969=DIRECTION ( 'NONE',  ( 0.000000000000000000, 0.000000000000000000, 1.000000000000000000 ) ) ;
#6984=ORIENTED_EDGE ( 'NONE', *, *, #15393, .T. ) ;
#6989=CARTESIAN_POINT ( 'NONE',  ( 2.131511515620586383, 3.916244202832140253, -0.1874999986344084990 ) ) ;
#6991=CARTESIAN_POINT ( 'NONE',  ( -0.5711823568785978633, -5.381735091635035495, -6.187499997268815832 ) ) ;
#6996=CARTESIAN_POINT ( 'NONE',  ( -4.336808689942017736E-16, -8.660254037844399733, -9.999999999999998224 ) ) ;
#6997=CARTESIAN_POINT ( 'NONE',  ( -7.500000000000005329, 4.330127018922194537, -7.422398894150031623 ) ) ;
#7003=CYLINDRICAL_SURFACE ( 'NONE', #4551, 5.000000000000000888 ) ;
#7005=EDGE_CURVE ( 'NONE', #8373, #5402, #3568, .T. ) ;
#7012=CARTESIAN_POINT ( 'NONE',  ( -6.288404560131955812, -5.029641972278938056, -0.4504974108211986517 ) ) ;
#7014=CARTESIAN_POINT ( 'NONE',  ( -4.799145180956616130, 0.5093500532425063732, -0.8749999986344056957 ) ) ;
#7016=CARTESIAN_POINT ( 'NONE',  ( 5.335963852943357288, 6.035591050532032042, -7.593821156097325442 ) ) ;
#7022=CARTESIAN_POINT ( 'NONE',  ( -3.401574460001765221, 4.209348295687701302, -7.687500000000004441 ) ) ;
#7024=EDGE_CURVE ( 'NONE', #9050, #7077, #12424, .T. ) ;
#7026=CARTESIAN_POINT ( 'NONE',  ( -3.916244202832140253, 2.131511515620587272, -4.937499998634406140 ) ) ;
#7027=CYLINDRICAL_SURFACE ( 'NONE', #8607, 5.000000000000000888 ) ;
#7028=AXIS2_PLACEMENT_3D ( 'NONE', #1160, #8540, #10944 ) ;
#7030=CARTESIAN_POINT ( 'NONE',  ( -2.390265326283148806, -4.391654775818394363, 1.624999999999998002 ) ) ;
#7034=ORIENTED_EDGE ( 'NONE', *, *, #10134, .T. ) ;
#7041=CARTESIAN_POINT ( 'NONE',  ( 0.000000000000000000, 0.000000000000000000, 0.000000000000000000 ) ) ;
#7057=ORIENTED_EDGE ( 'NONE', *, *, #14005, .T. ) ;
#7062=CARTESIAN_POINT ( 'NONE',  ( 5.000000000000004441, -2.247904837838113790E-16, -2.920263044861759472 ) ) ;
#7064=CARTESIAN_POINT ( 'NONE',  ( 4.799145180956616130, -0.5093500532425063732, 0.6250000013655918618 ) ) ;
#7066=( BOUNDED_CURVE ( )  B_SPLINE_CURVE ( 2, ( #1425, #4171, #8798, #7672, #12570, #6528, #1517, #15177, #5309, #6455, #10165 ),
 .UNSPECIFIED., .F., .F. ) 
 B_SPLINE_CURVE_WITH_KNOTS ( ( 3, 2, 2, 2, 2, 3 ),
 ( 0.4545872658012772849, 0.4625000000000000222, 0.4749999999999999778, 0.4874999999999999889, 0.5000000000000000000, 0.5045872658012773293 ),
 .UNSPECIFIED. ) 
 CURVE ( )  GEOMETRIC_REPRESENTATION_ITEM ( )  RATIONAL_B_SPLINE_CURVE ( ( 0.9646335149384808183, 0.9518143178943437865, 1.000000000000000000, 0.9238795325112867385, 1.000000000000000000, 0.9238795325112867385, 1.000000000000000000, 0.9238795325112867385, 1.000000000000000000, 0.9720652146169423968, 0.9646335149384803742 ) ) 
 REPRESENTATION_ITEM ( '' )  );
#7068=CARTESIAN_POINT ( 'NONE',  ( 3.033343224707661712, -3.753672977998669946, 0.2500000013655933606 ) ) ;
#7071=CARTESIAN_POINT ( 'NONE',  ( 2.459698528280935381, -7.240146430416074530, -0.09933465333851865253 ) ) ;
#7075=VERTEX_POINT ( 'NONE', #15629 ) ;
#7077=VERTEX_POINT ( 'NONE', #5685 ) ;
#7082=DIRECTION ( 'NONE',  ( -0.8660254037844383745, 0.5000000000000004441, 0.000000000000000000 ) ) ;
#7084=( GEOMETRIC_REPRESENTATION_CONTEXT ( 3 ) GLOBAL_UNCERTAINTY_ASSIGNED_CONTEXT ( ( #6581 ) ) GLOBAL_UNIT_ASSIGNED_CONTEXT ( ( #9620, #13654, #5014 ) ) REPRESENTATION_CONTEXT ( 'NONE', 'WORKASPACE' ) );
#7085=CARTESIAN_POINT ( 'NONE',  ( 4.391654775818395251, -2.390265326283149694, 2.731183335047404626E-09 ) ) ;
#7090=CARTESIAN_POINT ( 'NONE',  ( 3.753672977998667726, 3.033343224707664376, -2.249999998634408804 ) ) ;
#7104=DIRECTION ( 'NONE',  ( -1.000000000000000000, 0.000000000000000000, 0.000000000000000000 ) ) ;
#7107=CARTESIAN_POINT ( 'NONE',  ( -1.261996585732579224, 4.276409079477648589, -8.062499998634407916 ) ) ;
#7109=CARTESIAN_POINT ( 'NONE',  ( -0.8301538844988668453, -4.780499171557324622, -0.1086890209542362012 ) ) ;
#7121=ORIENTED_EDGE ( 'NONE', *, *, #2018, .F. ) ;
#7124=CARTESIAN_POINT ( 'NONE',  ( -0.5974722283283653290, 8.315303285985685022, -0.7026937717022876395 ) ) ;
#7125=FACE_OUTER_BOUND ( 'NONE', #12315, .T. ) ;
#7139=CARTESIAN_POINT ( 'NONE',  ( -6.486836893983028318, 4.915077010914117750, -7.231838333420224529 ) ) ;
#7145=CARTESIAN_POINT ( 'NONE',  ( 0.5093500532425063732, 4.799145180956616130, -1.124999998634405918 ) ) ;
#7148=CARTESIAN_POINT ( 'NONE',  ( -0.5093500532425060401, -4.799145180956616130, 0.1250000013655913900 ) ) ;
#7150=CARTESIAN_POINT ( 'NONE',  ( 3.096526599377913413, -6.872473572140724407, -6.360652745248294783E-15 ) ) ;
#7160=CARTESIAN_POINT ( 'NONE',  ( -3.916244202832140253, 2.131511515620587272, -3.187499998634407916 ) ) ;
#7165=DIRECTION ( 'NONE',  ( 0.000000000000000000, 0.000000000000000000, 1.000000000000000000 ) ) ;
#7169=CARTESIAN_POINT ( 'NONE',  ( -3.401574460001764777, 4.209348295687701302, 0.4375000027311838346 ) ) ;
#7171=FILL_AREA_STYLE_COLOUR ( '', #2024 ) ;
#7173=CARTESIAN_POINT ( 'NONE',  ( 3.916244202832140253, -2.131511515620588160, -2.437499998634407028 ) ) ;
#7176=CARTESIAN_POINT ( 'NONE',  ( 1.282512619719710756, 8.391164935524622948, -7.795653906409119038 ) ) ;
#7190=EDGE_CURVE ( 'NONE', #3174, #9050, #12200, .T. ) ;
#7192=CARTESIAN_POINT ( 'NONE',  ( 5.381735091635035495, -0.5711823568785978633, -2.062500000000000888 ) ) ;
#7193=CARTESIAN_POINT ( 'NONE',  ( -4.999999999999844569, 1.272547481429019856, -3.586597482644647616 ) ) ;
#7194=CARTESIAN_POINT ( 'NONE',  ( 4.104504678892250347, -2.845098865571579871, -0.009045026986704146621 ) ) ;
#7196=CARTESIAN_POINT ( 'NONE',  ( 1.261996585732578113, -4.276409079477644148, 1.187500001365592750 ) ) ;
#7202=AXIS2_PLACEMENT_3D ( 'NONE', #6008, #10934, #15872 ) ;
#7211=EDGE_CURVE ( 'NONE', #2517, #2401, #13985, .T. ) ;
#7216=CARTESIAN_POINT ( 'NONE',  ( 3.401574460001763445, -4.209348295687703079, -6.062499997268814056 ) ) ;
#7219=VERTEX_POINT ( 'NONE', #12681 ) ;
#7227=EDGE_CURVE ( 'NONE', #2247, #9162, #9079, .T. ) ;
#7230=CARTESIAN_POINT ( 'NONE',  ( 1.261996585732578113, -4.276409079477644148, -1.562499998634406140 ) ) ;
#7232=CARTESIAN_POINT ( 'NONE',  ( -3.916244202832140253, 2.131511515620587272, -2.187499998634407028 ) ) ;
#7239=CARTESIAN_POINT ( 'NONE',  ( -2.390265326283148806, -4.391654775818394363, -1.375000000000001332 ) ) ;
#7241=ORIENTED_EDGE ( 'NONE', *, *, #892, .T. ) ;
#7242=CARTESIAN_POINT ( 'NONE',  ( -3.916244202832140253, 2.131511515620587272, -4.187499998634405252 ) ) ;
#7248=CARTESIAN_POINT ( 'NONE',  ( -1.415196051561583790, 4.795541693661363958, -0.6249999972688171646 ) ) ;
#7252=CARTESIAN_POINT ( 'NONE',  ( 2.131511515620586383, 3.916244202832140253, -3.187499998634407916 ) ) ;
#7257=ORIENTED_EDGE ( 'NONE', *, *, #5223, .F. ) ;
#7264=CARTESIAN_POINT ( 'NONE',  ( -3.401574460001764777, 4.209348295687701302, -2.687500000000003553 ) ) ;
#7266=CARTESIAN_POINT ( 'NONE',  ( -2.975210800253060839, -3.755114819930441161, -0.1516074998685549846 ) ) ;
#7268=CARTESIAN_POINT ( 'NONE',  ( -3.916244202832140253, 2.131511515620587272, -1.187499998634405918 ) ) ;
#7284=FACE_OUTER_BOUND ( 'NONE', #2494, .T. ) ;
#7292=ORIENTED_EDGE ( 'NONE', *, *, #13177, .F. ) ;
#7302=CARTESIAN_POINT ( 'NONE',  ( 1.261996585732578113, -4.276409079477644148, 0.1875000013655918341 ) ) ;
#7304=CARTESIAN_POINT ( 'NONE',  ( 1.211595439868045521, -7.960739084487663320, -0.4504974108212069228 ) ) ;
#7309=CARTESIAN_POINT ( 'NONE',  ( -4.209348295687703079, -3.401574460001763445, -1.437500000000002220 ) ) ;
#7313=CARTESIAN_POINT ( 'NONE',  ( 4.276409079477644148, 1.261996585732577891, -3.562499998634407916 ) ) ;
#7314=CARTESIAN_POINT ( 'NONE',  ( 0.000000000000000000, 0.000000000000000000, -25.03750572909317285 ) ) ;
#7324=CARTESIAN_POINT ( 'NONE',  ( -1.261996585732579224, 4.276409079477648589, -6.062499998634407028 ) ) ;
#7328=ORIENTED_EDGE ( 'NONE', *, *, #11336, .T. ) ;
#7329=ADVANCED_FACE ( 'NONE', ( #10818 ), #9754, .F. ) ;
#7331=ORIENTED_EDGE ( 'NONE', *, *, #10252, .F. ) ;
#7335=CARTESIAN_POINT ( 'NONE',  ( 0.000000000000000000, 0.000000000000000000, 0.000000000000000000 ) ) ;
#7338=CARTESIAN_POINT ( 'NONE',  ( 2.390265326283148806, 4.391654775818395251, -1.875000000000001776 ) ) ;
#7340=CARTESIAN_POINT ( 'NONE',  ( -1.599579652451927014, -4.558710419355938015, -0.1233474730213283688 ) ) ;
#7342=CARTESIAN_POINT ( 'NONE',  ( 2.131511515620586383, 3.916244202832140253, -1.437499998634406140 ) ) ;
#7376=CARTESIAN_POINT ( 'NONE',  ( -1.261996585732579224, 4.276409079477648589, -2.062499998634406584 ) ) ;
#7379=CARTESIAN_POINT ( 'NONE',  ( 3.916244202832140253, -2.131511515620588160, -2.687499998634407028 ) ) ;
#7383=DIRECTION ( 'NONE',  ( 0.000000000000000000, 0.000000000000000000, 1.000000000000000000 ) ) ;
#7384=CONICAL_SURFACE ( 'NONE', #15863, 4.174999999999999822, 0.9599310885968795892 ) ;
#7390=CARTESIAN_POINT ( 'NONE',  ( 3.753672977998667726, 3.033343224707664820, -4.499999998634407028 ) ) ;
#7396=CARTESIAN_POINT ( 'NONE',  ( -3.033343224707664820, 3.753672977998667726, -7.999999998634411469 ) ) ;
#7402=CARTESIAN_POINT ( 'NONE',  ( -2.390265326283148806, -4.391654775818394363, 0.7500000027311839457 ) ) ;
#7407=CARTESIAN_POINT ( 'NONE',  ( -2.131511515620587272, -3.916244202832140253, -3.687499998634407916 ) ) ;
#7414=VERTEX_POINT ( 'NONE', #13867 ) ;
#7425=CARTESIAN_POINT ( 'NONE',  ( 4.209348295687701302, 3.401574460001765665, -0.9375000000000018874 ) ) ;
#7427=CARTESIAN_POINT ( 'NONE',  ( -4.009547343616874926, -2.543570988302763514, -0.1814977198071575648 ) ) ;
#7430=CARTESIAN_POINT ( 'NONE',  ( 3.916244202832140253, -2.131511515620588160, -3.687499998634407916 ) ) ;
#7431=ORIENTED_EDGE ( 'NONE', *, *, #4296, .F. ) ;
#7435=ORIENTED_EDGE ( 'NONE', *, *, #9886, .T. ) ;
#7464=CARTESIAN_POINT ( 'NONE',  ( -3.916244202832140253, 2.131511515620587272, -3.937499998634404808 ) ) ;
#7467=CARTESIAN_POINT ( 'NONE',  ( 4.276409079477644148, 1.261996585732577891, -5.562499998634406140 ) ) ;
#7477=CARTESIAN_POINT ( 'NONE',  ( -1.261996585732579224, 4.276409079477648589, -1.312499998634406140 ) ) ;
#7484=CARTESIAN_POINT ( 'NONE',  ( 5.381735091635035495, -0.5711823568785978633, -4.937499997268820273 ) ) ;
#7490=CARTESIAN_POINT ( 'NONE',  ( 4.799145180956616130, -0.5093500532425063732, -5.374999998634406140 ) ) ;
#7493=VERTEX_POINT ( 'NONE', #66 ) ;
#7497=ORIENTED_EDGE ( 'NONE', *, *, #13177, .T. ) ;
#7506=CARTESIAN_POINT ( 'NONE',  ( -3.401574460001764777, 4.209348295687701302, -1.687500000000002442 ) ) ;
#7507=CARTESIAN_POINT ( 'NONE',  ( 4.209348295687701302, 3.401574460001766109, -3.937500000000000888 ) ) ;
#7510=CARTESIAN_POINT ( 'NONE',  ( 2.131511515620586383, 3.916244202832140253, -2.437499998634407028 ) ) ;
#7513=ORIENTED_EDGE ( 'NONE', *, *, #9158, .T. ) ;
#7515=CARTESIAN_POINT ( 'NONE',  ( 4.458734124999998549, -3.052311964297492742E-11, -0.3789984458506765463 ) ) ;
#7520=ORIENTED_EDGE ( 'NONE', *, *, #10845, .T. ) ;
#7523=CARTESIAN_POINT ( 'NONE',  ( -3.033343224707664820, 3.753672977998667726, -2.999999998634409248 ) ) ;
#7526=CARTESIAN_POINT ( 'NONE',  ( -5.000000000000004441, -1.011557177027151181E-15, -4.420263044861760804 ) ) ;
#7529=B_SPLINE_CURVE_WITH_KNOTS ( 'NONE', 3,
 ( #3036, #1819, #5545, #3121, #13039, #1980, #6925, #8062, #12960, #13124 ),
 .UNSPECIFIED., .F., .F.,
 ( 4, 2, 2, 2, 4 ),
 ( 0.01051144076094935077, 0.01162027323572611091, 0.01272910571050287105, 0.01383793818527963120, 0.01494677066005639134 ),
 .UNSPECIFIED. ) ;
#7530=CARTESIAN_POINT ( 'NONE',  ( 4.391654775818395251, -2.390265326283149694, -5.999999997268814944 ) ) ;
#7543=CARTESIAN_POINT ( 'NONE',  ( -5.000000000000095035, -0.7223674278660573433, -4.396799362785971610 ) ) ;
#7544=CARTESIAN_POINT ( 'NONE',  ( 3.916244202832140253, -2.131511515620588160, -4.437499998634405252 ) ) ;
#7547=CARTESIAN_POINT ( 'NONE',  ( 3.033343224707661712, -3.753672977998669946, -6.749999998634408804 ) ) ;
#7550=VERTEX_POINT ( 'NONE', #1340 ) ;
#7551=CARTESIAN_POINT ( 'NONE',  ( -7.500000000000005329, 3.608439182435162262, -7.298562697733104621 ) ) ;
#7558=CARTESIAN_POINT ( 'NONE',  ( -3.753672977998669502, -3.033343224707661712, -6.999999998634409692 ) ) ;
#7561=CARTESIAN_POINT ( 'NONE',  ( -0.5093500532425060401, -4.799145180956616130, -7.624999998634407916 ) ) ;
#7565=CARTESIAN_POINT ( 'NONE',  ( -3.401574460001764777, 4.209348295687701302, -2.562499997268814944 ) ) ;
#7567=ADVANCED_FACE ( 'NONE', ( #11365 ), #3067, .T. ) ;
#7570=ORIENTED_EDGE ( 'NONE', *, *, #9644, .F. ) ;
#7572=CARTESIAN_POINT ( 'NONE',  ( 4.799145180956616130, -0.5093500532425063732, -7.374999998634408804 ) ) ;
#7582=CARTESIAN_POINT ( 'NONE',  ( -1.282512619719235580, -8.391164935524143331, -7.795653906408909428 ) ) ;
#7583=CARTESIAN_POINT ( 'NONE',  ( 0.000000000000000000, 0.000000000000000000, -8.499999999999996447 ) ) ;
#7584=CARTESIAN_POINT ( 'NONE',  ( -1.415196051561583790, 4.795541693661363958, -3.750000000000000000 ) ) ;
#7590=( BOUNDED_CURVE ( )  B_SPLINE_CURVE ( 2, ( #3772, #11056, #1268, #8403, #11206, #8482, #14608, #68, #1185, #6213, #8561 ),
 .UNSPECIFIED., .F., .F. ) 
 B_SPLINE_CURVE_WITH_KNOTS ( ( 3, 2, 2, 2, 2, 3 ),
 ( 0.3045872658012772627, 0.3125000000000000000, 0.3250000000000000111, 0.3375000000000000222, 0.3499999999999999778, 0.3545872658012772516 ),
 .UNSPECIFIED. ) 
 CURVE ( )  GEOMETRIC_REPRESENTATION_ITEM ( )  RATIONAL_B_SPLINE_CURVE ( ( 0.9646335149384808183, 0.9518143178943437865, 1.000000000000000000, 0.9238795325112867385, 1.000000000000000000, 0.9238795325112867385, 1.000000000000000000, 0.9238795325112867385, 1.000000000000000000, 0.9720652146169430630, 0.9646335149384808183 ) ) 
 REPRESENTATION_ITEM ( '' )  );
#7591=CARTESIAN_POINT ( 'NONE',  ( -4.276409079477644148, -1.261996585732578335, -3.062499998634407472 ) ) ;
#7597=CARTESIAN_POINT ( 'NONE',  ( -7.500000000000000000, -4.330127018922196314, -9.999999999999998224 ) ) ;
#7599=ORIENTED_EDGE ( 'NONE', *, *, #10570, .F. ) ;
#7602=CARTESIAN_POINT ( 'NONE',  ( 4.276409079477644148, 1.261996585732577891, -1.312499998634406140 ) ) ;
#7609=CARTESIAN_POINT ( 'NONE',  ( 4.999999999999845457, -1.272547481429021854, -3.086597482644650281 ) ) ;
#7624=EDGE_CURVE ( 'NONE', #10386, #10448, #12230, .T. ) ;
#7625=B_SPLINE_CURVE_WITH_KNOTS ( 'NONE', 3,
 ( #2068, #11756, #2956, #7012, #474, #632 ),
 .UNSPECIFIED., .F., .F.,
 ( 4, 2, 4 ),
 ( 0.004444412883774351460, 0.006655097293744442408, 0.008865781703714532488 ),
 .UNSPECIFIED. ) ;
#7629=EDGE_CURVE ( 'NONE', #11803, #4563, #15353, .T. ) ;
#7630=CARTESIAN_POINT ( 'NONE',  ( -3.916244202832140253, 2.131511515620587272, -7.187499998634407916 ) ) ;
#7635=CIRCLE ( 'NONE', #7884, 5.000000000000000000 ) ;
#7636=ORIENTED_EDGE ( 'NONE', *, *, #6961, .T. ) ;
#7642=CARTESIAN_POINT ( 'NONE',  ( 3.916244202832140253, -2.131511515620588160, -5.687499998634406140 ) ) ;
#7643=CARTESIAN_POINT ( 'NONE',  ( 5.000000000000093259, 0.7223674278660628945, -4.896799362785971610 ) ) ;
#7651=CARTESIAN_POINT ( 'NONE',  ( 0.5711823568785989735, 5.381735091635026613, -5.687499997268815832 ) ) ;
#7671=CARTESIAN_POINT ( 'NONE',  ( 3.401574460001763001, -4.209348295687703967, -6.187500000000003553 ) ) ;
#7672=CARTESIAN_POINT ( 'NONE',  ( -3.401574460001765221, 4.209348295687701302, -2.687500000000002665 ) ) ;
#7675=CARTESIAN_POINT ( 'NONE',  ( 4.276409079477644148, 1.261996585732577891, -7.562499998634407916 ) ) ;
#7677=CARTESIAN_POINT ( 'NONE',  ( -7.500000000000006217, -2.930060224340423680, -0.4701183149080278012 ) ) ;
#7690=CARTESIAN_POINT ( 'NONE',  ( -4.799145180956616130, 0.5093500532425063732, -0.8749999986344056957 ) ) ;
#7715=CARTESIAN_POINT ( 'NONE',  ( 2.131511515620586383, 3.916244202832140253, -7.437499998634407916 ) ) ;
#7719=CARTESIAN_POINT ( 'NONE',  ( -5.000000000000004441, -1.011557177027151181E-15, -5.420263044861760804 ) ) ;
#7726=ORIENTED_EDGE ( 'NONE', *, *, #10314, .T. ) ;
#7727=CARTESIAN_POINT ( 'NONE',  ( 3.033343224707661712, -3.753672977998669502, -6.749999998634408804 ) ) ;
#7737=CARTESIAN_POINT ( 'NONE',  ( 0.5711823568785989735, 5.381735091635026613, -3.687499997268817609 ) ) ;
#7743=CARTESIAN_POINT ( 'NONE',  ( -3.033343224707664376, 3.753672977998667726, -7.999999998634409692 ) ) ;
#7746=ORIENTED_EDGE ( 'NONE', *, *, #13822, .T. ) ;
#7747=EDGE_LOOP ( 'NONE', ( #12577, #11397, #14479, #6852, #12415 ) ) ;
#7749=CARTESIAN_POINT ( 'NONE',  ( -5.000000000000000888, 6.123233995736767268E-16, -25.03750572909317285 ) ) ;
#7754=CARTESIAN_POINT ( 'NONE',  ( -8.673617379884035472E-16, -9.147862274876560562, -8.047472243342939535 ) ) ;
#7758=CARTESIAN_POINT ( 'NONE',  ( 1.415196051561583790, -4.795541693661363958, -5.250000000000000888 ) ) ;
#7762=CARTESIAN_POINT ( 'NONE',  ( -4.799145180956616130, 0.5093500532425063732, -7.124999998634407916 ) ) ;
#7764=CARTESIAN_POINT ( 'NONE',  ( -2.720782245279947563E-14, 8.716839668575689259, -7.700121441565839220 ) ) ;
#7779=CARTESIAN_POINT ( 'NONE',  ( -0.5711823568785977523, -5.381735091635034607, -3.312500000000001776 ) ) ;
#7784=EDGE_LOOP ( 'NONE', ( #12511, #8904, #14499, #3007 ) ) ;
#7790=CARTESIAN_POINT ( 'NONE',  ( 4.795541693661363958, 1.415196051561583790, -6.000000000000001776 ) ) ;
#7792=CARTESIAN_POINT ( 'NONE',  ( 0.5093500532425063732, 4.799145180956616130, -4.374999998634405252 ) ) ;
#7802=CARTESIAN_POINT ( 'NONE',  ( -2.131511515620587272, -3.916244202832140253, -7.937499998634408804 ) ) ;
#7803=B_SPLINE_CURVE_WITH_KNOTS ( 'NONE', 3,
 ( #5246, #6542, #14867, #11306, #1283, #3790, #5087, #11142, #4024, #10100 ),
 .UNSPECIFIED., .F., .F.,
 ( 4, 2, 2, 2, 4 ),
 ( 0.000000000000000000, 0.002305503304226490767, 0.004611006608452981534, 0.006916509912679473168, 0.009222013216905964803 ),
 .UNSPECIFIED. ) ;
#7804=CARTESIAN_POINT ( 'NONE',  ( -4.999999999999844569, 1.272547481429019856, -4.461597479913466557 ) ) ;
#7805=AXIS2_PLACEMENT_3D ( 'NONE', #10865, #8461, #7082 ) ;
#7806=CARTESIAN_POINT ( 'NONE',  ( 4.999999999999848121, -1.272547481429015859, -4.961597479913466557 ) ) ;
#7808=CARTESIAN_POINT ( 'NONE',  ( -4.391654775818395251, 2.390265326283148806, -3.499999997268816276 ) ) ;
#7813=EDGE_LOOP ( 'NONE', ( #7257, #8056, #12604, #11023, #13342 ) ) ;
#7815=CARTESIAN_POINT ( 'NONE',  ( 3.033343224707661712, -3.753672977998669946, -7.499999998634409692 ) ) ;
#7818=DIRECTION ( 'NONE',  ( 0.000000000000000000, 0.000000000000000000, 1.000000000000000000 ) ) ;
#7825=CARTESIAN_POINT ( 'NONE',  ( 5.000000000000004441, -2.247904837838113790E-16, -7.920263044861759028 ) ) ;
#7828=CARTESIAN_POINT ( 'NONE',  ( -1.415196051561583790, 4.795541693661363958, -5.750000000000001776 ) ) ;
#7834=CARTESIAN_POINT ( 'NONE',  ( -1.261996585732579224, 4.276409079477648589, -6.312499998634407028 ) ) ;
#7836=CARTESIAN_POINT ( 'NONE',  ( 2.602085213965210642E-15, 8.660254037844392627, -7.422398894150035176 ) ) ;
#7838=ORIENTED_EDGE ( 'NONE', *, *, #11222, .F. ) ;
#7847=CARTESIAN_POINT ( 'NONE',  ( 0.5093500532425063732, 4.799145180956616130, -5.124999998634405252 ) ) ;
#7848=CARTESIAN_POINT ( 'NONE',  ( -4.336808689942017736E-16, -8.660254037844399733, -7.422398894150038728 ) ) ;
#7849=DIRECTION ( 'NONE',  ( -0.000000000000000000, -0.000000000000000000, -1.000000000000000000 ) ) ;
#7866=CARTESIAN_POINT ( 'NONE',  ( 4.209348295687701302, 3.401574460001766109, -0.8124999972688135008 ) ) ;
#7868=CARTESIAN_POINT ( 'NONE',  ( -3.033343224707664376, 3.753672977998667726, -8.249999998634409692 ) ) ;
#7877=CARTESIAN_POINT ( 'NONE',  ( -3.401574460001765221, 4.209348295687701302, -4.687500000000000888 ) ) ;
#7880=LINE ( 'NONE', #10062, #4371 ) ;
#7881=CARTESIAN_POINT ( 'NONE',  ( -5.000000000000092371, -0.7223674278660636716, -8.396799362785968057 ) ) ;
#7884=AXIS2_PLACEMENT_3D ( 'NONE', #2192, #11962, #5837 ) ;
#7885=CARTESIAN_POINT ( 'NONE',  ( 4.209348295687701302, 3.401574460001765665, -7.812499997268815832 ) ) ;
#7909=CARTESIAN_POINT ( 'NONE',  ( 3.753672977998667726, 3.033343224707664376, -5.499999998634407916 ) ) ;
#7912=LINE ( 'NONE', #5234, #1441 ) ;
#7919=CARTESIAN_POINT ( 'NONE',  ( -5.000000000000000888, 6.123233995736767268E-16, -25.03750572909317285 ) ) ;
#7923=( BOUNDED_SURFACE ( )  B_SPLINE_SURFACE ( 3, 2, ( 
 ( #8892, #8008, #1767 ),
 ( #10505, #12739, #801 ),
 ( #12905, #725, #12823 ),
 ( #9366, #15516, #15352 ),
 ( #15438, #4271, #4361 ),
 ( #2971, #14290, #13961 ),
 ( #11539, #1685, #5412 ),
 ( #489, #3139, #14046 ) ),
 .UNSPECIFIED., .F., .F., .F. ) 
 B_SPLINE_SURFACE_WITH_KNOTS ( ( 4, 2, 2, 4 ),
 ( 3, 3 ),
 ( 0.03850042371095789562, 0.04313406099830586343, 0.04545087964197984387, 0.04776769828565383125 ),
 ( 0.000000000000000000, 1.000000000000000000 ),
 .UNSPECIFIED. ) 
 GEOMETRIC_REPRESENTATION_ITEM ( )  RATIONAL_B_SPLINE_SURFACE ( (
 ( 1.000000000000000000, 0.8047781847388131293, 1.000000000000000000),
 ( 1.000000000000000000, 0.8123760230792201886, 1.000000000000000000),
 ( 1.000000000000000000, 0.8190653851697322629, 1.000000000000000000),
 ( 1.000000000000000000, 0.8191940386278004915, 1.000000000000000000),
 ( 1.000000000000000000, 0.8176096570058365431, 1.000000000000000000),
 ( 1.000000000000000000, 0.8122964723274869181, 1.000000000000000000),
 ( 1.000000000000000000, 0.8086312464134836064, 1.000000000000000000),
 ( 1.000000000000000000, 0.8047712192439642198, 1.000000000000000000) ) ) 
 REPRESENTATION_ITEM ( '' )  SURFACE ( )  );
#7926=CARTESIAN_POINT ( 'NONE',  ( 3.753672977998667726, 3.033343224707664820, -7.249999998634409692 ) ) ;
#7931=CARTESIAN_POINT ( 'NONE',  ( 2.131511515620586383, 3.916244202832140253, -4.187499998634405252 ) ) ;
#7937=FACE_BOUND ( 'NONE', #5849, .T. ) ;
#7944=CARTESIAN_POINT ( 'NONE',  ( 4.391654775818395251, -2.390265326283149694, -6.999999997268815832 ) ) ;
#7950=CARTESIAN_POINT ( 'NONE',  ( -3.401574460001765221, 4.209348295687701302, -0.5624999972688168315 ) ) ;
#7951=CARTESIAN_POINT ( 'NONE',  ( 4.276409079477644148, 1.261996585732577891, -8.562499998634409692 ) ) ;
#7952=FACE_OUTER_BOUND ( 'NONE', #13496, .T. ) ;
#7966=CARTESIAN_POINT ( 'NONE',  ( -4.209348295687703967, -3.401574460001763001, -8.312499997268812280 ) ) ;
#7971=CARTESIAN_POINT ( 'NONE',  ( 7.499999999999999112, 1.854554393013824631, -0.1880126015361718583 ) ) ;
#7974=CARTESIAN_POINT ( 'NONE',  ( 3.750000000000005773, 6.495190528383288253, 0.000000000000000000 ) ) ;
#7996=CARTESIAN_POINT ( 'NONE',  ( 3.033343224707661712, -3.753672977998669946, -6.749999998634408804 ) ) ;
#7998=CARTESIAN_POINT ( 'NONE',  ( -2.666517441655246264E-14, 8.895721644649745130, -7.917989418073288377 ) ) ;
#8008=CARTESIAN_POINT ( 'NONE',  ( 7.500000000000000888, -4.651016565836978423, -7.928861822685568050 ) ) ;
#8009=CARTESIAN_POINT ( 'NONE',  ( 3.753672977998667726, 3.033343224707664820, -5.249999998634407916 ) ) ;
#8010=CARTESIAN_POINT ( 'NONE',  ( 0.5984201754795555050, 8.314755988442760426, -0.7022220667781343684 ) ) ;
#8013=CARTESIAN_POINT ( 'NONE',  ( -0.5093500532425060401, -4.799145180956616130, -6.624999998634407916 ) ) ;
#8014=CARTESIAN_POINT ( 'NONE',  ( 0.000000000000000000, 0.000000000000000000, -25.03750572909317285 ) ) ;
#8015=DIRECTION ( 'NONE',  ( -1.000000000000000000, 0.000000000000000000, 0.000000000000000000 ) ) ;
#8020=CARTESIAN_POINT ( 'NONE',  ( -0.04606493828583544531, -9.175055303659563677, -8.057411785091796119 ) ) ;
#8024=CARTESIAN_POINT ( 'NONE',  ( 2.390265326283148806, 4.391654775818395251, -3.749999997268816720 ) ) ;
#8027=LINE ( 'NONE', #10751, #10479 ) ;
#8033=CARTESIAN_POINT ( 'NONE',  ( 4.209348295687701302, 3.401574460001766109, -6.812499997268814944 ) ) ;
#8034=CARTESIAN_POINT ( 'NONE',  ( -4.209348295687703079, -3.401574460001763445, -4.437500000000001776 ) ) ;
#8036=CYLINDRICAL_SURFACE ( 'NONE', #2001, 5.000000000000000888 ) ;
#8044=DIRECTION ( 'NONE',  ( 1.000000000000000000, 0.000000000000000000, 0.000000000000000000 ) ) ;
#8047=CARTESIAN_POINT ( 'NONE',  ( 2.390265326283148806, 4.391654775818395251, -6.749999997268815832 ) ) ;
#8049=CARTESIAN_POINT ( 'NONE',  ( 0.5711823568785988625, 5.381735091635026613, -1.812500000000000666 ) ) ;
#8056=ORIENTED_EDGE ( 'NONE', *, *, #5540, .T. ) ;
#8059=ORIENTED_EDGE ( 'NONE', *, *, #9292, .T. ) ;
#8062=CARTESIAN_POINT ( 'NONE',  ( -7.500000000000007105, 3.639598441879744239, -0.7155132341745296110 ) ) ;
#8065=EDGE_CURVE ( 'NONE', #1633, #12516, #6261, .T. ) ;
#8074=CARTESIAN_POINT ( 'NONE',  ( 1.261996585732578113, -4.276409079477644148, -0.5624999986344088043 ) ) ;
#8087=CARTESIAN_POINT ( 'NONE',  ( 1.261996585732578113, -4.276409079477644148, -6.562499998634407028 ) ) ;
#8091=CARTESIAN_POINT ( 'NONE',  ( -3.916244202832140253, 2.131511515620587272, -5.937499998634407028 ) ) ;
#8095=ORIENTED_EDGE ( 'NONE', *, *, #6819, .F. ) ;
#8097=CARTESIAN_POINT ( 'NONE',  ( 5.112021521198525598, -5.708827036477267747, -7.069802615102038779 ) ) ;
#8099=ORIENTED_EDGE ( 'NONE', *, *, #2831, .F. ) ;
#8100=CARTESIAN_POINT ( 'NONE',  ( -7.500000000000671463, 3.157052757790888453, -7.642767288269949333 ) ) ;
#8113=DIRECTION ( 'NONE',  ( 0.000000000000000000, 0.000000000000000000, 1.000000000000000000 ) ) ;
#8116=ORIENTED_EDGE ( 'NONE', *, *, #5593, .T. ) ;
#8126=CARTESIAN_POINT ( 'NONE',  ( -3.401574460001764777, 4.209348295687701302, -8.562499997268812280 ) ) ;
#8131=DIRECTION ( 'NONE',  ( 1.000000000000000000, 0.000000000000000000, 0.000000000000000000 ) ) ;
#8144=CARTESIAN_POINT ( 'NONE',  ( -4.209348295687703079, -3.401574460001763445, -5.437500000000002665 ) ) ;
#8152=CARTESIAN_POINT ( 'NONE',  ( 4.799145180956616130, -0.5093500532425063732, 0.6250000013655918618 ) ) ;
#8156=VERTEX_POINT ( 'NONE', #9239 ) ;
#8164=CARTESIAN_POINT ( 'NONE',  ( 2.131511515620586383, 3.916244202832140253, -4.187499998634405252 ) ) ;
#8165=CARTESIAN_POINT ( 'NONE',  ( 0.5711823568785988625, 5.381735091635026613, -5.687499997268815832 ) ) ;
#8168=CARTESIAN_POINT ( 'NONE',  ( 4.209348295687701302, 3.401574460001765665, 1.062499999999996225 ) ) ;
#8178=ORIENTED_EDGE ( 'NONE', *, *, #8757, .T. ) ;
#8179=CARTESIAN_POINT ( 'NONE',  ( 4.795541693661363958, 1.415196051561583790, -3.874999997268816720 ) ) ;
#8181=CARTESIAN_POINT ( 'NONE',  ( -4.209348295687703079, -3.401574460001763445, -7.312499997268814944 ) ) ;
#8182=EDGE_CURVE ( 'NONE', #13323, #5937, #9558, .T. ) ;
#8190=AXIS2_PLACEMENT_3D ( 'NONE', #10629, #4557, #6757 ) ;
#8199=DIRECTION ( 'NONE',  ( 1.000000000000000000, 0.000000000000000000, 0.000000000000000000 ) ) ;
#8204=CARTESIAN_POINT ( 'NONE',  ( -5.000000000000004441, -7.530481206757679743E-15, -3.420263044861759916 ) ) ;
#8205=CARTESIAN_POINT ( 'NONE',  ( -4.799145180956616130, 0.5093500532425063732, 1.125000001365592306 ) ) ;
#8207=CARTESIAN_POINT ( 'NONE',  ( -0.5711823568785978633, -5.381735091635035495, -7.187499997268817609 ) ) ;
#8212=ORIENTED_EDGE ( 'NONE', *, *, #8757, .F. ) ;
#8213=LINE ( 'NONE', #13112, #4077 ) ;
#8214=CARTESIAN_POINT ( 'NONE',  ( 0.5711823568785988625, 5.381735091635026613, -2.687499997268816720 ) ) ;
#8216=ADVANCED_FACE ( 'NONE', ( #6154 ), #4931, .F. ) ;
#8227=CARTESIAN_POINT ( 'NONE',  ( -5.000000000000095035, -0.7223674278660573433, -5.521799365517154889 ) ) ;
#8236=CARTESIAN_POINT ( 'NONE',  ( -3.753672977998669946, -3.033343224707661712, 0.2500000013655933606 ) ) ;
#8239=CARTESIAN_POINT ( 'NONE',  ( 7.968863443239234456, 4.547634245050475421, -8.057411785091789014 ) ) ;
#8251=DIRECTION ( 'NONE',  ( 1.000000000000000000, 0.000000000000000000, 0.000000000000000000 ) ) ;
#8253=CARTESIAN_POINT ( 'NONE',  ( -4.799145180956616130, 0.5093500532425063732, -4.874999998634406140 ) ) ;
#8258=CARTESIAN_POINT ( 'NONE',  ( 2.390265326283148806, 4.391654775818395251, 1.124999999999997558 ) ) ;
#8267=CARTESIAN_POINT ( 'NONE',  ( 4.209348295687701302, 3.401574460001766109, -3.812499997268816276 ) ) ;
#8268=ADVANCED_FACE ( 'NONE', ( #7284 ), #8582, .F. ) ;
#8289=CARTESIAN_POINT ( 'NONE',  ( 1.261996585732578113, -4.276409079477644148, -0.5624999986344088043 ) ) ;
#8292=CARTESIAN_POINT ( 'NONE',  ( 3.033343224707661712, -3.753672977998669946, -2.749999998634409248 ) ) ;
#8296=DIRECTION ( 'NONE',  ( 0.8660254037844383745, 0.5000000000000004441, 0.000000000000000000 ) ) ;
#8303=CARTESIAN_POINT ( 'NONE',  ( -5.000000000000003553, 1.292545281756915047E-15, -0.4202630448617610814 ) ) ;
#8306=CARTESIAN_POINT ( 'NONE',  ( -7.908030677224559213, 3.059924800338342354, -7.792662696733363425 ) ) ;
#8307=CARTESIAN_POINT ( 'NONE',  ( -5.000000000000004441, -7.530481206757679743E-15, -2.545263047592944972 ) ) ;
#8308=EDGE_CURVE ( 'NONE', #1307, #2200, #10286, .T. ) ;
#8310=CARTESIAN_POINT ( 'NONE',  ( 1.415196051561583790, -4.795541693661363958, 0.8750000027311841677 ) ) ;
#8312=SURFACE_SIDE_STYLE ('',( #15892 ) ) ;
#8314=CARTESIAN_POINT ( 'NONE',  ( 3.753672977998667726, 3.033343224707664376, -0.2499999986344070280 ) ) ;
#8316=CARTESIAN_POINT ( 'NONE',  ( 0.3875187462269810701, 8.436519985397781696, -7.781689322728073677 ) ) ;
#8317=ORIENTED_EDGE ( 'NONE', *, *, #15194, .T. ) ;
#8326=EDGE_CURVE ( 'NONE', #13728, #1787, #5917, .T. ) ;
#8329=CARTESIAN_POINT ( 'NONE',  ( 2.131511515620586383, 3.916244202832140253, -7.187499998634407916 ) ) ;
#8331=CARTESIAN_POINT ( 'NONE',  ( -4.359993798267272069, -1.826517121560402579, -0.1962993159364725404 ) ) ;
#8337=CARTESIAN_POINT ( 'NONE',  ( -7.894706624614594048, -0.7534108004377911838, -7.590222617908730207 ) ) ;
#8341=CARTESIAN_POINT ( 'NONE',  ( 0.000000000000000000, 0.000000000000000000, -9.999999999999998224 ) ) ;
#8343=EDGE_CURVE ( 'NONE', #637, #3959, #338, .T. ) ;
#8349=CARTESIAN_POINT ( 'NONE',  ( -3.750000000000007550, -6.495190528383289141, 0.000000000000000000 ) ) ;
#8360=CARTESIAN_POINT ( 'NONE',  ( -3.033343224707664376, 3.753672977998667726, -0.9999999986344076941 ) ) ;
#8362=PRODUCT ( 'hex flange nut gradea 1_iso_ISO - 4161 - M10 - N', 'hex flange nut gradea 1_iso_ISO - 4161 - M10 - N', '', ( #11094 ) ) ;
#8363=CARTESIAN_POINT ( 'NONE',  ( -4.276409079477644148, -1.261996585732578335, -2.062499998634406584 ) ) ;
#8373=VERTEX_POINT ( 'NONE', #1448 ) ;
#8375=CARTESIAN_POINT ( 'NONE',  ( 0.5093500532425063732, 4.799145180956616130, -1.374999998634406140 ) ) ;
#8385=DIRECTION ( 'NONE',  ( 0.000000000000000000, 0.000000000000000000, 1.000000000000000000 ) ) ;
#8387=CARTESIAN_POINT ( 'NONE',  ( -4.276409079477644148, -1.261996585732578335, 0.1875000013655918341 ) ) ;
#8389=CARTESIAN_POINT ( 'NONE',  ( -0.2791032213812753571, 8.821394357840558698, -7.929128246061909024 ) ) ;
#8395=B_SPLINE_CURVE_WITH_KNOTS ( 'NONE', 3,
 ( #14876, #11151, #1367, #2492, #176, #6314, #15853, #8584, #10913, #16 ),
 .UNSPECIFIED., .F., .F.,
 ( 4, 2, 2, 2, 4 ),
 ( 0.000000000000000000, 0.002305503304226492935, 0.004611006608452985871, 0.006916509912679477505, 0.009222013216905968272 ),
 .UNSPECIFIED. ) ;
#8398=CYLINDRICAL_SURFACE ( 'NONE', #4505, 5.000000000000000888 ) ;
#8402=CARTESIAN_POINT ( 'NONE',  ( -4.391654775818395251, 2.390265326283148806, 0.3749999999999968914 ) ) ;
#8403=CARTESIAN_POINT ( 'NONE',  ( 3.401574460001763445, -4.209348295687703079, -2.062499997268814500 ) ) ;
#8407=B_SPLINE_CURVE_WITH_KNOTS ( 'NONE', 3,
 ( #2652, #408, #15035, #10023, #334, #14960, #15276, #10270, #11541, #5331, #1769, #11308, #3875, #9136, #5174, #8817, #6716, #13719 ),
 .UNSPECIFIED., .F., .F.,
 ( 4, 2, 2, 2, 2, 2, 2, 2, 4 ),
 ( 0.0005803541179376217390, 0.001389229044063926190, 0.002198103970190230967, 0.003006978896316535744, 0.003815853822442840087, 0.004624728748569143996, 0.005433603674695449207, 0.006242478600821752682, 0.007051353526948056158 ),
 .UNSPECIFIED. ) ;
#8408=CARTESIAN_POINT ( 'NONE',  ( 3.916244202832140253, -2.131511515620588160, 1.312500001365592750 ) ) ;
#8414=DIRECTION ( 'NONE',  ( -0.9396926207859143121, 0.000000000000000000, -0.3420201433256525592 ) ) ;
#8443=CARTESIAN_POINT ( 'NONE',  ( 4.799145180956616130, -0.5093500532425063732, -0.3749999986344090264 ) ) ;
#8446=CARTESIAN_POINT ( 'NONE',  ( 4.276409079477644148, 1.261996585732577891, -1.562499998634406140 ) ) ;
#8448=CARTESIAN_POINT ( 'NONE',  ( 0.5974722283283607771, -8.315303285985692128, -0.7026937717022981866 ) ) ;
#8452=CARTESIAN_POINT ( 'NONE',  ( 4.391654775818395251, -2.390265326283149694, -1.125000000000000888 ) ) ;
#8456=CARTESIAN_POINT ( 'NONE',  ( 4.799145180956616130, -0.5093500532425063732, -3.624999998634407916 ) ) ;
#8461=DIRECTION ( 'NONE',  ( 0.5000000000000004441, 0.8660254037844383745, 0.000000000000000000 ) ) ;
#8463=CARTESIAN_POINT ( 'NONE',  ( 0.5711823568785989735, 5.381735091635026613, -1.687499997268816054 ) ) ;
#8467=CARTESIAN_POINT ( 'NONE',  ( 1.261996585732578113, -4.276409079477644148, -4.562499998634405252 ) ) ;
#8477=AXIS2_PLACEMENT_3D ( 'NONE', #13831, #3971, #8922 ) ;
#8481=CARTESIAN_POINT ( 'NONE',  ( -4.391654775818395251, 2.390265326283148806, -2.625000000000002220 ) ) ;
#8482=CARTESIAN_POINT ( 'NONE',  ( -0.5711823568785977523, -5.381735091635034607, -2.187499997268816276 ) ) ;
#8485=CARTESIAN_POINT ( 'NONE',  ( -4.671041856245029322, -9.682850088987660890E-14, -0.2303389720127052009 ) ) ;
#8489=CARTESIAN_POINT ( 'NONE',  ( -0.5093500532425060401, -4.799145180956616130, -2.874999998634407472 ) ) ;
#8495=AXIS2_PLACEMENT_3D ( 'NONE', #14253, #9255, #2114 ) ;
#8510=CARTESIAN_POINT ( 'NONE',  ( 0.000000000000000000, 0.000000000000000000, -25.03750572909317285 ) ) ;
#8522=CARTESIAN_POINT ( 'NONE',  ( -3.033343224707664376, 3.753672977998667726, 1.365593156898739876E-09 ) ) ;
#8524=ADVANCED_FACE ( 'NONE', ( #1773 ), #9526, .T. ) ;
#8525=CARTESIAN_POINT ( 'NONE',  ( 1.261996585732578113, -4.276409079477644148, -1.812499998634406584 ) ) ;
#8526=DIRECTION ( 'NONE',  ( 0.000000000000000000, 0.000000000000000000, 1.000000000000000000 ) ) ;
#8530=ORIENTED_EDGE ( 'NONE', *, *, #15439, .T. ) ;
#8531=CARTESIAN_POINT ( 'NONE',  ( 3.401574460001763445, -4.209348295687703079, -1.187500000000001998 ) ) ;
#8533=EDGE_LOOP ( 'NONE', ( #2185, #15602, #12196, #15642 ) ) ;
#8535=CARTESIAN_POINT ( 'NONE',  ( 2.131511515620586383, 3.916244202832140253, -3.437499998634407916 ) ) ;
#8540=DIRECTION ( 'NONE',  ( -0.5000000000000008882, -0.8660254037844382635, 0.000000000000000000 ) ) ;
#8542=B_SPLINE_CURVE_WITH_KNOTS ( 'NONE', 3,
 ( #1273, #6218, #8641, #7677, #14857, #3778, #4916, #9763 ),
 .UNSPECIFIED., .F., .F.,
 ( 4, 2, 2, 4 ),
 ( 0.006061689441712453386, 0.007174127271521678166, 0.008286565101330902947, 0.01051144076094935077 ),
 .UNSPECIFIED. ) ;
#8544=CARTESIAN_POINT ( 'NONE',  ( -4.795541693661363958, -1.415196051561583790, -0.3749999972688169980 ) ) ;
#8548=CARTESIAN_POINT ( 'NONE',  ( 2.131511515620586383, 3.916244202832140253, -5.187499998634406140 ) ) ;
#8560=CARTESIAN_POINT ( 'NONE',  ( -4.209348295687703967, -3.401574460001763001, 0.5624999999999957812 ) ) ;
#8561=CARTESIAN_POINT ( 'NONE',  ( -5.000000000000004441, -7.530481206757679743E-15, -2.420263044861759472 ) ) ;
#8564=CARTESIAN_POINT ( 'NONE',  ( -4.799145180956616130, 0.5093500532425063732, -2.124999998634406584 ) ) ;
#8569=LINE ( 'NONE', #15768, #14957 ) ;
#8582=CYLINDRICAL_SURFACE ( 'NONE', #10046, 5.000000000000000888 ) ;
#8584=CARTESIAN_POINT ( 'NONE',  ( 6.602753909532903087, 5.319290460493538042, -7.792447862505328615 ) ) ;
#8595=CARTESIAN_POINT ( 'NONE',  ( -4.799145180956616130, 0.5093500532425063732, -2.874999998634407472 ) ) ;
#8597=CARTESIAN_POINT ( 'NONE',  ( -3.753672977998669946, -3.033343224707661712, -0.9999999986344076941 ) ) ;
#8603=CONICAL_SURFACE ( 'NONE', #1626, 4.174999999999999822, 0.9599310885968795892 ) ;
#8605=CARTESIAN_POINT ( 'NONE',  ( -4.276409079477644148, -1.261996585732578335, -4.062499998634405252 ) ) ;
#8607=AXIS2_PLACEMENT_3D ( 'NONE', #648, #3217, #11928 ) ;
#8608=EDGE_CURVE ( 'NONE', #5764, #13099, #12911, .T. ) ;
#8610=B_SPLINE_CURVE_WITH_KNOTS ( 'NONE', 3,
 ( #12605, #13735, #1703, #5509, #12758, #1548 ),
 .UNSPECIFIED., .F., .F.,
 ( 4, 2, 4 ),
 ( 0.004615310220740744332, 0.006918661718823354567, 0.009222013216905964803 ),
 .UNSPECIFIED. ) ;
#8612=DIRECTION ( 'NONE',  ( 0.000000000000000000, 0.000000000000000000, 1.000000000000000000 ) ) ;
#8617=DIRECTION ( 'NONE',  ( 0.000000000000000000, 0.000000000000000000, 1.000000000000000000 ) ) ;
#8621=CARTESIAN_POINT ( 'NONE',  ( 3.753672977998667726, 3.033343224707664376, -3.249999998634409692 ) ) ;
#8636=CARTESIAN_POINT ( 'NONE',  ( 3.401574460001763001, -4.209348295687703967, -0.1875000000000048572 ) ) ;
#8639=CARTESIAN_POINT ( 'NONE',  ( -3.916244202832140253, 2.131511515620587272, -4.187499998634405252 ) ) ;
#8641=CARTESIAN_POINT ( 'NONE',  ( -7.500000000000005329, -3.640541674360518787, -0.7158139487964652048 ) ) ;
#8644=CARTESIAN_POINT ( 'NONE',  ( -7.500000000000000888, -4.652405105468739421, -7.929127756970859586 ) ) ;
#8647=CARTESIAN_POINT ( 'NONE',  ( 7.894787914004607998, 1.231001383561881556E-13, -7.591390474663423760 ) ) ;
#8652=CARTESIAN_POINT ( 'NONE',  ( 0.000000000000000000, 0.000000000000000000, -25.03750572909317285 ) ) ;
#8670=CARTESIAN_POINT ( 'NONE',  ( 3.401574460001763445, -4.209348295687703079, -4.062499997268815832 ) ) ;
#8671=CARTESIAN_POINT ( 'NONE',  ( 1.261996585732578113, -4.276409079477644148, -3.562499998634407916 ) ) ;
#8674=CARTESIAN_POINT ( 'NONE',  ( -4.276409079477644148, -1.261996585732578335, -4.062499998634405252 ) ) ;
#8682=ORIENTED_EDGE ( 'NONE', *, *, #15378, .F. ) ;
#8686=CARTESIAN_POINT ( 'NONE',  ( -0.5093500532425060401, -4.799145180956616130, -4.874999998634406140 ) ) ;
#8687=CARTESIAN_POINT ( 'NONE',  ( -3.401574460001765221, 4.209348295687701302, -4.562499997268816720 ) ) ;
#8693=CARTESIAN_POINT ( 'NONE',  ( 4.391654775818395251, -2.390265326283149694, -3.999999997268816720 ) ) ;
#8702=CARTESIAN_POINT ( 'NONE',  ( 3.916244202832140253, -2.131511515620588160, -3.437499998634407916 ) ) ;
#8704=ORIENTED_EDGE ( 'NONE', *, *, #7629, .F. ) ;
#8705=ORIENTED_EDGE ( 'NONE', *, *, #4867, .T. ) ;
#8716=CARTESIAN_POINT ( 'NONE',  ( -5.381735091635034607, 0.5711823568785950878, -2.562500000000000888 ) ) ;
#8717=CARTESIAN_POINT ( 'NONE',  ( -1.415196051561583790, 4.795541693661363958, -3.750000000000000000 ) ) ;
#8721=( BOUNDED_SURFACE ( )  B_SPLINE_SURFACE ( 3, 2, ( 
 ( #11440, #15257, #6288 ),
 ( #10331, #12566, #1514 ),
 ( #314, #1422, #11364 ),
 ( #6604, #13866, #13775 ),
 ( #6452, #3855, #2631 ),
 ( #9041, #10085, #7582 ),
 ( #5225, #6369, #10161 ),
 ( #11519, #2799, #2711 ) ),
 .UNSPECIFIED., .F., .F., .F. ) 
 B_SPLINE_SURFACE_WITH_KNOTS ( ( 4, 2, 2, 4 ),
 ( 3, 3 ),
 ( 0.03861844051980971304, 0.04325213341840643266, 0.04556897986770479247, 0.04788582631700314535 ),
 ( 0.000000000000000000, 1.000000000000000000 ),
 .UNSPECIFIED. ) 
 GEOMETRIC_REPRESENTATION_ITEM ( )  RATIONAL_B_SPLINE_SURFACE ( (
 ( 1.000000000000000000, 0.8047781759831923454, 1.000000000000000000),
 ( 1.000000000000000000, 0.8123762462804495765, 1.000000000000000000),
 ( 1.000000000000000000, 0.8190659850617496573, 1.000000000000000000),
 ( 1.000000000000000000, 0.8191937571013253594, 1.000000000000000000),
 ( 1.000000000000000000, 0.8176092952781198742, 1.000000000000000000),
 ( 1.000000000000000000, 0.8122962088595745422, 1.000000000000000000),
 ( 1.000000000000000000, 0.8086311330828506172, 1.000000000000000000),
 ( 1.000000000000000000, 0.8047712282214323221, 1.000000000000000000) ) ) 
 REPRESENTATION_ITEM ( '' )  SURFACE ( )  );
#8723=CARTESIAN_POINT ( 'NONE',  ( 0.5093500532425063732, 4.799145180956616130, -4.374999998634405252 ) ) ;
#8726=CARTESIAN_POINT ( 'NONE',  ( -7.894787914004611551, -0.7661396099416333261, -7.591390474663429089 ) ) ;
#8736=CIRCLE ( 'NONE', #10793, 10.39117206796836079 ) ;
#8749=FILL_AREA_STYLE_COLOUR ( '', #2681 ) ;
#8751=CARTESIAN_POINT ( 'NONE',  ( 4.535975386569504053, 1.338596318647080397, -8.156249999317205734 ) ) ;
#8757=EDGE_CURVE ( 'NONE', #3896, #1633, #861, .T. ) ;
#8758=DIRECTION ( 'NONE',  ( 0.000000000000000000, 0.000000000000000000, 1.000000000000000000 ) ) ;
#8759=CARTESIAN_POINT ( 'NONE',  ( 4.799145180956616130, -0.5093500532425063732, -4.374999998634405252 ) ) ;
#8762=CARTESIAN_POINT ( 'NONE',  ( -3.916244202832140253, 2.131511515620587272, -6.187499998634407028 ) ) ;
#8766=CARTESIAN_POINT ( 'NONE',  ( -7.500000000000005329, 4.330127018922194537, -7.422398894150031623 ) ) ;
#8767=ORIENTED_EDGE ( 'NONE', *, *, #14160, .F. ) ;
#8768=CARTESIAN_POINT ( 'NONE',  ( 5.000000000000004441, 6.350331166892669572E-15, -1.045263047592943417 ) ) ;
#8771=CARTESIAN_POINT ( 'NONE',  ( -3.033343224707664820, 3.753672977998667726, -8.249999998634409692 ) ) ;
#8779=CARTESIAN_POINT ( 'NONE',  ( 4.391654775818395251, -2.390265326283149694, -1.999999997268814944 ) ) ;
#8781=CARTESIAN_POINT ( 'NONE',  ( -4.361069479627173173, 1.579581656101586296, -0.2612589832309742399 ) ) ;
#8784=DIRECTION ( 'NONE',  ( -1.000000000000000000, 0.000000000000000000, 0.000000000000000000 ) ) ;
#8785=CARTESIAN_POINT ( 'NONE',  ( 1.261996585732578113, -4.276409079477644148, -3.562499998634407916 ) ) ;
#8794=CARTESIAN_POINT ( 'NONE',  ( -0.6508621380849234361, -8.763657152406455708, -7.907633014911227498 ) ) ;
#8797=CARTESIAN_POINT ( 'NONE',  ( 1.415196051561583790, -4.795541693661363958, -6.250000000000001776 ) ) ;
#8798=CARTESIAN_POINT ( 'NONE',  ( -4.391654775818395251, 2.390265326283148806, -2.625000000000002220 ) ) ;
#8801=CARTESIAN_POINT ( 'NONE',  ( 3.916244202832140253, -2.131511515620588160, -0.6874999986344089153 ) ) ;
#8803=CARTESIAN_POINT ( 'NONE',  ( -7.914973979435151463, -3.817460047930451239, -7.907502498112421563 ) ) ;
#8813=ADVANCED_FACE ( 'NONE', ( #5071, #10166 ), #11522, .T. ) ;
#8816=CARTESIAN_POINT ( 'NONE',  ( 3.033343224707661712, -3.753672977998669502, -0.4999999986344072500 ) ) ;
#8817=CARTESIAN_POINT ( 'NONE',  ( 1.111665111977238718, 4.326204543705408412, -0.3789984458506780451 ) ) ;
#8836=CARTESIAN_POINT ( 'NONE',  ( -2.131511515620587272, -3.916244202832140253, -6.937499998634407916 ) ) ;
#8841=B_SPLINE_CURVE_WITH_KNOTS ( 'NONE', 3,
 ( #2990, #1373, #5430, #12440, #11558, #9074 ),
 .UNSPECIFIED., .F., .F.,
 ( 4, 2, 4 ),
 ( 0.000000000000000000, 0.0004189869898914150835, 0.0008379739797828320100 ),
 .UNSPECIFIED. ) ;
#8847=CARTESIAN_POINT ( 'NONE',  ( -4.276409079477644148, -1.261996585732578335, -8.062499998634407916 ) ) ;
#8848=CARTESIAN_POINT ( 'NONE',  ( 2.390265326283148806, 4.391654775818395251, -4.749999997268817609 ) ) ;
#8851=CARTESIAN_POINT ( 'NONE',  ( -3.093157300003891663, -6.874418838041295388, -4.773877690725237500E-15 ) ) ;
#8854=CARTESIAN_POINT ( 'NONE',  ( 4.795541693661363958, 1.415196051561583790, -3.874999997268816720 ) ) ;
#8855=CARTESIAN_POINT ( 'NONE',  ( 0.5711823568785988625, 5.381735091635026613, -8.687499997268814056 ) ) ;
#8860=CARTESIAN_POINT ( 'NONE',  ( 2.131511515620586383, 3.916244202832140253, -7.187499998634407916 ) ) ;
#8874=CARTESIAN_POINT ( 'NONE',  ( 5.381735091635035495, -0.5711823568785978633, -4.062499999999999112 ) ) ;
#8878=CARTESIAN_POINT ( 'NONE',  ( 4.799145180956616130, -0.5093500532425063732, -7.624999998634408804 ) ) ;
#8880=DIRECTION ( 'NONE',  ( -1.000000000000000000, 0.000000000000000000, 0.000000000000000000 ) ) ;
#8892=CARTESIAN_POINT ( 'NONE',  ( 7.500000000000000000, -4.730916290271727220, -7.493595886788497751 ) ) ;
#8896=FACE_OUTER_BOUND ( 'NONE', #5366, .T. ) ;
#8899=CARTESIAN_POINT ( 'NONE',  ( 0.000000000000000000, 0.000000000000000000, -25.03750572909317285 ) ) ;
#8904=ORIENTED_EDGE ( 'NONE', *, *, #4007, .T. ) ;
#8919=CARTESIAN_POINT ( 'NONE',  ( 2.131511515620586383, 3.916244202832140253, -4.437499998634405252 ) ) ;
#8922=DIRECTION ( 'NONE',  ( 1.000000000000000000, 0.000000000000000000, 0.000000000000000000 ) ) ;
#8926=CARTESIAN_POINT ( 'NONE',  ( -0.5711823568785977523, -5.381735091635034607, -7.312500000000006217 ) ) ;
#8930=CARTESIAN_POINT ( 'NONE',  ( 4.276409079477644148, 1.261996585732577891, -6.562499998634407028 ) ) ;
#8937=CARTESIAN_POINT ( 'NONE',  ( 4.795541693661363958, 1.415196051561583790, -5.874999997268814944 ) ) ;
#8939=CARTESIAN_POINT ( 'NONE',  ( -1.036170633859778700, 4.395255856367823455, -0.3471699856533662087 ) ) ;
#8958=CARTESIAN_POINT ( 'NONE',  ( -4.795541693661363958, -1.415196051561583790, -3.499999999999999556 ) ) ;
#8963=CARTESIAN_POINT ( 'NONE',  ( -2.131511515620587272, -3.916244202832140253, -7.937499998634408804 ) ) ;
#8965=CARTESIAN_POINT ( 'NONE',  ( 6.874999999999999112, 4.690970937165705124, -7.298562697733105509 ) ) ;
#8976=CARTESIAN_POINT ( 'NONE',  ( -4.276409079477644148, -1.261996585732578335, -1.812499998634406584 ) ) ;
#8984=CARTESIAN_POINT ( 'NONE',  ( 0.000000000000000000, 0.000000000000000000, -0.5776712190230133270 ) ) ;
#8990=AXIS2_PLACEMENT_3D ( 'NONE', #303, #12785, #8784 ) ;
#9001=CARTESIAN_POINT ( 'NONE',  ( -4.391654775818395251, 2.390265326283148806, -5.625000000000001776 ) ) ;
#9002=CARTESIAN_POINT ( 'NONE',  ( 2.131511515620586383, 3.916244202832140253, -6.437499998634407028 ) ) ;
#9015=CARTESIAN_POINT ( 'NONE',  ( 2.131511515620586383, 3.916244202832140253, -5.437499998634406140 ) ) ;
#9017=EDGE_CURVE ( 'NONE', #3976, #12516, #9430, .T. ) ;
#9021=CARTESIAN_POINT ( 'NONE',  ( 4.795541693661363958, 1.415196051561583790, -3.469446951953614189E-15 ) ) ;
#9022=CARTESIAN_POINT ( 'NONE',  ( -0.5984201754795709371, -8.314755988442765755, -0.7022220667781371439 ) ) ;
#9024=CARTESIAN_POINT ( 'NONE',  ( -0.5711823568785978633, -5.381735091635035495, -3.187499997268817609 ) ) ;
#9030=CARTESIAN_POINT ( 'NONE',  ( 7.500000000000000000, 4.330127018922190096, -7.422398894150031623 ) ) ;
#9036=CARTESIAN_POINT ( 'NONE',  ( -1.305263714129176078, 8.377797850839289850, -7.792447862505333056 ) ) ;
#9039=EDGE_CURVE ( 'NONE', #5622, #3351, #7625, .T. ) ;
#9041=CARTESIAN_POINT ( 'NONE',  ( -1.013163106017127779, -8.075304045852414347, -7.231838333420567366 ) ) ;
#9043=CARTESIAN_POINT ( 'NONE',  ( -0.5711823568785978633, -5.381735091635035495, -7.312500000000004441 ) ) ;
#9047=CARTESIAN_POINT ( 'NONE',  ( 2.131511515620586383, 3.916244202832140253, -6.437499998634407028 ) ) ;
#9049=CARTESIAN_POINT ( 'NONE',  ( 7.500000000000009770, -4.330127018922195425, -7.564338275809340040 ) ) ;
#9050=VERTEX_POINT ( 'NONE', #12968 ) ;
#9060=CARTESIAN_POINT ( 'NONE',  ( -0.5093500532425060401, -4.799145180956616130, -1.624999998634406362 ) ) ;
#9063=CARTESIAN_POINT ( 'NONE',  ( -3.916244202832140253, 2.131511515620587272, -4.937499998634406140 ) ) ;
#9070=ORIENTED_EDGE ( 'NONE', *, *, #15170, .T. ) ;
#9072=ADVANCED_FACE ( 'NONE', ( #1903 ), #5113, .T. ) ;
#9074=CARTESIAN_POINT ( 'NONE',  ( 7.922281120364393914, 4.573931137438269623, -8.047472243342932430 ) ) ;
#9079=LINE ( 'NONE', #13820, #12863 ) ;
#9083=CARTESIAN_POINT ( 'NONE',  ( 3.033343224707661712, -3.753672977998669946, 0.2500000013655933606 ) ) ;
#9095=CARTESIAN_POINT ( 'NONE',  ( 4.209348295687701302, 3.401574460001765665, -8.812499997268814056 ) ) ;
#9102=CARTESIAN_POINT ( 'NONE',  ( 6.288404560131952259, 5.029641972278930062, -0.4504974108211944883 ) ) ;
#9106=ORIENTED_EDGE ( 'NONE', *, *, #11651, .F. ) ;
#9107=EDGE_CURVE ( 'NONE', #5402, #2543, #8736, .T. ) ;
#9118=CARTESIAN_POINT ( 'NONE',  ( -3.401574460001764777, 4.209348295687701302, -3.687500000000000444 ) ) ;
#9120=DIRECTION ( 'NONE',  ( 0.000000000000000000, 0.000000000000000000, 1.000000000000000000 ) ) ;
#9122=CARTESIAN_POINT ( 'NONE',  ( -1.261996585732579224, 4.276409079477648589, -5.312499998634406140 ) ) ;
#9124=CARTESIAN_POINT ( 'NONE',  ( 7.922281120364393914, -4.573931137438281169, -8.047472243342932430 ) ) ;
#9135=CARTESIAN_POINT ( 'NONE',  ( -3.916244202832140253, 2.131511515620587272, -2.937499998634407472 ) ) ;
#9136=CARTESIAN_POINT ( 'NONE',  ( 1.865935176646638549, 4.058319590311958436, -0.3789984458506300835 ) ) ;
#9138=CARTESIAN_POINT ( 'NONE',  ( -3.753672977998669946, -3.033343224707661712, -1.749999998634408360 ) ) ;
#9139=DIRECTION ( 'NONE',  ( 0.000000000000000000, 0.000000000000000000, 1.000000000000000000 ) ) ;
#9140=MANIFOLD_SOLID_BREP ( 'Cavity1', #6899 ) ;
#9143=FACE_OUTER_BOUND ( 'NONE', #3989, .T. ) ;
#9145=CARTESIAN_POINT ( 'NONE',  ( -4.999999999999847233, 1.272547481429013860, -6.586597482644652501 ) ) ;
#9146=VERTEX_POINT ( 'NONE', #6269 ) ;
#9152=ORIENTED_EDGE ( 'NONE', *, *, #11942, .F. ) ;
#9158=EDGE_CURVE ( 'NONE', #13539, #3896, #11639, .T. ) ;
#9162=VERTEX_POINT ( 'NONE', #1325 ) ;
#9174=CARTESIAN_POINT ( 'NONE',  ( -4.209348295687703967, -3.401574460001763001, -7.312499997268814944 ) ) ;
#9184=CARTESIAN_POINT ( 'NONE',  ( 0.000000000000000000, 0.000000000000000000, -9.999999999999998224 ) ) ;
#9192=APPLICATION_CONTEXT ( 'automotive_design' ) ;
#9202=CARTESIAN_POINT ( 'NONE',  ( 4.799145180956616130, -0.5093500532425063732, -5.624999998634406140 ) ) ;
#9209=CARTESIAN_POINT ( 'NONE',  ( 10.39117206796836079, 1.272551561242683567E-15, -8.499999999999996447 ) ) ;
#9213=CARTESIAN_POINT ( 'NONE',  ( 2.131511515620586383, 3.916244202832140253, -5.187499998634406140 ) ) ;
#9218=CARTESIAN_POINT ( 'NONE',  ( -4.799145180956616130, 0.5093500532425063732, -7.874999998634408804 ) ) ;
#9224=CARTESIAN_POINT ( 'NONE',  ( 5.000000000000095923, 0.7223674278660565662, -7.021799365517158442 ) ) ;
#9227=ORIENTED_EDGE ( 'NONE', *, *, #15781, .F. ) ;
#9230=ORIENTED_EDGE ( 'NONE', *, *, #4162, .F. ) ;
#9234=AXIS2_PLACEMENT_3D ( 'NONE', #9329, #6672, #4471 ) ;
#9238=CARTESIAN_POINT ( 'NONE',  ( 2.390265326283148806, 4.391654775818395251, -6.749999997268815832 ) ) ;
#9239=CARTESIAN_POINT ( 'NONE',  ( 5.000000000000003553, 1.275685995473128912E-14, -5.920263044861758139 ) ) ;
#9242=CARTESIAN_POINT ( 'NONE',  ( 7.500000000000003553, -4.330127018922199866, -7.422398894150035176 ) ) ;
#9245=( BOUNDED_CURVE ( )  B_SPLINE_CURVE ( 2, ( #10710, #13034, #1977, #6923, #11828, #777, #10636, #15646, #4564, #9498, #14430, #3355, #14740, #15963, #1008, #9726, #7477, #8375, #5939, #10863, #12061, #12381, #1316, #6260, #15804, #4884, #13353, #14662, #5038, #117, #13266, #11175, #9968, #13589, #11104, #2438, #3422, #14574, #1153, #9811, #3497, #6095, #11024, #13425, #12298, #2208, #7160, #2518, #4720, #3589, #8535, #9640, #7313, #8456, #2363, #12215, #2294, #3662, #4800, #1234, #8605, #6185, #7242, #12139, #42, #13500, #4956, #7390, #9884, #14816, #3741, #1078, #6015, #8686, #10940, #15879, #12694, #12458, #11414, #4142, #2684, #13839, #9015, #15063, #14988, #1564, #7642, #13752, #13674, #11258, #2605, #2770, #10059, #14909, #12537, #1637, #13921, #5279, #10307, #5127, #8930, #289, #1482, #7727, #12623, #5202, #10219, #7558, #1394, #6576, #5367, #10133, #3977, #11493, #6502, #3901, #363, #15143, #440, #4063, #6426, #2848, #7802, #15231, #8847, #208, #3827, #8771, #6340, #11342, #13558, #5008, #2410 ),
 .UNSPECIFIED., .F., .F. ) 
 B_SPLINE_CURVE_WITH_KNOTS ( ( 3, 2, 2, 2, 2, 2, 2, 2, 2, 2, 2, 2, 2, 2, 2, 2, 2, 2, 2, 2, 2, 2, 2, 2, 2, 2, 2, 2, 2, 2, 2, 2, 2, 2, 2, 2, 2, 2, 2, 2, 2, 2, 2, 2, 2, 2, 2, 2, 2, 2, 2, 2, 2, 2, 2, 2, 2, 2, 2, 2, 2, 2, 2, 2, 2, 2, 3 ),
 ( 0.1816346841896726849, 0.1875000000000000000, 0.2000000000000000111, 0.2124999999999999944, 0.2250000000000000056, 0.2374999999999999889, 0.2500000000000000000, 0.2625000000000000111, 0.2750000000000000222, 0.2874999999999999778, 0.2999999999999999889, 0.3125000000000000000, 0.3250000000000000111, 0.3375000000000000222, 0.3499999999999999778, 0.3624999999999999889, 0.3750000000000000000, 0.3875000000000000111, 0.4000000000000000222, 0.4124999999999999778, 0.4250000000000000444, 0.4375000000000000000, 0.4499999999999999556, 0.4625000000000000222, 0.4749999999999999778, 0.4875000000000000444, 0.5000000000000000000, 0.5124999999999999556, 0.5250000000000000222, 0.5374999999999999778, 0.5500000000000000444, 0.5625000000000000000, 0.5749999999999999556, 0.5875000000000000222, 0.5999999999999999778, 0.6125000000000000444, 0.6250000000000000000, 0.6374999999999999556, 0.6500000000000000222, 0.6624999999999999778, 0.6750000000000001554, 0.6875000000000000000, 0.6999999999999999556, 0.7125000000000000222, 0.7249999999999999778, 0.7375000000000000444, 0.7500000000000000000, 0.7624999999999999556, 0.7750000000000000222, 0.7874999999999999778, 0.8000000000000000444, 0.8125000000000000000, 0.8249999999999999556, 0.8375000000000000222, 0.8499999999999999778, 0.8625000000000000444, 0.8750000000000000000, 0.8874999999999999556, 0.8999999999999999112, 0.9124999999999999778, 0.9250000000000000444, 0.9375000000000000000, 0.9499999999999999556, 0.9624999999999999112, 0.9749999999999999778, 0.9875000000000000444, 1.000000000000000000 ),
 .UNSPECIFIED. ) 
 CURVE ( )  GEOMETRIC_REPRESENTATION_ITEM ( )  RATIONAL_B_SPLINE_CURVE ( ( 0.9620839512587866516, 0.9642823534839155553, 1.000000000000000000, 0.9238795325112867385, 1.000000000000000000, 0.9238795325112867385, 1.000000000000000000, 0.9238795325112867385, 1.000000000000000000, 0.9238795325112867385, 1.000000000000000000, 0.9238795325112867385, 1.000000000000000000, 0.9238795325112867385, 1.000000000000000000, 0.9238795325112867385, 1.000000000000000000, 0.9238795325112867385, 1.000000000000000000, 0.9238795325112867385, 1.000000000000000000, 0.9238795325112867385, 1.000000000000000000, 0.9238795325112867385, 1.000000000000000000, 0.9238795325112867385, 1.000000000000000000, 0.9238795325112867385, 1.000000000000000000, 0.9238795325112867385, 1.000000000000000000, 0.9238795325112867385, 1.000000000000000000, 0.9238795325112867385, 1.000000000000000000, 0.9238795325112867385, 1.000000000000000000, 0.9238795325112867385, 1.000000000000000000, 0.9238795325112867385, 1.000000000000000000, 0.9238795325112867385, 1.000000000000000000, 0.9238795325112867385, 1.000000000000000000, 0.9238795325112867385, 1.000000000000000000, 0.9238795325112867385, 1.000000000000000000, 0.9238795325112867385, 1.000000000000000000, 0.9238795325112867385, 1.000000000000000000, 0.9238795325112867385, 1.000000000000000000, 0.9238795325112867385, 1.000000000000000000, 0.9238795325112867385, 1.000000000000000000, 0.9238795325112867385, 1.000000000000000000, 0.9238795325112867385, 1.000000000000000000, 0.9238795325112867385, 1.000000000000000000, 0.9238795325112867385, 1.000000000000000000, 0.9238795325112867385, 1.000000000000000000, 0.9238795325112867385, 1.000000000000000000, 0.9238795325112867385, 1.000000000000000000, 0.9238795325112867385, 1.000000000000000000, 0.9238795325112867385, 1.000000000000000000, 0.9238795325112867385, 1.000000000000000000, 0.9238795325112867385, 1.000000000000000000, 0.9238795325112867385, 1.000000000000000000, 0.9238795325112867385, 1.000000000000000000, 0.9238795325112867385, 1.000000000000000000, 0.9238795325112867385, 1.000000000000000000, 0.9238795325112867385, 1.000000000000000000, 0.9238795325112867385, 1.000000000000000000, 0.9238795325112867385, 1.000000000000000000, 0.9238795325112867385, 1.000000000000000000, 0.9238795325112867385, 1.000000000000000000, 0.9238795325112867385, 1.000000000000000000, 0.9238795325112867385, 1.000000000000000000, 0.9238795325112867385, 1.000000000000000000, 0.9238795325112867385, 1.000000000000000000, 0.9238795325112867385, 1.000000000000000000, 0.9238795325112867385, 1.000000000000000000, 0.9238795325112867385, 1.000000000000000000, 0.9238795325112867385, 1.000000000000000000, 0.9238795325112867385, 1.000000000000000000, 0.9238795325112867385, 1.000000000000000000, 0.9238795325112867385, 1.000000000000000000, 0.9238795325112867385, 1.000000000000000000, 0.9238795325112867385, 1.000000000000000000, 0.9238795325112867385, 1.000000000000000000, 0.9238795325112867385, 1.000000000000000000, 0.9238795325112867385, 1.000000000000000000, 0.9238795325112867385, 1.000000000000000000 ) ) 
 REPRESENTATION_ITEM ( '' )  );
#9248=CARTESIAN_POINT ( 'NONE',  ( -7.779103221381285849, 4.168986698926044454, -7.929128246061914354 ) ) ;
#9250=ORIENTED_EDGE ( 'NONE', *, *, #4567, .F. ) ;
#9255=DIRECTION ( 'NONE',  ( -0.000000000000000000, -0.000000000000000000, -1.000000000000000000 ) ) ;
#9258=CARTESIAN_POINT ( 'NONE',  ( -1.261996585732579224, 4.276409079477648589, 0.6875000013655923059 ) ) ;
#9260=CARTESIAN_POINT ( 'NONE',  ( -1.415196051561583790, 4.795541693661363958, -1.750000000000001554 ) ) ;
#9267=ORIENTED_EDGE ( 'NONE', *, *, #14135, .F. ) ;
#9285=CARTESIAN_POINT ( 'NONE',  ( 1.261996585732578113, -4.276409079477644148, 1.437500001365592972 ) ) ;
#9287=CARTESIAN_POINT ( 'NONE',  ( 4.859103478305521033E-15, 8.660254037844390851, -7.564335161054499324 ) ) ;
#9292=EDGE_CURVE ( 'NONE', #10281, #1816, #11817, .T. ) ;
#9294=CARTESIAN_POINT ( 'NONE',  ( -5.000000000000002665, -1.404940523648820476E-14, -6.545263047592945860 ) ) ;
#9297=CARTESIAN_POINT ( 'NONE',  ( 3.753672977998667726, 3.033343224707664820, -6.249999998634408804 ) ) ;
#9300=CARTESIAN_POINT ( 'NONE',  ( -3.916244202832140253, 2.131511515620587272, -7.937499998634408804 ) ) ;
#9309=CARTESIAN_POINT ( 'NONE',  ( 5.000000000000004441, -2.247904837838113790E-16, -3.920263044861760360 ) ) ;
#9314=ORIENTED_EDGE ( 'NONE', *, *, #11198, .F. ) ;
#9320=CARTESIAN_POINT ( 'NONE',  ( 0.5093500532425063732, 4.799145180956616130, -8.374999998634409692 ) ) ;
#9321=CARTESIAN_POINT ( 'NONE',  ( 0.5093500532425063732, 4.799145180956616130, -0.3749999986344090264 ) ) ;
#9323=ORIENTED_EDGE ( 'NONE', *, *, #8182, .F. ) ;
#9329=CARTESIAN_POINT ( 'NONE',  ( 0.000000000000000000, 0.000000000000000000, -9.999999999999998224 ) ) ;
#9330=( BOUNDED_CURVE ( )  B_SPLINE_CURVE ( 2, ( #6362, #11282, #6688, #10394, #12643, #1581, #11596, #380, #1507, #11434, #5300 ),
 .UNSPECIFIED., .F., .F. ) 
 B_SPLINE_CURVE_WITH_KNOTS ( ( 3, 2, 2, 2, 2, 3 ),
 ( 0.2045872658012772849, 0.2124999999999999944, 0.2250000000000000056, 0.2374999999999999889, 0.2500000000000000000, 0.2545872658012772738 ),
 .UNSPECIFIED. ) 
 CURVE ( )  GEOMETRIC_REPRESENTATION_ITEM ( )  RATIONAL_B_SPLINE_CURVE ( ( 0.9646335149384808183, 0.9518143178943438976, 1.000000000000000000, 0.9238795325112867385, 1.000000000000000000, 0.9238795325112867385, 1.000000000000000000, 0.9238795325112867385, 1.000000000000000000, 0.9720652146169430630, 0.9646335149384808183 ) ) 
 REPRESENTATION_ITEM ( '' )  );
#9331=CARTESIAN_POINT ( 'NONE',  ( -3.401574460001764777, 4.209348295687701302, -6.562499997268814944 ) ) ;
#9337=CARTESIAN_POINT ( 'NONE',  ( -7.703920929261746764, 4.447860822324885888, -7.917989418073283048 ) ) ;
#9341=ORIENTED_EDGE ( 'NONE', *, *, #2677, .T. ) ;
#9349=CARTESIAN_POINT ( 'NONE',  ( 4.458734124999998549, -3.052311964297492742E-11, -0.3789984458506765463 ) ) ;
#9356=CARTESIAN_POINT ( 'NONE',  ( 4.276409079477644148, 1.261996585732577891, -1.312499998634406140 ) ) ;
#9359=DIRECTION ( 'NONE',  ( 0.000000000000000000, 0.000000000000000000, -1.000000000000000000 ) ) ;
#9364=DIRECTION ( 'NONE',  ( 0.000000000000000000, 0.000000000000000000, 1.000000000000000000 ) ) ;
#9366=CARTESIAN_POINT ( 'NONE',  ( 7.500000000000000000, 0.7723602884921818568, -7.026388801733943978 ) ) ;
#9368=CARTESIAN_POINT ( 'NONE',  ( -0.5093500532425060401, -4.799145180956616130, -5.624999998634405252 ) ) ;
#9369=CARTESIAN_POINT ( 'NONE',  ( -5.000000000000004441, -1.011557177027151181E-15, -5.420263044861760804 ) ) ;
#9371=CARTESIAN_POINT ( 'NONE',  ( -5.381735091635034607, 0.5711823568785950878, 1.437499999999998446 ) ) ;
#9373=EDGE_CURVE ( 'NONE', #7550, #12914, #15129, .T. ) ;
#9380=EDGE_LOOP ( 'NONE', ( #5698, #9915, #5741, #4971 ) ) ;
#9381=VERTEX_POINT ( 'NONE', #4554 ) ;
#9394=CARTESIAN_POINT ( 'NONE',  ( 3.033343224707661712, -3.753672977998669946, -7.749999998634409692 ) ) ;
#9406=CARTESIAN_POINT ( 'NONE',  ( -3.401574460001764777, 4.209348295687701302, -7.562499997268814944 ) ) ;
#9412=CARTESIAN_POINT ( 'NONE',  ( 4.209348295687701302, 3.401574460001766109, -2.812499997268815388 ) ) ;
#9415=ORIENTED_EDGE ( 'NONE', *, *, #6179, .F. ) ;
#9422=CARTESIAN_POINT ( 'NONE',  ( -4.406842699996125212, 6.115962218725290001, -6.301925127571993537E-16 ) ) ;
#9430=LINE ( 'NONE', #3287, #480 ) ;
#9432=CARTESIAN_POINT ( 'NONE',  ( -3.753672977998669946, -3.033343224707661712, 1.250000001365594304 ) ) ;
#9434=CARTESIAN_POINT ( 'NONE',  ( 5.174575781540989183, 5.672711317429576461, -7.030005583190789942 ) ) ;
#9442=EDGE_CURVE ( 'NONE', #1601, #2454, #10111, .T. ) ;
#9444=CARTESIAN_POINT ( 'NONE',  ( 0.5093500532425063732, 4.799145180956616130, -7.124999998634407916 ) ) ;
#9445=CARTESIAN_POINT ( 'NONE',  ( 4.209348295687701302, 3.401574460001766109, -5.812499997268813168 ) ) ;
#9447=CARTESIAN_POINT ( 'NONE',  ( 3.916244202832140253, -2.131511515620588160, -6.437499998634407028 ) ) ;
#9452=ORIENTED_EDGE ( 'NONE', *, *, #1485, .F. ) ;
#9457=CARTESIAN_POINT ( 'NONE',  ( 7.500000000000000888, -3.640541674360524116, -0.7158139487964624292 ) ) ;
#9460=ORIENTED_EDGE ( 'NONE', *, *, #5449, .F. ) ;
#9483=CARTESIAN_POINT ( 'NONE',  ( 3.753672977998667726, 3.033343224707664376, -0.2499999986344070280 ) ) ;
#9485=CARTESIAN_POINT ( 'NONE',  ( -4.276409079477644148, -1.261996585732578335, -0.06249999863440838799 ) ) ;
#9486=CARTESIAN_POINT ( 'NONE',  ( 4.209348295687701302, 3.401574460001766109, -0.9375000000000017764 ) ) ;
#9490=CARTESIAN_POINT ( 'NONE',  ( 4.631580223510930239, 1.444531747605005878E-11, -0.2579703047231843294 ) ) ;
#9498=CARTESIAN_POINT ( 'NONE',  ( -0.5093500532425060401, -4.799145180956616130, -0.8749999986344056957 ) ) ;
#9507=CARTESIAN_POINT ( 'NONE',  ( 0.5711823568785989735, 5.381735091635026613, -7.812500000000005329 ) ) ;
#9508=CARTESIAN_POINT ( 'NONE',  ( 5.000000000000004441, -2.247904837838113790E-16, -3.045263047592945860 ) ) ;
#9510=CARTESIAN_POINT ( 'NONE',  ( 4.276409079477644148, 1.261996585732577891, -0.3124999986344085823 ) ) ;
#9512=CARTESIAN_POINT ( 'NONE',  ( 2.411464220262452773, 7.267994521134256480, -7.491772860716523041 ) ) ;
#9513=ORIENTED_EDGE ( 'NONE', *, *, #11222, .T. ) ;
#9516=VECTOR ( 'NONE', #768, 1000.000000000000000 ) ;
#9526=CONICAL_SURFACE ( 'NONE', #11578, 7.500000000000001776, 0.8594454914424796144 ) ;
#9528=CARTESIAN_POINT ( 'NONE',  ( 0.5093500532425063732, 4.799145180956616130, -6.124999998634407916 ) ) ;
#9530=CARTESIAN_POINT ( 'NONE',  ( -4.524602526901894350, -1.321206833522081014, -0.2058151098866615736 ) ) ;
#9532=VERTEX_POINT ( 'NONE', #2674 ) ;
#9538=CARTESIAN_POINT ( 'NONE',  ( -7.897827455343219505, -1.533134349199730018, -7.633632140068247196 ) ) ;
#9553=EDGE_CURVE ( 'NONE', #11169, #6761, #282, .T. ) ;
#9554=ORIENTED_EDGE ( 'NONE', *, *, #1540, .F. ) ;
#9558=( BOUNDED_CURVE ( )  B_SPLINE_CURVE ( 2, ( #14400, #10530, #6893, #4300, #11797, #15465, #750, #8034, #12928, #15615, #5675 ),
 .UNSPECIFIED., .F., .F. ) 
 B_SPLINE_CURVE_WITH_KNOTS ( ( 3, 2, 2, 2, 2, 3 ),
 ( 0.6045872658012773071, 0.6125000000000000444, 0.6250000000000000000, 0.6374999999999999556, 0.6500000000000000222, 0.6545872658012773515 ),
 .UNSPECIFIED. ) 
 CURVE ( )  GEOMETRIC_REPRESENTATION_ITEM ( )  RATIONAL_B_SPLINE_CURVE ( ( 0.9646335149384808183, 0.9518143178943441196, 1.000000000000000000, 0.9238795325112867385, 1.000000000000000000, 0.9238795325112867385, 1.000000000000000000, 0.9238795325112867385, 1.000000000000000000, 0.9720652146169423968, 0.9646335149384803742 ) ) 
 REPRESENTATION_ITEM ( '' )  );
#9559=CARTESIAN_POINT ( 'NONE',  ( 3.401574460001763445, -4.209348295687703079, -3.062499997268815388 ) ) ;
#9561=CARTESIAN_POINT ( 'NONE',  ( -0.5093500532425060401, -4.799145180956616130, -2.874999998634407472 ) ) ;
#9576=CARTESIAN_POINT ( 'NONE',  ( -2.390265326283148806, -4.391654775818394363, -1.249999997268814278 ) ) ;
#9581=ADVANCED_FACE ( 'NONE', ( #12449 ), #1386, .T. ) ;
#9582=CARTESIAN_POINT ( 'NONE',  ( 3.916244202832140253, -2.131511515620588160, 1.562500001365592972 ) ) ;
#9583=ORIENTED_EDGE ( 'NONE', *, *, #13822, .F. ) ;
#9594=CARTESIAN_POINT ( 'NONE',  ( -5.381735091635034607, 0.5711823568785950878, -1.562500000000000666 ) ) ;
#9595=CARTESIAN_POINT ( 'NONE',  ( 4.795541693661363958, 1.415196051561583790, -8.437499998634409692 ) ) ;
#9606=ORIENTED_EDGE ( 'NONE', *, *, #6863, .F. ) ;
#9608=AXIS2_PLACEMENT_3D ( 'NONE', #3447, #12163, #14527 ) ;
#9620=( LENGTH_UNIT ( ) NAMED_UNIT ( * ) SI_UNIT ( .MILLI., .METRE. ) );
#9627=CARTESIAN_POINT ( 'NONE',  ( -3.033343224707664376, 3.753672977998667726, 1.000000001365594082 ) ) ;
#9630=CARTESIAN_POINT ( 'NONE',  ( -4.799145180956616130, 0.5093500532425063732, -1.124999998634405918 ) ) ;
#9640=CARTESIAN_POINT ( 'NONE',  ( 3.753672977998667726, 3.033343224707664820, -3.499999998634409692 ) ) ;
#9641=( BOUNDED_CURVE ( )  B_SPLINE_CURVE ( 2, ( #13081, #3231, #3317, #15368, #4376, #13160, #8024, #8267, #8179, #11868, #9309 ),
 .UNSPECIFIED., .F., .F. ) 
 B_SPLINE_CURVE_WITH_KNOTS ( ( 3, 2, 2, 2, 2, 3 ),
 ( 0.4545872658012772849, 0.4625000000000000222, 0.4749999999999999778, 0.4874999999999999889, 0.5000000000000000000, 0.5045872658012773293 ),
 .UNSPECIFIED. ) 
 CURVE ( )  GEOMETRIC_REPRESENTATION_ITEM ( )  RATIONAL_B_SPLINE_CURVE ( ( 0.9646335149384808183, 0.9518143178943437865, 1.000000000000000000, 0.9238795325112867385, 1.000000000000000000, 0.9238795325112867385, 1.000000000000000000, 0.9238795325112867385, 1.000000000000000000, 0.9720652146169423968, 0.9646335149384803742 ) ) 
 REPRESENTATION_ITEM ( '' )  );
#9644=EDGE_CURVE ( 'NONE', #15708, #14775, #13753, .T. ) ;
#9646=CARTESIAN_POINT ( 'NONE',  ( -4.209348295687703079, -3.401574460001763445, -2.437500000000003109 ) ) ;
#9649=CARTESIAN_POINT ( 'NONE',  ( 5.381735091635035495, -0.5711823568785978633, 1.062500002731182613 ) ) ;
#9653=CARTESIAN_POINT ( 'NONE',  ( 3.916244202832140253, -2.131511515620588160, -5.437499998634406140 ) ) ;
#9669=CARTESIAN_POINT ( 'NONE',  ( -2.390265326283148806, -4.391654775818394363, -1.375000000000001332 ) ) ;
#9671=CARTESIAN_POINT ( 'NONE',  ( 3.187317364896726790, -3.801046099509943765, -0.03262248246693635195 ) ) ;
#9674=CARTESIAN_POINT ( 'NONE',  ( 4.799145180956616130, -0.5093500532425063732, -1.624999998634406362 ) ) ;
#9679=ORIENTED_EDGE ( 'NONE', *, *, #8343, .F. ) ;
#9687=CIRCLE ( 'NONE', #4789, 7.500000000000001776 ) ;
#9688=CARTESIAN_POINT ( 'NONE',  ( 2.602085213965210642E-15, 8.660254037844392627, -1.000000000000000888 ) ) ;
#9693=CIRCLE ( 'NONE', #2724, 10.12668159690567649 ) ;
#9694=CARTESIAN_POINT ( 'NONE',  ( -1.908195823574487804E-14, -8.660254037844392627, -1.000000000000000888 ) ) ;
#9696=CARTESIAN_POINT ( 'NONE',  ( -5.000000000000004441, -7.530481206757679743E-15, -1.420263044861758361 ) ) ;
#9702=SURFACE_SIDE_STYLE ('',( #23 ) ) ;
#9705=VECTOR ( 'NONE', #3136, 1000.000000000000000 ) ;
#9706=EDGE_LOOP ( 'NONE', ( #7431, #14282, #11154, #3103 ) ) ;
#9711=CARTESIAN_POINT ( 'NONE',  ( -2.131511515620587272, -3.916244202832140253, -1.687499998634406362 ) ) ;
#9714=CARTESIAN_POINT ( 'NONE',  ( -3.753672977998669946, -3.033343224707661712, 1.365593156898739876E-09 ) ) ;
#9716=CARTESIAN_POINT ( 'NONE',  ( 3.750000000000004441, -6.495190528383289141, 0.000000000000000000 ) ) ;
#9726=CARTESIAN_POINT ( 'NONE',  ( -3.033343224707664820, 3.753672977998667726, -1.249999998634407916 ) ) ;
#9734=CARTESIAN_POINT ( 'NONE',  ( 4.209348295687701302, 3.401574460001765665, 0.1875000027311836681 ) ) ;
#9737=CARTESIAN_POINT ( 'NONE',  ( 0.5093500532425063732, 4.799145180956616130, -5.124999998634405252 ) ) ;
#9744=( BOUNDED_CURVE ( )  B_SPLINE_CURVE ( 2, ( #532, #7806, #13999, #5369, #13842, #12698, #1641, #11344, #210, #5450, #2926 ),
 .UNSPECIFIED., .F., .T. ) 
 B_SPLINE_CURVE_WITH_KNOTS ( ( 3, 2, 2, 2, 2, 3 ),
 ( 0.6045872658012773071, 0.6125000000000000444, 0.6250000000000000000, 0.6374999999999999556, 0.6500000000000000222, 0.6545872658012773515 ),
 .UNSPECIFIED. ) 
 CURVE ( )  GEOMETRIC_REPRESENTATION_ITEM ( )  RATIONAL_B_SPLINE_CURVE ( ( 0.9646335149384808183, 0.9518143178943441196, 1.000000000000000000, 0.9238795325112867385, 1.000000000000000000, 0.9238795325112867385, 1.000000000000000000, 0.9238795325112867385, 1.000000000000000000, 0.9720652146169423968, 0.9646335149384803742 ) ) 
 REPRESENTATION_ITEM ( '' )  );
#9752=CARTESIAN_POINT ( 'NONE',  ( 7.500000000000000000, 4.330127018922190096, -9.999999999999998224 ) ) ;
#9754=CYLINDRICAL_SURFACE ( 'NONE', #15474, 5.000000000000000888 ) ;
#9755=CARTESIAN_POINT ( 'NONE',  ( 3.401574460001763001, -4.209348295687703967, -2.187500000000002665 ) ) ;
#9760=AXIS2_PLACEMENT_3D ( 'NONE', #6331, #11250, #197 ) ;
#9761=CARTESIAN_POINT ( 'NONE',  ( -2.131511515620587272, -3.916244202832140253, -0.9374999986344056957 ) ) ;
#9763=CARTESIAN_POINT ( 'NONE',  ( -7.500000000000001776, 0.000000000000000000, 0.000000000000000000 ) ) ;
#9793=FILL_AREA_STYLE ('',( #8749 ) ) ;
#9800=CARTESIAN_POINT ( 'NONE',  ( 3.033343224707661712, -3.753672977998669946, -2.499999998634408804 ) ) ;
#9802=CARTESIAN_POINT ( 'NONE',  ( 2.131511515620586383, 3.916244202832140253, -1.437499998634406140 ) ) ;
#9809=ORIENTED_EDGE ( 'NONE', *, *, #6093, .T. ) ;
#9811=CARTESIAN_POINT ( 'NONE',  ( 3.033343224707661712, -3.753672977998669502, -2.749999998634409248 ) ) ;
#9813=CARTESIAN_POINT ( 'NONE',  ( 3.033343224707661712, -3.753672977998669502, -7.499999998634409692 ) ) ;
#9817=CARTESIAN_POINT ( 'NONE',  ( 1.415196051561583790, -4.795541693661363958, -0.1249999972688167760 ) ) ;
#9819=PRESENTATION_STYLE_ASSIGNMENT (( #12223 ) ) ;
#9822=CARTESIAN_POINT ( 'NONE',  ( 3.753672977998667726, 3.033343224707664376, -4.249999998634406140 ) ) ;
#9829=DIRECTION ( 'NONE',  ( 0.000000000000000000, 0.000000000000000000, 1.000000000000000000 ) ) ;
#9835=CARTESIAN_POINT ( 'NONE',  ( 4.209348295687701302, 3.401574460001765665, -1.937500000000002442 ) ) ;
#9837=CARTESIAN_POINT ( 'NONE',  ( -4.257077077555639910, -2.071027201601217893, -0.1914352921446037803 ) ) ;
#9840=CARTESIAN_POINT ( 'NONE',  ( 4.799145180956616130, -0.5093500532425063732, -0.6249999986344092484 ) ) ;
#9844=ORIENTED_EDGE ( 'NONE', *, *, #14622, .F. ) ;
#9845=CARTESIAN_POINT ( 'NONE',  ( -7.922811899608412034, -4.628803996615322269, -8.057669882367653358 ) ) ;
#9854=DIRECTION ( 'NONE',  ( 0.8191520442889907994, 0.000000000000000000, 0.5735764363510474917 ) ) ;
#9857=DIRECTION ( 'NONE',  ( 0.000000000000000000, 0.000000000000000000, 1.000000000000000000 ) ) ;
#9868=B_SPLINE_CURVE_WITH_KNOTS ( 'NONE', 3,
 ( #11528, #3054, #7998, #7764, #9287, #7836 ),
 .UNSPECIFIED., .F., .F.,
 ( 4, 2, 4 ),
 ( -5.145455527303427788E-06, 0.0004153350442917243344, 0.0008358155441107501145 ),
 .UNSPECIFIED. ) ;
#9869=EDGE_CURVE ( 'NONE', #9381, #11190, #7803, .T. ) ;
#9874=CARTESIAN_POINT ( 'NONE',  ( -0.5093500532425060401, -4.799145180956616130, -2.624999998634407028 ) ) ;
#9876=CARTESIAN_POINT ( 'NONE',  ( -3.753672977998669946, -3.033343224707661712, -5.999999998634407916 ) ) ;
#9882=ORIENTED_EDGE ( 'NONE', *, *, #3082, .F. ) ;
#9884=CARTESIAN_POINT ( 'NONE',  ( 4.276409079477644148, 1.261996585732577891, -4.562499998634405252 ) ) ;
#9886=EDGE_CURVE ( 'NONE', #2474, #2543, #6955, .T. ) ;
#9887=FACE_OUTER_BOUND ( 'NONE', #14446, .T. ) ;
#9891=CARTESIAN_POINT ( 'NONE',  ( -2.390265326283148806, -4.391654775818394363, -0.2499999972688168870 ) ) ;
#9896=CARTESIAN_POINT ( 'NONE',  ( -2.131511515620587272, -3.916244202832140253, -2.687499998634407028 ) ) ;
#9910=CARTESIAN_POINT ( 'NONE',  ( -1.415196051561583790, 4.795541693661363958, 0.2499999999999967526 ) ) ;
#9914=CARTESIAN_POINT ( 'NONE',  ( -3.753672977998669946, -3.033343224707661712, -0.9999999986344076941 ) ) ;
#9915=ORIENTED_EDGE ( 'NONE', *, *, #3634, .T. ) ;
#9920=B_SPLINE_CURVE_WITH_KNOTS ( 'NONE', 3,
 ( #15338, #1901, #6847, #11912, #11754, #12890 ),
 .UNSPECIFIED., .F., .F.,
 ( 4, 2, 4 ),
 ( 2.475503369187537856E-07, 0.002222330217055623267, 0.004444412883774327173 ),
 .UNSPECIFIED. ) ;
#9927=CARTESIAN_POINT ( 'NONE',  ( 5.000000000000004441, -2.247904837838113790E-16, -6.920263044861760804 ) ) ;
#9941=ORIENTED_EDGE ( 'NONE', *, *, #5179, .T. ) ;
#9942=ADVANCED_FACE ( 'NONE', ( #12425 ), #7923, .F. ) ;
#9952=CARTESIAN_POINT ( 'NONE',  ( -1.261996585732579224, 4.276409079477648589, -4.062499998634405252 ) ) ;
#9955=CARTESIAN_POINT ( 'NONE',  ( -4.799145180956616130, 0.5093500532425063732, -4.124999998634405252 ) ) ;
#9958=EDGE_LOOP ( 'NONE', ( #11471, #12098, #13111, #578 ) ) ;
#9968=CARTESIAN_POINT ( 'NONE',  ( -1.261996585732579224, 4.276409079477648589, -2.312499998634407028 ) ) ;
#9976=CARTESIAN_POINT ( 'NONE',  ( -3.401574460001764777, 4.209348295687701302, -4.562499997268816720 ) ) ;
#9983=CARTESIAN_POINT ( 'NONE',  ( 3.916244202832140253, -2.131511515620588160, -4.437499998634405252 ) ) ;
#10001=CARTESIAN_POINT ( 'NONE',  ( -3.401574460001764777, 4.209348295687701302, -5.687500000000003553 ) ) ;
#10004=CARTESIAN_POINT ( 'NONE',  ( -3.916244202832140253, 2.131511515620587272, -3.187499998634407916 ) ) ;
#10018=DIRECTION ( 'NONE',  ( 0.000000000000000000, 0.000000000000000000, 1.000000000000000000 ) ) ;
#10022=CARTESIAN_POINT ( 'NONE',  ( -4.276409079477644148, -1.261996585732578335, -2.812499998634407472 ) ) ;
#10023=CARTESIAN_POINT ( 'NONE',  ( 4.339338055002142092, 1.058955340485046692, -0.3789984458506918119 ) ) ;
#10027=ADVANCED_FACE ( 'NONE', ( #567 ), #2002, .F. ) ;
#10040=ORIENTED_EDGE ( 'NONE', *, *, #7227, .F. ) ;
#10041=FACE_OUTER_BOUND ( 'NONE', #10173, .T. ) ;
#10046=AXIS2_PLACEMENT_3D ( 'NONE', #14790, #11081, #14634 ) ;
#10048=CARTESIAN_POINT ( 'NONE',  ( 4.276409079477644148, 1.261996585732577891, -6.562499998634407028 ) ) ;
#10059=CARTESIAN_POINT ( 'NONE',  ( -4.276409079477644148, -1.261996585732578335, -6.062499998634407028 ) ) ;
#10061=TOROIDAL_SURFACE ( 'NONE', #15224, 10.12668159690567649, 0.7733184030943209830 ) ;
#10062=CARTESIAN_POINT ( 'NONE',  ( -5.000000000000000888, 6.123233995736767268E-16, -25.03750572909317285 ) ) ;
#10067=CARTESIAN_POINT ( 'NONE',  ( -4.391654775818395251, 2.390265326283148806, -4.499999997268817609 ) ) ;
#10069=CARTESIAN_POINT ( 'NONE',  ( -2.104132545462253034, 4.020150199444661787, -0.3258662981471979747 ) ) ;
#10085=CARTESIAN_POINT ( 'NONE',  ( -1.060314165522904917, -8.048081368953686976, -7.659344964963222147 ) ) ;
#10088=CARTESIAN_POINT ( 'NONE',  ( -1.415196051561583790, 4.795541693661363958, -6.750000000000002665 ) ) ;
#10092=CARTESIAN_POINT ( 'NONE',  ( -3.916244202832140253, 2.131511515620587272, -7.187499998634407916 ) ) ;
#10100=CARTESIAN_POINT ( 'NONE',  ( -8.673617379884035472E-16, -9.147862274876560562, -8.047472243342939535 ) ) ;
#10101=CARTESIAN_POINT ( 'NONE',  ( 1.261996585732578113, -4.276409079477644148, -1.562499998634406140 ) ) ;
#10103=EDGE_CURVE ( 'NONE', #14425, #6438, #6882, .T. ) ;
#10105=CARTESIAN_POINT ( 'NONE',  ( -3.750000000000000000, -6.495190528383298023, -6.991905250253757309 ) ) ;
#10111=B_SPLINE_CURVE_WITH_KNOTS ( 'NONE', 3,
 ( #9716, #7150, #7071, #7304, #8448, #11892 ),
 .UNSPECIFIED., .F., .F.,
 ( 4, 2, 4 ),
 ( 0.004444412883774327173, 0.006655097293744434601, 0.008865781703714541162 ),
 .UNSPECIFIED. ) ;
#10123=CARTESIAN_POINT ( 'NONE',  ( -1.261996585732579224, 4.276409079477648589, -7.312499998634407916 ) ) ;
#10127=FACE_OUTER_BOUND ( 'NONE', #10668, .T. ) ;
#10133=CARTESIAN_POINT ( 'NONE',  ( -3.033343224707664820, 3.753672977998667726, -7.249999998634409692 ) ) ;
#10134=EDGE_CURVE ( 'NONE', #3959, #9532, #6551, .T. ) ;
#10143=CARTESIAN_POINT ( 'NONE',  ( 0.5711823568785989735, 5.381735091635026613, -2.687499997268816720 ) ) ;
#10149=CARTESIAN_POINT ( 'NONE',  ( 1.261996585732578113, -4.276409079477644148, -6.562499998634407028 ) ) ;
#10156=EDGE_CURVE ( 'NONE', #7077, #2517, #9641, .T. ) ;
#10158=EDGE_CURVE ( 'NONE', #7075, #4036, #814, .T. ) ;
#10160=CARTESIAN_POINT ( 'NONE',  ( 4.631580223510930239, 1.444531747605005878E-11, -0.2579703047231843294 ) ) ;
#10161=CARTESIAN_POINT ( 'NONE',  ( -0.6169862416622959866, -8.783631307151361867, -7.913704048099982735 ) ) ;
#10164=CARTESIAN_POINT ( 'NONE',  ( 1.415196051561583790, -4.795541693661363958, -7.250000000000002665 ) ) ;
#10165=CARTESIAN_POINT ( 'NONE',  ( 5.000000000000004441, -2.247904837838113790E-16, -3.045263047592945860 ) ) ;
#10166=FACE_OUTER_BOUND ( 'NONE', #4847, .T. ) ;
#10168=CARTESIAN_POINT ( 'NONE',  ( 3.753672977998667726, 3.033343224707664376, -6.499999998634407916 ) ) ;
#10170=CARTESIAN_POINT ( 'NONE',  ( 7.500000000000000000, 4.330127018922190096, -7.422398894150031623 ) ) ;
#10173=EDGE_LOOP ( 'NONE', ( #1972, #15450, #1733, #906 ) ) ;
#10183=CARTESIAN_POINT ( 'NONE',  ( 3.033343224707661712, -3.753672977998669502, -2.499999998634408804 ) ) ;
#10197=ADVANCED_FACE ( 'NONE', ( #4289 ), #12852, .F. ) ;
#10203=CARTESIAN_POINT ( 'NONE',  ( 5.000000000000004441, 6.350331166892669572E-15, -1.920263044861758583 ) ) ;
#10208=CARTESIAN_POINT ( 'NONE',  ( 0.5093500532425063732, 4.799145180956616130, -6.374999998634407028 ) ) ;
#10219=CARTESIAN_POINT ( 'NONE',  ( -2.131511515620587272, -3.916244202832140253, -6.937499998634407916 ) ) ;
#10226=CARTESIAN_POINT ( 'NONE',  ( 1.415196051561583790, -4.795541693661363958, -5.124999997268817609 ) ) ;
#10232=ORIENTED_EDGE ( 'NONE', *, *, #6700, .T. ) ;
#10234=CARTESIAN_POINT ( 'NONE',  ( -3.753672977998669946, -3.033343224707661712, -7.749999998634409692 ) ) ;
#10236=ORIENTED_EDGE ( 'NONE', *, *, #1363, .F. ) ;
#10248=CARTESIAN_POINT ( 'NONE',  ( 0.5711823568785989735, 5.381735091635026613, -5.812500000000000000 ) ) ;
#10252=EDGE_CURVE ( 'NONE', #7219, #5402, #8569, .T. ) ;
#10256=CARTESIAN_POINT ( 'NONE',  ( -3.033343224707664376, 3.753672977998667726, -8.249999998634409692 ) ) ;
#10269=CARTESIAN_POINT ( 'NONE',  ( -2.131511515620587272, -3.916244202832140253, -2.687499998634407028 ) ) ;
#10270=CARTESIAN_POINT ( 'NONE',  ( 3.688361877192762428, 2.519395953540043198, -0.3789984458506766574 ) ) ;
#10272=CARTESIAN_POINT ( 'NONE',  ( 3.033343224707661712, -3.753672977998669946, -3.499999998634410137 ) ) ;
#10281=VERTEX_POINT ( 'NONE', #15686 ) ;
#10286=( BOUNDED_CURVE ( )  B_SPLINE_CURVE ( 2, ( #1052, #14715, #2489, #5986, #10911, #12269, #1210, #3710, #15852, #4771, #9696 ),
 .UNSPECIFIED., .F., .F. ) 
 B_SPLINE_CURVE_WITH_KNOTS ( ( 3, 2, 2, 2, 2, 3 ),
 ( 0.2045872658012772849, 0.2124999999999999944, 0.2250000000000000056, 0.2374999999999999889, 0.2500000000000000000, 0.2545872658012772738 ),
 .UNSPECIFIED. ) 
 CURVE ( )  GEOMETRIC_REPRESENTATION_ITEM ( )  RATIONAL_B_SPLINE_CURVE ( ( 0.9646335149384808183, 0.9518143178943438976, 1.000000000000000000, 0.9238795325112867385, 1.000000000000000000, 0.9238795325112867385, 1.000000000000000000, 0.9238795325112867385, 1.000000000000000000, 0.9720652146169430630, 0.9646335149384808183 ) ) 
 REPRESENTATION_ITEM ( '' )  );
#10290=CARTESIAN_POINT ( 'NONE',  ( -3.401574460001765221, 4.209348295687701302, -1.562499997268814056 ) ) ;
#10303=CARTESIAN_POINT ( 'NONE',  ( -4.795541693661363958, -1.415196051561583790, -1.500000000000001332 ) ) ;
#10307=CARTESIAN_POINT ( 'NONE',  ( 2.131511515620586383, 3.916244202832140253, -6.437499998634407028 ) ) ;
#10312=CARTESIAN_POINT ( 'NONE',  ( -4.209348295687703079, -3.401574460001763445, -8.312499997268812280 ) ) ;
#10314=EDGE_CURVE ( 'NONE', #8373, #2474, #2296, .T. ) ;
#10315=CARTESIAN_POINT ( 'NONE',  ( 4.391654775818395251, -2.390265326283149694, -7.999999997268813168 ) ) ;
#10316=CARTESIAN_POINT ( 'NONE',  ( -5.000000000000002665, -1.404940523648820476E-14, -8.420263044861757251 ) ) ;
#10327=CARTESIAN_POINT ( 'NONE',  ( -2.623433461001182465, 7.604994000793860565, -7.633824513837113912 ) ) ;
#10330=CARTESIAN_POINT ( 'NONE',  ( 3.401574460001763445, -4.209348295687703079, -5.187500000000000888 ) ) ;
#10331=CARTESIAN_POINT ( 'NONE',  ( -6.523606932383977153, -4.893847819345195305, -7.213065638942927293 ) ) ;
#10333=CARTESIAN_POINT ( 'NONE',  ( -3.401574460001764777, 4.209348295687701302, -6.687500000000003553 ) ) ;
#10337=CARTESIAN_POINT ( 'NONE',  ( 1.261996585732578113, -4.276409079477644148, -5.812499998634406140 ) ) ;
#10339=CARTESIAN_POINT ( 'NONE',  ( 7.703928834700302986, -4.447865386531949738, -7.917997657324739258 ) ) ;
#10348=CARTESIAN_POINT ( 'NONE',  ( -3.753672977998669502, -3.033343224707661712, -2.749999998634409248 ) ) ;
#10351=CARTESIAN_POINT ( 'NONE',  ( -4.276409079477644148, -1.261996585732578335, -2.812499998634407472 ) ) ;
#10352=CARTESIAN_POINT ( 'NONE',  ( -6.874999999999999112, -4.690970937165712229, -7.298562697733106397 ) ) ;
#10370=CARTESIAN_POINT ( 'NONE',  ( -1.261996585732579224, 4.276409079477648589, -8.312499998634407916 ) ) ;
#10371=CARTESIAN_POINT ( 'NONE',  ( 3.753672977998667726, 3.033343224707664376, 0.5000000013655936382 ) ) ;
#10372=ORIENTED_EDGE ( 'NONE', *, *, #1363, .T. ) ;
#10383=CARTESIAN_POINT ( 'NONE',  ( 4.795541693661363958, 1.415196051561583790, -6.874999997268815832 ) ) ;
#10386=VERTEX_POINT ( 'NONE', #1814 ) ;
#10387=PLANE ( 'NONE',  #3318 ) ;
#10388=CARTESIAN_POINT ( 'NONE',  ( 4.276409079477644148, 1.261996585732577891, -7.312499998634407916 ) ) ;
#10391=DIRECTION ( 'NONE',  ( 1.000000000000000000, 0.000000000000000000, 0.000000000000000000 ) ) ;
#10393=ORIENTED_EDGE ( 'NONE', *, *, #9869, .T. ) ;
#10394=CARTESIAN_POINT ( 'NONE',  ( 3.401574460001763445, -4.209348295687703079, -0.1875000000000048572 ) ) ;
#10404=CARTESIAN_POINT ( 'NONE',  ( 4.795541693661363958, 1.415196051561583790, -8.000000000000003553 ) ) ;
#10406=CARTESIAN_POINT ( 'NONE',  ( 3.916244202832140253, -2.131511515620588160, -7.687499998634407916 ) ) ;
#10419=CARTESIAN_POINT ( 'NONE',  ( -4.799145180956616130, 0.5093500532425063732, -3.874999998634404363 ) ) ;
#10422=CARTESIAN_POINT ( 'NONE',  ( 4.799145180956616130, -0.5093500532425063732, -7.374999998634408804 ) ) ;
#10429=CARTESIAN_POINT ( 'NONE',  ( 2.352174619734370697, -7.302225387959956571, -7.450218641349208859 ) ) ;
#10438=CARTESIAN_POINT ( 'NONE',  ( 0.5711823568785988625, 5.381735091635026613, -1.687499997268816054 ) ) ;
#10441=CARTESIAN_POINT ( 'NONE',  ( -5.000000000000004441, -7.530481206757679743E-15, -1.420263044861758361 ) ) ;
#10445=CARTESIAN_POINT ( 'NONE',  ( 1.250000000000000444, -7.938566201357367902, -7.198902722707432034 ) ) ;
#10446=CARTESIAN_POINT ( 'NONE',  ( -4.276409079477644148, -1.261996585732578335, -0.06249999863440838799 ) ) ;
#10448=VERTEX_POINT ( 'NONE', #7515 ) ;
#10456=CARTESIAN_POINT ( 'NONE',  ( 5.000000000000093259, 0.7223674278660628945, -5.021799365517154001 ) ) ;
#10460=VECTOR ( 'NONE', #3569, 1000.000000000000000 ) ;
#10461=CARTESIAN_POINT ( 'NONE',  ( -1.415196051561583790, 4.795541693661363958, -8.624999997268814056 ) ) ;
#10463=CARTESIAN_POINT ( 'NONE',  ( -4.391654775818395251, 2.390265326283148806, -1.625000000000001332 ) ) ;
#10468=CARTESIAN_POINT ( 'NONE',  ( 7.500000000000002665, 3.639598441879749124, -0.7155132341745285007 ) ) ;
#10469=CARTESIAN_POINT ( 'NONE',  ( -7.549004593702457022, 4.358419834287859729, -7.700121441565834779 ) ) ;
#10479=VECTOR ( 'NONE', #5506, 1000.000000000000000 ) ;
#10482=CARTESIAN_POINT ( 'NONE',  ( 7.500000000000000000, 4.330127018922190096, -7.422398894150031623 ) ) ;
#10492=CARTESIAN_POINT ( 'NONE',  ( 3.033343224707661712, -3.753672977998669946, -0.4999999986344072500 ) ) ;
#10505=CARTESIAN_POINT ( 'NONE',  ( 7.500000000000000000, -3.202733125952097915, -7.213074474937297254 ) ) ;
#10506=CARTESIAN_POINT ( 'NONE',  ( 4.276409079477644148, 1.261996585732577891, -4.312499998634405252 ) ) ;
#10507=CARTESIAN_POINT ( 'NONE',  ( 5.000000000000093259, 0.7223674278660628945, -5.896799362785968945 ) ) ;
#10511=CARTESIAN_POINT ( 'NONE',  ( -3.033343224707664376, 3.753672977998667726, -6.999999998634408804 ) ) ;
#10521=CARTESIAN_POINT ( 'NONE',  ( 7.500000000000000888, -0.7512838658081425480, 1.521271173268723212E-15 ) ) ;
#10523=CARTESIAN_POINT ( 'NONE',  ( -3.916244202832140253, 2.131511515620587272, -2.937499998634407472 ) ) ;
#10530=CARTESIAN_POINT ( 'NONE',  ( 4.999999999999848121, -1.272547481429015859, -4.086597482644646284 ) ) ;
#10532=CARTESIAN_POINT ( 'NONE',  ( 0.5711823568785988625, 5.381735091635026613, -7.687499997268817609 ) ) ;
#10533=CARTESIAN_POINT ( 'NONE',  ( -7.500000000000005329, 4.330127018922194537, -0.9999999999999974465 ) ) ;
#10536=VECTOR ( 'NONE', #2979, 1000.000000000000000 ) ;
#10543=CIRCLE ( 'NONE', #3062, 5.000000000000000888 ) ;
#10549=DIRECTION ( 'NONE',  ( 0.000000000000000000, 0.000000000000000000, 1.000000000000000000 ) ) ;
#10552=CARTESIAN_POINT ( 'NONE',  ( 0.5711823568785989735, 5.381735091635026613, -8.687499997268814056 ) ) ;
#10559=AXIS2_PLACEMENT_3D ( 'NONE', #11964, #10776, #4629 ) ;
#10570=EDGE_CURVE ( 'NONE', #12914, #11431, #6832, .T. ) ;
#10575=CARTESIAN_POINT ( 'NONE',  ( -7.500000000000001776, -4.330127018922197202, -7.564335161054499324 ) ) ;
#10580=CARTESIAN_POINT ( 'NONE',  ( 0.5093500532425063732, 4.799145180956616130, -1.124999998634405918 ) ) ;
#10584=ORIENTED_EDGE ( 'NONE', *, *, #12912, .F. ) ;
#10587=B_SPLINE_CURVE_WITH_KNOTS ( 'NONE', 3,
 ( #3245, #13008, #10445, #1946, #4214, #12686, #6894, #5677, #9242 ),
 .UNSPECIFIED., .F., .F.,
 ( 4, 2, 1, 2, 4 ),
 ( 0.000000000000000000, 0.002165063509461099666, 0.004330127018922197597, 0.006495190528383295095, 0.008660254037844393460 ),
 .UNSPECIFIED. ) ;
#10593=CARTESIAN_POINT ( 'NONE',  ( 3.916244202832140253, -2.131511515620588160, -4.437499998634405252 ) ) ;
#10596=CARTESIAN_POINT ( 'NONE',  ( 4.795541693661363958, 1.415196051561583790, 1.999999999999998224 ) ) ;
#10602=CARTESIAN_POINT ( 'NONE',  ( 6.439685834476867932, -4.942299687812352182, -7.659344964962495617 ) ) ;
#10605=CARTESIAN_POINT ( 'NONE',  ( -5.000000000000000888, 6.123233995736767268E-16, -25.03750572909317285 ) ) ;
#10615=CARTESIAN_POINT ( 'NONE',  ( 3.753672977998667726, 3.033343224707664376, -0.4999999986344072500 ) ) ;
#10618=CARTESIAN_POINT ( 'NONE',  ( -1.249327701956659542, 8.410337540185347294, -7.776713651266385696 ) ) ;
#10623=B_SPLINE_CURVE_WITH_KNOTS ( 'NONE', 3,
 ( #7974, #12877, #1812, #9102, #14103, #11356 ),
 .UNSPECIFIED., .F., .F.,
 ( 4, 2, 4 ),
 ( 0.004444412883774352327, 0.006655097293744444142, 0.008865781703714535958 ),
 .UNSPECIFIED. ) ;
#10624=CARTESIAN_POINT ( 'NONE',  ( 5.381735091635035495, -0.5711823568785978633, -7.937499997268813168 ) ) ;
#10626=CARTESIAN_POINT ( 'NONE',  ( 2.602085213965210642E-15, 8.660254037844392627, -9.999999999999998224 ) ) ;
#10628=CARTESIAN_POINT ( 'NONE',  ( 7.500000000000000888, 4.330127018922199866, -1.000000000000000888 ) ) ;
#10629=CARTESIAN_POINT ( 'NONE',  ( 2.602085213965210642E-15, 8.660254037844392627, -9.999999999999998224 ) ) ;
#10636=CARTESIAN_POINT ( 'NONE',  ( 3.916244202832140253, -2.131511515620588160, -0.6874999986344089153 ) ) ;
#10640=CARTESIAN_POINT ( 'NONE',  ( -2.390265326283148806, -4.391654775818394363, -5.375000000000000888 ) ) ;
#10642=CARTESIAN_POINT ( 'NONE',  ( 4.446142487674360488, -0.3868705316447643150, -0.3789984458506777676 ) ) ;
#10646=CARTESIAN_POINT ( 'NONE',  ( -3.916244202832140253, 2.131511515620587272, -1.937499998634406584 ) ) ;
#10648=CARTESIAN_POINT ( 'NONE',  ( 7.777900015783946408, 4.169681370001526943, -7.928862157988302073 ) ) ;
#10657=CARTESIAN_POINT ( 'NONE',  ( -1.261996585732579224, 4.276409079477648589, -5.062499998634406140 ) ) ;
#10660=CARTESIAN_POINT ( 'NONE',  ( 0.5093500532425063732, 4.799145180956616130, -8.124999998634409692 ) ) ;
#10668=EDGE_LOOP ( 'NONE', ( #4379, #2312, #13206, #12132 ) ) ;
#10676=DIRECTION ( 'NONE',  ( 1.000000000000000000, 0.000000000000000000, 0.000000000000000000 ) ) ;
#10695=CARTESIAN_POINT ( 'NONE',  ( -3.916244202832140253, 2.131511515620587272, 1.062500001365592528 ) ) ;
#10697=CARTESIAN_POINT ( 'NONE',  ( 1.261996585732578113, -4.276409079477644148, -2.812499998634407472 ) ) ;
#10698=CARTESIAN_POINT ( 'NONE',  ( -4.391654775818395251, 2.390265326283148806, -0.6250000000000005551 ) ) ;
#10701=DIRECTION ( 'NONE',  ( 0.5000000000000004441, -0.8660254037844383745, 0.000000000000000000 ) ) ;
#10702=CARTESIAN_POINT ( 'NONE',  ( 5.000000000000004441, -2.247904837838113790E-16, -2.920263044861759472 ) ) ;
#10703=EDGE_CURVE ( 'NONE', #15838, #7550, #6458, .T. ) ;
#10710=CARTESIAN_POINT ( 'NONE',  ( 0.5789871446316211534, 4.420982230657665824, -0.3789984458506777676 ) ) ;
#10720=CARTESIAN_POINT ( 'NONE',  ( -4.795541693661363958, -1.415196051561583790, -7.500000000000003553 ) ) ;
#10723=CARTESIAN_POINT ( 'NONE',  ( -4.799145180956616130, 0.5093500532425063732, 1.125000001365592306 ) ) ;
#10725=DIRECTION ( 'NONE',  ( -1.000000000000000000, 0.000000000000000000, 0.000000000000000000 ) ) ;
#10734=CARTESIAN_POINT ( 'NONE',  ( -3.753672977998669502, -3.033343224707661712, -4.749999998634407028 ) ) ;
#10738=AXIS2_PLACEMENT_3D ( 'NONE', #13367, #9359, #10725 ) ;
#10739=CARTESIAN_POINT ( 'NONE',  ( 1.415196051561583790, -4.795541693661363958, 0.7499999999999972244 ) ) ;
#10741=CARTESIAN_POINT ( 'NONE',  ( 0.000000000000000000, 0.000000000000000000, 0.000000000000000000 ) ) ;
#10751=CARTESIAN_POINT ( 'NONE',  ( -5.000000000000000888, 6.123233995736767268E-16, -25.03750572909317285 ) ) ;
#10769=CARTESIAN_POINT ( 'NONE',  ( -2.325424218458715053, 7.317669739337203438, -7.030005583190798824 ) ) ;
#10771=B_SPLINE_CURVE_WITH_KNOTS ( 'NONE', 3,
 ( #9490, #11588, #14101, #13029 ),
 .UNSPECIFIED., .F., .F.,
 ( 4, 4 ),
 ( 0.001452767664617488205, 0.002080905508140416978 ),
 .UNSPECIFIED. ) ;
#10776=DIRECTION ( 'NONE',  ( 1.224646799147353207E-16, 1.000000000000000000, -0.000000000000000000 ) ) ;
#10777=CARTESIAN_POINT ( 'NONE',  ( -3.753672977998669946, -3.033343224707661712, -0.7499999986344074721 ) ) ;
#10779=CARTESIAN_POINT ( 'NONE',  ( -1.261996585732579224, 4.276409079477648589, -1.312499998634406140 ) ) ;
#10793=AXIS2_PLACEMENT_3D ( 'NONE', #11989, #8385, #3363 ) ;
#10800=CYLINDRICAL_SURFACE ( 'NONE', #4584, 5.000000000000000888 ) ;
#10803=CARTESIAN_POINT ( 'NONE',  ( 4.276409079477644148, 1.261996585732577891, 1.687500001365593194 ) ) ;
#10805=CARTESIAN_POINT ( 'NONE',  ( -0.3483149870578519658, 8.861353789385018942, -7.493854785173811983 ) ) ;
#10814=FACE_OUTER_BOUND ( 'NONE', #7784, .T. ) ;
#10818=FACE_OUTER_BOUND ( 'NONE', #12017, .T. ) ;
#10819=CARTESIAN_POINT ( 'NONE',  ( -4.795541693661363958, -1.415196051561583790, -2.500000000000002220 ) ) ;
#10820=LINE ( 'NONE', #9595, #12738 ) ;
#10821=CARTESIAN_POINT ( 'NONE',  ( -0.03800824613358327192, -4.872903691120612280, -0.09399265280457684557 ) ) ;
#10830=ORIENTED_EDGE ( 'NONE', *, *, #10845, .F. ) ;
#10839=CARTESIAN_POINT ( 'NONE',  ( -5.000000000000004441, -1.011557177027151181E-15, -5.545263047592944972 ) ) ;
#10845=EDGE_CURVE ( 'NONE', #5764, #7493, #15757, .T. ) ;
#10849=CARTESIAN_POINT ( 'NONE',  ( 4.799145180956616130, -0.5093500532425063732, -1.374999998634406140 ) ) ;
#10851=CARTESIAN_POINT ( 'NONE',  ( 0.5093500532425063732, 4.799145180956616130, -0.3749999986344090264 ) ) ;
#10863=CARTESIAN_POINT ( 'NONE',  ( 3.753672977998667726, 3.033343224707664820, -1.499999998634408138 ) ) ;
#10865=CARTESIAN_POINT ( 'NONE',  ( 7.500000000000000000, 4.330127018922190096, -9.999999999999998224 ) ) ;
#10868=CARTESIAN_POINT ( 'NONE',  ( -4.391654775818395251, 2.390265326283148806, -0.4999999972688171090 ) ) ;
#10872=CARTESIAN_POINT ( 'NONE',  ( -3.033343224707664376, 3.753672977998667726, -4.999999998634407028 ) ) ;
#10873=ORIENTED_EDGE ( 'NONE', *, *, #10252, .T. ) ;
#10874=CARTESIAN_POINT ( 'NONE',  ( 1.013163106017221704, 8.075304045852348622, -7.231838333420562037 ) ) ;
#10878=( BOUNDED_CURVE ( )  B_SPLINE_CURVE ( 2, ( #5352, #13981, #1549, #10290, #6487, #10438, #12760, #11401, #14070, #5264, #10203 ),
 .UNSPECIFIED., .F., .F. ) 
 B_SPLINE_CURVE_WITH_KNOTS ( ( 3, 2, 2, 2, 2, 3 ),
 ( 0.2545872658012772738, 0.2625000000000000111, 0.2750000000000000222, 0.2874999999999999778, 0.2999999999999999889, 0.3045872658012772627 ),
 .UNSPECIFIED. ) 
 CURVE ( )  GEOMETRIC_REPRESENTATION_ITEM ( )  RATIONAL_B_SPLINE_CURVE ( ( 0.9646335149384808183, 0.9518143178943437865, 1.000000000000000000, 0.9238795325112867385, 1.000000000000000000, 0.9238795325112867385, 1.000000000000000000, 0.9238795325112867385, 1.000000000000000000, 0.9720652146169430630, 0.9646335149384808183 ) ) 
 REPRESENTATION_ITEM ( '' )  );
#10888=CARTESIAN_POINT ( 'NONE',  ( -3.401574460001764777, 4.209348295687701302, -0.6875000000000016653 ) ) ;
#10889=CARTESIAN_POINT ( 'NONE',  ( -5.000000000000004441, -1.011557177027151181E-15, -3.545263047592942307 ) ) ;
#10892=CARTESIAN_POINT ( 'NONE',  ( 2.131511515620586383, 3.916244202832140253, 0.5625000013655921949 ) ) ;
#10896=B_SPLINE_CURVE_WITH_KNOTS ( 'NONE', 3,
 ( #547, #5464, #12476, #1415, #309, #4083, #10327, #9036, #15252, #230 ),
 .UNSPECIFIED., .F., .F.,
 ( 4, 2, 2, 2, 4 ),
 ( 0.000000000000000000, 0.002305503304226492935, 0.004611006608452985871, 0.006916509912679479240, 0.009222013216905970007 ),
 .UNSPECIFIED. ) ;
#10898=CARTESIAN_POINT ( 'NONE',  ( -7.500000000000003553, -4.732323933430408580, -7.493854309896105015 ) ) ;
#10907=CARTESIAN_POINT ( 'NONE',  ( 4.174999999999999822, 0.000000000000000000, -0.5776712190230133270 ) ) ;
#10911=CARTESIAN_POINT ( 'NONE',  ( 1.415196051561583790, -4.795541693661363958, -1.124999997268814278 ) ) ;
#10913=CARTESIAN_POINT ( 'NONE',  ( 7.263825692932296185, 4.945657111639574666, -7.907570769506047981 ) ) ;
#10920=LINE ( 'NONE', #8751, #6345 ) ;
#10925=CARTESIAN_POINT ( 'NONE',  ( -0.5093500532425060401, -4.799145180956616130, -1.624999998634406362 ) ) ;
#10926=ADVANCED_FACE ( 'NONE', ( #910 ), #14708, .F. ) ;
#10929=CARTESIAN_POINT ( 'NONE',  ( 3.753672977998667726, 3.033343224707664376, -2.499999998634408804 ) ) ;
#10934=DIRECTION ( 'NONE',  ( 0.000000000000000000, 0.000000000000000000, -1.000000000000000000 ) ) ;
#10940=CARTESIAN_POINT ( 'NONE',  ( -2.131511515620587272, -3.916244202832140253, -4.937499998634406140 ) ) ;
#10942=CARTESIAN_POINT ( 'NONE',  ( 0.5093500532425063732, 4.799145180956616130, -8.124999998634407916 ) ) ;
#10944=DIRECTION ( 'NONE',  ( 0.8660254037844381525, -0.5000000000000007772, 0.000000000000000000 ) ) ;
#10945=ADVANCED_FACE ( 'NONE', ( #1870 ), #10061, .T. ) ;
#10948=CARTESIAN_POINT ( 'NONE',  ( -1.415196051561583790, 4.795541693661363958, 0.3750000027311836681 ) ) ;
#10951=VECTOR ( 'NONE', #10018, 1000.000000000000000 ) ;
#10952=CARTESIAN_POINT ( 'NONE',  ( 3.033343224707661712, -3.753672977998669946, -4.499999998634407028 ) ) ;
#10960=B_SPLINE_CURVE_WITH_KNOTS ( 'NONE', 3,
 ( #6193, #14508, #1085, #15889, #3430, #6024 ),
 .UNSPECIFIED., .F., .F.,
 ( 4, 2, 4 ),
 ( 0.000000000000000000, 0.0004189869898914128608, 0.0008379739797828257217 ),
 .UNSPECIFIED. ) ;
#10968=CARTESIAN_POINT ( 'NONE',  ( 3.401574460001763001, -4.209348295687703967, -3.187500000000003553 ) ) ;
#10974=CARTESIAN_POINT ( 'NONE',  ( -2.131511515620587272, -3.916244202832140253, -2.937499998634407472 ) ) ;
#10989=CARTESIAN_POINT ( 'NONE',  ( 5.000000000000004441, 3.034671531081452754E-15, -0.9202630448617579173 ) ) ;
#10997=CARTESIAN_POINT ( 'NONE',  ( 5.000000000000002665, 1.275685995473128912E-14, -5.920263044861758139 ) ) ;
#10998=CARTESIAN_POINT ( 'NONE',  ( 5.000000000000004441, -2.247904837838113790E-16, -7.045263047592947636 ) ) ;
#11008=DIRECTION ( 'NONE',  ( 0.000000000000000000, 0.000000000000000000, 1.000000000000000000 ) ) ;
#11010=CARTESIAN_POINT ( 'NONE',  ( 5.000000000000000888, 0.000000000000000000, -25.03750572909317285 ) ) ;
#11011=CARTESIAN_POINT ( 'NONE',  ( 0.5093500532425063732, 4.799145180956616130, 0.8750000013655920839 ) ) ;
#11014=CARTESIAN_POINT ( 'NONE',  ( -3.033343224707664376, 3.753672977998667726, -3.249999998634409692 ) ) ;
#11023=ORIENTED_EDGE ( 'NONE', *, *, #5359, .T. ) ;
#11024=CARTESIAN_POINT ( 'NONE',  ( -2.131511515620587272, -3.916244202832140253, -2.937499998634407472 ) ) ;
#11034=FACE_OUTER_BOUND ( 'NONE', #4350, .T. ) ;
#11038=CARTESIAN_POINT ( 'NONE',  ( -2.131511515620587272, -3.916244202832140253, -4.687499998634405252 ) ) ;
#11042=ORIENTED_EDGE ( 'NONE', *, *, #9886, .F. ) ;
#11048=EDGE_CURVE ( 'NONE', #3061, #11169, #10920, .T. ) ;
#11055=CARTESIAN_POINT ( 'NONE',  ( 1.415196051561583790, -4.795541693661363958, -3.250000000000002665 ) ) ;
#11056=CARTESIAN_POINT ( 'NONE',  ( 4.999999999999849898, -1.272547481429010530, -1.961597479913463449 ) ) ;
#11057=STYLED_ITEM ( 'NONE', ( #9819 ), #9140 ) ;
#11061=CARTESIAN_POINT ( 'NONE',  ( 4.799145180956616130, -0.5093500532425063732, -3.624999998634407916 ) ) ;
#11062=ORIENTED_EDGE ( 'NONE', *, *, #11048, .T. ) ;
#11066=CARTESIAN_POINT ( 'NONE',  ( -7.915341292091955694, -3.857523022641926591, -7.913710289177963375 ) ) ;
#11071=ORIENTED_EDGE ( 'NONE', *, *, #3634, .F. ) ;
#11081=DIRECTION ( 'NONE',  ( 0.000000000000000000, 0.000000000000000000, 1.000000000000000000 ) ) ;
#11090=ORIENTED_EDGE ( 'NONE', *, *, #10156, .T. ) ;
#11093=CARTESIAN_POINT ( 'NONE',  ( -3.916244202832140253, 2.131511515620587272, -2.937499998634407472 ) ) ;
#11094=PRODUCT_CONTEXT ( 'NONE', #9192, 'mechanical' ) ;
#11095=CARTESIAN_POINT ( 'NONE',  ( 4.799145180956616130, -0.5093500532425063732, -3.624999998634407916 ) ) ;
#11096=DIRECTION ( 'NONE',  ( 1.000000000000000000, 0.000000000000000000, 0.000000000000000000 ) ) ;
#11104=CARTESIAN_POINT ( 'NONE',  ( 2.131511515620586383, 3.916244202832140253, -2.437499998634407028 ) ) ;
#11107=CARTESIAN_POINT ( 'NONE',  ( -1.206569728928479579, -7.963640680051486953, -0.4524126574264535905 ) ) ;
#11108=FACE_OUTER_BOUND ( 'NONE', #219, .T. ) ;
#11109=CARTESIAN_POINT ( 'NONE',  ( -4.391654775818395251, 2.390265326283148806, 0.5000000027311837236 ) ) ;
#11115=CARTESIAN_POINT ( 'NONE',  ( 4.276409079477644148, 1.261996585732577891, -4.312499998634405252 ) ) ;
#11123=PLANE ( 'NONE',  #6903 ) ;
#11126=CARTESIAN_POINT ( 'NONE',  ( -3.401574460001764777, 4.209348295687701302, 0.3124999999999955591 ) ) ;
#11129=CARTESIAN_POINT ( 'NONE',  ( -2.319649502132982821, -4.215050057573432873, -0.1373479633058615201 ) ) ;
#11132=CARTESIAN_POINT ( 'NONE',  ( 3.033343224707661712, -3.753672977998669946, -1.749999998634408360 ) ) ;
#11134=CARTESIAN_POINT ( 'NONE',  ( 3.750000000000005773, 6.495190528383288253, 0.000000000000000000 ) ) ;
#11142=CARTESIAN_POINT ( 'NONE',  ( 1.305263714129178299, -8.377797850839291627, -7.792447862505336609 ) ) ;
#11146=CARTESIAN_POINT ( 'NONE',  ( 10.12668159690567649, 0.000000000000000000, -9.999999999999998224 ) ) ;
#11151=CARTESIAN_POINT ( 'NONE',  ( 0.6508621380849223259, 8.763657152406455708, -7.907633014911222169 ) ) ;
#11154=ORIENTED_EDGE ( 'NONE', *, *, #14294, .T. ) ;
#11158=DIRECTION ( 'NONE',  ( 1.000000000000000000, 0.000000000000000000, 0.000000000000000000 ) ) ;
#11161=CARTESIAN_POINT ( 'NONE',  ( 4.276409079477644148, 1.261996585732577891, -3.312499998634407916 ) ) ;
#11165=CARTESIAN_POINT ( 'NONE',  ( -0.5093500532425060401, -4.799145180956616130, -5.874999998634406140 ) ) ;
#11169=VERTEX_POINT ( 'NONE', #15047 ) ;
#11175=CARTESIAN_POINT ( 'NONE',  ( -3.033343224707664820, 3.753672977998667726, -2.249999998634408804 ) ) ;
#11178=CARTESIAN_POINT ( 'NONE',  ( -2.452879891156813041, -7.244083172395187731, -0.1007566405101838203 ) ) ;
#11181=CARTESIAN_POINT ( 'NONE',  ( -4.391654775818395251, 2.390265326283148806, -2.499999997268815388 ) ) ;
#11188=CARTESIAN_POINT ( 'NONE',  ( 3.033343224707661712, -3.753672977998669946, -2.499999998634408804 ) ) ;
#11190=VERTEX_POINT ( 'NONE', #15291 ) ;
#11198=EDGE_CURVE ( 'NONE', #1925, #13370, #8841, .T. ) ;
#11205=CARTESIAN_POINT ( 'NONE',  ( -1.415196051561583790, 4.795541693661363958, -4.750000000000000888 ) ) ;
#11206=CARTESIAN_POINT ( 'NONE',  ( 1.415196051561583790, -4.795541693661363958, -2.124999997268814944 ) ) ;
#11209=CARTESIAN_POINT ( 'NONE',  ( 3.753672977998667726, 3.033343224707664376, -4.499999998634407028 ) ) ;
#11210=ORIENTED_EDGE ( 'NONE', *, *, #5204, .F. ) ;
#11220=LINE ( 'NONE', #4022, #679 ) ;
#11222=EDGE_CURVE ( 'NONE', #9532, #15211, #14599, .T. ) ;
#11224=CARTESIAN_POINT ( 'NONE',  ( 0.5093500532425063732, 4.799145180956616130, -2.124999998634406584 ) ) ;
#11228=CARTESIAN_POINT ( 'NONE',  ( 0.000000000000000000, 0.000000000000000000, -9.226681596905677907 ) ) ;
#11245=CARTESIAN_POINT ( 'NONE',  ( 1.261996585732578113, -4.276409079477644148, -2.562499998634407028 ) ) ;
#11248=CARTESIAN_POINT ( 'NONE',  ( -4.799145180956616130, 0.5093500532425063732, -6.124999998634407916 ) ) ;
#11250=DIRECTION ( 'NONE',  ( 0.2830392103123166025, -0.9591083387322728582, 0.000000000000000000 ) ) ;
#11258=CARTESIAN_POINT ( 'NONE',  ( -0.5093500532425060401, -4.799145180956616130, -5.874999998634406140 ) ) ;
#11267=CARTESIAN_POINT ( 'NONE',  ( -2.390265326283148806, -4.391654775818394363, -5.249999997268817609 ) ) ;
#11273=CARTESIAN_POINT ( 'NONE',  ( 2.131511515620586383, 3.916244202832140253, -8.187499998634407916 ) ) ;
#11282=CARTESIAN_POINT ( 'NONE',  ( 4.999999999999849898, -1.272547481429012084, -0.08659748264465111367 ) ) ;
#11289=CARTESIAN_POINT ( 'NONE',  ( 3.401574460001763001, -4.209348295687703967, -5.187500000000001776 ) ) ;
#11293=CARTESIAN_POINT ( 'NONE',  ( -4.799145180956616130, 0.5093500532425063732, -6.124999998634407916 ) ) ;
#11296=CARTESIAN_POINT ( 'NONE',  ( 0.000000000000000000, 0.000000000000000000, 0.000000000000000000 ) ) ;
#11306=CARTESIAN_POINT ( 'NONE',  ( 5.276765049035075705, -6.073111908730306929, -7.634085501268428331 ) ) ;
#11307=CARTESIAN_POINT ( 'NONE',  ( 4.799145180956616130, -0.5093500532425063732, -1.374999998634406140 ) ) ;
#11308=CARTESIAN_POINT ( 'NONE',  ( 2.564533730342835938, 3.657148745220786257, -0.3789984458506786558 ) ) ;
#11311=DIRECTION ( 'NONE',  ( 1.000000000000000000, 0.000000000000000000, 0.000000000000000000 ) ) ;
#11312=DIRECTION ( 'NONE',  ( 0.000000000000000000, 0.000000000000000000, 1.000000000000000000 ) ) ;
#11319=ORIENTED_EDGE ( 'NONE', *, *, #6819, .T. ) ;
#11331=CARTESIAN_POINT ( 'NONE',  ( -4.799145180956616130, 0.5093500532425063732, -5.124999998634405252 ) ) ;
#11333=EDGE_CURVE ( 'NONE', #7550, #2200, #8027, .T. ) ;
#11336=EDGE_CURVE ( 'NONE', #13099, #3963, #366, .T. ) ;
#11339=CARTESIAN_POINT ( 'NONE',  ( 4.999999999999845457, -1.272547481429021854, -7.086597482644653390 ) ) ;
#11342=CARTESIAN_POINT ( 'NONE',  ( 0.5093500532425063732, 4.799145180956616130, -8.374999998634409692 ) ) ;
#11344=CARTESIAN_POINT ( 'NONE',  ( -4.209348295687703079, -3.401574460001763445, -5.312499997268816720 ) ) ;
#11346=CARTESIAN_POINT ( 'NONE',  ( -3.401574460001764777, 4.209348295687701302, -3.562499997268815832 ) ) ;
#11347=CARTESIAN_POINT ( 'NONE',  ( -5.000000000000004441, -7.530481206757679743E-15, -2.545263047592944972 ) ) ;
#11356=CARTESIAN_POINT ( 'NONE',  ( 7.500000000000000888, 4.330127018922199866, -1.000000000000000888 ) ) ;
#11363=CARTESIAN_POINT ( 'NONE',  ( -5.000000000000000888, 6.123233995736767268E-16, -25.03750572909317285 ) ) ;
#11364=CARTESIAN_POINT ( 'NONE',  ( -5.335963852939856977, -6.035591050534137025, -7.593821156097345870 ) ) ;
#11365=FACE_OUTER_BOUND ( 'NONE', #3716, .T. ) ;
#11366=CARTESIAN_POINT ( 'NONE',  ( -5.381735091635034607, 0.5711823568785950878, -5.562500000000000000 ) ) ;
#11372=CARTESIAN_POINT ( 'NONE',  ( -4.276409079477644148, -1.261996585732578335, -5.062499998634406140 ) ) ;
#11382=CARTESIAN_POINT ( 'NONE',  ( -2.131511515620587272, -3.916244202832140253, -1.687499998634406362 ) ) ;
#11385=CARTESIAN_POINT ( 'NONE',  ( -2.500000000000000888, -7.216878364870333407, -7.063244554130006847 ) ) ;
#11388=EDGE_CURVE ( 'NONE', #15211, #15708, #11749, .T. ) ;
#11391=CARTESIAN_POINT ( 'NONE',  ( 2.602085213965210642E-15, 8.660254037844392627, -1.000000000000000888 ) ) ;
#11392=ORIENTED_EDGE ( 'NONE', *, *, #6933, .F. ) ;
#11396=( BOUNDED_CURVE ( )  B_SPLINE_CURVE ( 2, ( #11947, #13164, #2098 ),
 .UNSPECIFIED., .F., .F. ) 
 B_SPLINE_CURVE_WITH_KNOTS ( ( 3, 3 ),
 ( 0.2000000000000001776, 0.2045872658012772849 ),
 .UNSPECIFIED. ) 
 CURVE ( )  GEOMETRIC_REPRESENTATION_ITEM ( )  RATIONAL_B_SPLINE_CURVE ( ( 0.9999999999999990008, 0.9720652146169426189, 0.9646335149384808183 ) ) 
 REPRESENTATION_ITEM ( '' )  );
#11397=ORIENTED_EDGE ( 'NONE', *, *, #9017, .T. ) ;
#11401=CARTESIAN_POINT ( 'NONE',  ( 4.209348295687701302, 3.401574460001766109, -1.812499997268814278 ) ) ;
#11403=CARTESIAN_POINT ( 'NONE',  ( 0.5711823568785988625, 5.381735091635026613, -6.687499997268816720 ) ) ;
#11405=CARTESIAN_POINT ( 'NONE',  ( 3.033343224707661712, -3.753672977998669946, -4.749999998634407028 ) ) ;
#11408=CARTESIAN_POINT ( 'NONE',  ( -7.500000000000003553, -2.886751345948131320, -7.198902722707431145 ) ) ;
#11412=ORIENTED_EDGE ( 'NONE', *, *, #383, .F. ) ;
#11414=CARTESIAN_POINT ( 'NONE',  ( -3.916244202832140253, 2.131511515620587272, -5.187499998634406140 ) ) ;
#11419=DIRECTION ( 'NONE',  ( 0.000000000000000000, 0.000000000000000000, 1.000000000000000000 ) ) ;
#11422=CARTESIAN_POINT ( 'NONE',  ( -1.415196051561583790, 4.795541693661363958, -3.624999997268816276 ) ) ;
#11424=CARTESIAN_POINT ( 'NONE',  ( -1.654942507329426382, 4.210624982170731556, -0.3352054413388214082 ) ) ;
#11428=CARTESIAN_POINT ( 'NONE',  ( 7.500000000000000000, -5.204170427930421283E-15, -6.991905250253757309 ) ) ;
#11431=VERTEX_POINT ( 'NONE', #1116 ) ;
#11434=CARTESIAN_POINT ( 'NONE',  ( -5.000000000000091482, -0.7223674278660691117, -0.5217993655171538903 ) ) ;
#11439=CARTESIAN_POINT ( 'NONE',  ( -7.263825692932306843, -4.945657111639584436, -7.907570769506049757 ) ) ;
#11440=CARTESIAN_POINT ( 'NONE',  ( -7.847095227763516867, -4.129731495738497848, -7.493596212620241559 ) ) ;
#11442=CARTESIAN_POINT ( 'NONE',  ( -2.390265326283148806, -4.391654775818394363, -5.375000000000000888 ) ) ;
#11446=CARTESIAN_POINT ( 'NONE',  ( 0.5093500532425063732, 4.799145180956616130, -5.374999998634406140 ) ) ;
#11449=CARTESIAN_POINT ( 'NONE',  ( 2.500000000000000000, 7.216878364870322748, -7.063244554130002406 ) ) ;
#11460=CARTESIAN_POINT ( 'NONE',  ( 3.916244202832140253, -2.131511515620588160, -1.437499998634406140 ) ) ;
#11466=CARTESIAN_POINT ( 'NONE',  ( 1.415196051561583790, -4.795541693661363958, -3.250000000000002665 ) ) ;
#11471=ORIENTED_EDGE ( 'NONE', *, *, #4162, .T. ) ;
#11483=CARTESIAN_POINT ( 'NONE',  ( -3.401574460001765221, 4.209348295687701302, -7.562499997268815832 ) ) ;
#11486=( BOUNDED_CURVE ( )  B_SPLINE_CURVE ( 2, ( #10316, #450, #12464, #3909, #2854, #8855, #1403, #299, #15241 ),
 .UNSPECIFIED., .F., .F. ) 
 B_SPLINE_CURVE_WITH_KNOTS ( ( 3, 2, 2, 2, 3 ),
 ( 0.9545872658012772849, 0.9625000000000000222, 0.9749999999999999778, 0.9875000000000000444, 1.000000000000000000 ),
 .UNSPECIFIED. ) 
 CURVE ( )  GEOMETRIC_REPRESENTATION_ITEM ( )  RATIONAL_B_SPLINE_CURVE ( ( 0.9646335149384808183, 0.9518143178943441196, 1.000000000000000000, 0.9238795325112867385, 1.000000000000000000, 0.9238795325112867385, 1.000000000000000000, 0.9238795325112867385, 1.000000000000000000 ) ) 
 REPRESENTATION_ITEM ( '' )  );
#11493=CARTESIAN_POINT ( 'NONE',  ( 0.5093500532425063732, 4.799145180956616130, -7.374999998634407916 ) ) ;
#11499=CARTESIAN_POINT ( 'NONE',  ( -4.209348295687703967, -3.401574460001763001, -2.312499997268814500 ) ) ;
#11507=ORIENTED_EDGE ( 'NONE', *, *, #9553, .F. ) ;
#11514=AXIS2_PLACEMENT_3D ( 'NONE', #12442, #11008, #14725 ) ;
#11518=CIRCLE ( 'NONE', #1209, 5.000000000000000888 ) ;
#11519=CARTESIAN_POINT ( 'NONE',  ( 0.3483149870578527429, -8.861353789385033153, -7.493854785173817312 ) ) ;
#11521=CARTESIAN_POINT ( 'NONE',  ( 4.795541693661363958, 1.415196051561583790, -7.000000000000002665 ) ) ;
#11522=PLANE ( 'NONE',  #14158 ) ;
#11526=CARTESIAN_POINT ( 'NONE',  ( 2.131511515620586383, 3.916244202832140253, -5.437499998634406140 ) ) ;
#11528=CARTESIAN_POINT ( 'NONE',  ( -4.336808689942017736E-16, 9.147862274876558786, -8.047472243342932430 ) ) ;
#11535=CIRCLE ( 'NONE', #9234, 5.000000000000000888 ) ;
#11539=CARTESIAN_POINT ( 'NONE',  ( 7.500000000000000000, 3.948247735265757452, -7.349893093596098659 ) ) ;
#11540=CARTESIAN_POINT ( 'NONE',  ( 0.5093500532425063732, 4.799145180956616130, -1.124999998634405918 ) ) ;
#11541=CARTESIAN_POINT ( 'NONE',  ( 3.528469415195318426, 2.738956135389102098, -0.3789984458506761023 ) ) ;
#11543=CARTESIAN_POINT ( 'NONE',  ( -2.131511515620587272, -3.916244202832140253, -3.687499998634407916 ) ) ;
#11549=CYLINDRICAL_SURFACE ( 'NONE', #3685, 5.000000000000000888 ) ;
#11558=CARTESIAN_POINT ( 'NONE',  ( 7.808623696107322765, 4.508310992947620832, -7.999704684617482187 ) ) ;
#11564=CARTESIAN_POINT ( 'NONE',  ( -4.391654775818395251, 2.390265326283148806, -6.499999997268815832 ) ) ;
#11566=CARTESIAN_POINT ( 'NONE',  ( -4.391654775818395251, 2.390265326283148806, -7.499999997268816720 ) ) ;
#11570=EDGE_CURVE ( 'NONE', #6761, #4915, #2400, .T. ) ;
#11576=VECTOR ( 'NONE', #12046, 1000.000000000000000 ) ;
#11577=VERTEX_POINT ( 'NONE', #8647 ) ;
#11578=AXIS2_PLACEMENT_3D ( 'NONE', #10741, #884, #8015 ) ;
#11581=CARTESIAN_POINT ( 'NONE',  ( 4.999999999999845457, -1.272547481429021854, -7.961597479913462116 ) ) ;
#11583=CARTESIAN_POINT ( 'NONE',  ( -3.916244202832140253, 2.131511515620587272, 0.8125000013655924169 ) ) ;
#11588=CARTESIAN_POINT ( 'NONE',  ( 4.575072720889181710, -0.1979831123187004716, -0.2975372840247698103 ) ) ;
#11596=CARTESIAN_POINT ( 'NONE',  ( -2.390265326283148806, -4.391654775818394363, -0.3750000000000003331 ) ) ;
#11598=CARTESIAN_POINT ( 'NONE',  ( -6.293430271071540183, 5.026740376715094882, -0.4524126574264508149 ) ) ;
#11600=CARTESIAN_POINT ( 'NONE',  ( -5.000000000000004441, -1.011557177027151181E-15, -5.545263047592944972 ) ) ;
#11602=CARTESIAN_POINT ( 'NONE',  ( 4.420982230657666712, -0.5789871446316176007, -0.3789984458506777676 ) ) ;
#11606=CARTESIAN_POINT ( 'NONE',  ( 3.916244202832140253, -2.131511515620588160, -4.687499998634405252 ) ) ;
#11608=CARTESIAN_POINT ( 'NONE',  ( 2.602085213965210642E-15, 8.660254037844392627, -7.422398894150035176 ) ) ;
#11614=CARTESIAN_POINT ( 'NONE',  ( -4.795541693661363958, -1.415196051561583790, -6.500000000000002665 ) ) ;
#11617=CARTESIAN_POINT ( 'NONE',  ( 3.033343224707661712, -3.753672977998669502, -4.499999998634407028 ) ) ;
#11621=CARTESIAN_POINT ( 'NONE',  ( -0.5093500532425060401, -4.799145180956616130, -5.624999998634406140 ) ) ;
#11627=CARTESIAN_POINT ( 'NONE',  ( 1.015826369459312373, -8.073766409986486536, -7.642786413609471197 ) ) ;
#11635=CARTESIAN_POINT ( 'NONE',  ( 7.897836333153806621, 1.530409084195002656, -7.633857274177626273 ) ) ;
#11639=B_SPLINE_CURVE_WITH_KNOTS ( 'NONE', 3,
 ( #2448, #1404, #12389, #1247, #8939, #5210, #11424, #12550, #10069, #3838, #14998, #3911, #371, #5139, #4966, #8781, #4072, #14830, #1572, #5288 ),
 .UNSPECIFIED., .F., .F.,
 ( 4, 2, 2, 2, 2, 2, 2, 2, 2, 4 ),
 ( 0.000000000000000000, 0.0009685699525029332598, 0.001937139905005866520, 0.002421424881257333312, 0.002905709857508799888, 0.003874279810011731304, 0.004842849762514664022, 0.005811419715017596306, 0.006779989667520527723, 0.007748559620023459139 ),
 .UNSPECIFIED. ) ;
#11642=CARTESIAN_POINT ( 'NONE',  ( -2.131511515620587272, -3.916244202832140253, 0.06250000136559172303 ) ) ;
#11647=CARTESIAN_POINT ( 'NONE',  ( 4.795541693661363958, 1.415196051561583790, -5.000000000000000888 ) ) ;
#11651=EDGE_CURVE ( 'NONE', #4563, #3351, #3869, .T. ) ;
#11655=CARTESIAN_POINT ( 'NONE',  ( 1.261996585732578113, -4.276409079477644148, 1.187500001365592750 ) ) ;
#11679=DIRECTION ( 'NONE',  ( 0.000000000000000000, 0.000000000000000000, -1.000000000000000000 ) ) ;
#11681=CARTESIAN_POINT ( 'NONE',  ( 1.261996585732578113, -4.276409079477644148, 0.4375000013655920839 ) ) ;
#11690=CARTESIAN_POINT ( 'NONE',  ( 5.000000000000004441, -2.247904837838113790E-16, -6.045263047592945860 ) ) ;
#11692=CARTESIAN_POINT ( 'NONE',  ( -4.276409079477644148, -1.261996585732578335, -5.812499998634406140 ) ) ;
#11693=CARTESIAN_POINT ( 'NONE',  ( 5.000000000000002665, 1.275685995473128912E-14, -5.920263044861758139 ) ) ;
#11695=CARTESIAN_POINT ( 'NONE',  ( -3.753672977998669946, -3.033343224707661712, -5.749999998634407916 ) ) ;
#11701=CARTESIAN_POINT ( 'NONE',  ( -0.2779000157839473517, -8.820699686765063774, -7.928862157988307402 ) ) ;
#11713=CARTESIAN_POINT ( 'NONE',  ( -1.415196051561583790, 4.795541693661363958, -6.624999997268815832 ) ) ;
#11718=CARTESIAN_POINT ( 'NONE',  ( 5.000000000000004441, -2.247904837838113790E-16, -7.920263044861759028 ) ) ;
#11719=CARTESIAN_POINT ( 'NONE',  ( -3.033343224707664376, 3.753672977998667726, 0.7500000013655939712 ) ) ;
#11728=CARTESIAN_POINT ( 'NONE',  ( -4.336808689942017736E-16, -8.660254037844399733, -9.999999999999998224 ) ) ;
#11730=CARTESIAN_POINT ( 'NONE',  ( 4.209348295687701302, 3.401574460001765665, -6.812499997268814944 ) ) ;
#11749=CIRCLE ( 'NONE', #13816, 7.500000000000001776 ) ;
#11754=CARTESIAN_POINT ( 'NONE',  ( 4.406842699996126989, -6.115962218725296218, -6.661067097207817866E-15 ) ) ;
#11756=CARTESIAN_POINT ( 'NONE',  ( -4.403473400622100797, -6.117907484625868086, -4.528238136021488035E-15 ) ) ;
#11758=CARTESIAN_POINT ( 'NONE',  ( 0.5093500532425063732, 4.799145180956616130, -0.1249999986344088321 ) ) ;
#11771=DIRECTION ( 'NONE',  ( 1.000000000000000000, 0.000000000000000000, 0.000000000000000000 ) ) ;
#11772=CARTESIAN_POINT ( 'NONE',  ( -0.5093500532425060401, -4.799145180956616130, -6.624999998634407916 ) ) ;
#11777=CARTESIAN_POINT ( 'NONE',  ( 4.799145180956616130, -0.5093500532425063732, -6.374999998634407028 ) ) ;
#11784=ORIENTED_EDGE ( 'NONE', *, *, #4510, .T. ) ;
#11785=AXIS2_PLACEMENT_3D ( 'NONE', #3667, #3427, #7165 ) ;
#11787=CARTESIAN_POINT ( 'NONE',  ( 7.500000000000000000, -2.571118828324946648, -0.3627527587569098766 ) ) ;
#11797=CARTESIAN_POINT ( 'NONE',  ( 1.415196051561583790, -4.795541693661363958, -4.250000000000000000 ) ) ;
#11800=CARTESIAN_POINT ( 'NONE',  ( 4.276409079477644148, 1.261996585732577891, -7.562499998634407916 ) ) ;
#11801=CARTESIAN_POINT ( 'NONE',  ( 3.916244202832140253, -2.131511515620588160, 0.3125000013655919728 ) ) ;
#11803=VERTEX_POINT ( 'NONE', #4105 ) ;
#11816=CARTESIAN_POINT ( 'NONE',  ( 2.390265326283148806, 4.391654775818395251, -8.749999997268814056 ) ) ;
#11817=LINE ( 'NONE', #3184, #9516 ) ;
#11818=DIRECTION ( 'NONE',  ( 0.000000000000000000, 0.000000000000000000, 1.000000000000000000 ) ) ;
#11828=CARTESIAN_POINT ( 'NONE',  ( 4.276409079477644148, 1.261996585732577891, -0.5624999986344088043 ) ) ;
#11832=CARTESIAN_POINT ( 'NONE',  ( 4.795541693661363958, 1.415196051561583790, -3.469446951953614189E-15 ) ) ;
#11833=EDGE_CURVE ( 'NONE', #7493, #3061, #789, .T. ) ;
#11842=CARTESIAN_POINT ( 'NONE',  ( -0.5093500532425060401, -4.799145180956616130, -1.624999998634406362 ) ) ;
#11854=CARTESIAN_POINT ( 'NONE',  ( -4.276409079477644148, -1.261996585732578335, -6.812499998634407028 ) ) ;
#11858=CARTESIAN_POINT ( 'NONE',  ( 3.401574460001763001, -4.209348295687703967, 0.8124999999999960032 ) ) ;
#11862=ORIENTED_EDGE ( 'NONE', *, *, #8608, .T. ) ;
#11867=ORIENTED_EDGE ( 'NONE', *, *, #7211, .T. ) ;
#11868=CARTESIAN_POINT ( 'NONE',  ( 5.000000000000095923, 0.7223674278660565662, -3.896799362785971610 ) ) ;
#11870=CARTESIAN_POINT ( 'NONE',  ( 1.415196051561583790, -4.795541693661363958, -7.124999997268815832 ) ) ;
#11877=CARTESIAN_POINT ( 'NONE',  ( 1.415196051561583790, -4.795541693661363958, -0.1249999972688167760 ) ) ;
#11888=CARTESIAN_POINT ( 'NONE',  ( 1.261996585732578113, -4.276409079477644148, 0.4375000013655920839 ) ) ;
#11890=CARTESIAN_POINT ( 'NONE',  ( 1.415196051561583790, -4.795541693661363958, -6.124999997268814944 ) ) ;
#11892=CARTESIAN_POINT ( 'NONE',  ( -1.908195823574487804E-14, -8.660254037844392627, -1.000000000000000888 ) ) ;
#11896=CARTESIAN_POINT ( 'NONE',  ( 2.390265326283148806, 4.391654775818395251, -2.749999997268815832 ) ) ;
#11897=CARTESIAN_POINT ( 'NONE',  ( 0.000000000000000000, 0.000000000000000000, 0.000000000000000000 ) ) ;
#11908=CARTESIAN_POINT ( 'NONE',  ( -6.901579824520448270, 4.675625068323816969, -0.7022220667781353676 ) ) ;
#11912=CARTESIAN_POINT ( 'NONE',  ( 5.047120108843203390, -5.746297884371400322, -0.1007566405101857077 ) ) ;
#11916=CARTESIAN_POINT ( 'NONE',  ( 4.799145180956616130, -0.5093500532425063732, 1.625000001365592528 ) ) ;
#11918=CARTESIAN_POINT ( 'NONE',  ( 6.658902113223716057, 5.287118297637872999, -7.776713651266099703 ) ) ;
#11922=ORIENTED_EDGE ( 'NONE', *, *, #11833, .F. ) ;
#11924=CARTESIAN_POINT ( 'NONE',  ( -4.391654775818395251, 2.390265326283148806, -7.625000000000003553 ) ) ;
#11927=CARTESIAN_POINT ( 'NONE',  ( 4.276409079477644148, 1.261996585732577891, -5.312499998634406140 ) ) ;
#11928=DIRECTION ( 'NONE',  ( 1.000000000000000000, 0.000000000000000000, 0.000000000000000000 ) ) ;
#11930=CARTESIAN_POINT ( 'NONE',  ( 0.5711823568785989735, 5.381735091635026613, 1.187499999999998224 ) ) ;
#11942=EDGE_CURVE ( 'NONE', #11577, #2543, #563, .T. ) ;
#11943=CARTESIAN_POINT ( 'NONE',  ( 5.000000000000004441, -2.247904837838113790E-16, -6.920263044861760804 ) ) ;
#11947=CARTESIAN_POINT ( 'NONE',  ( 4.795541693661363958, 1.415196051561583790, -3.469446951953614189E-15 ) ) ;
#11962=DIRECTION ( 'NONE',  ( -0.000000000000000000, -0.000000000000000000, -1.000000000000000000 ) ) ;
#11964=CARTESIAN_POINT ( 'NONE',  ( -10.12668159690567649, 1.240160820363494356E-15, -9.226681596905677907 ) ) ;
#11965=CARTESIAN_POINT ( 'NONE',  ( -4.799145180956616130, 0.5093500532425063732, 0.1250000013655913900 ) ) ;
#11967=CARTESIAN_POINT ( 'NONE',  ( -2.131511515620587272, -3.916244202832140253, 0.06250000136559172303 ) ) ;
#11968=CYLINDRICAL_SURFACE ( 'NONE', #13344, 5.000000000000000888 ) ;
#11972=DIRECTION ( 'NONE',  ( 0.000000000000000000, 0.000000000000000000, 1.000000000000000000 ) ) ;
#11982=CARTESIAN_POINT ( 'NONE',  ( -7.922281120364393914, 4.573931137438272287, -8.047472243342932430 ) ) ;
#11983=CARTESIAN_POINT ( 'NONE',  ( 1.415196051561583790, -4.795541693661363958, -2.250000000000001776 ) ) ;
#11986=CARTESIAN_POINT ( 'NONE',  ( 2.390265326283148806, 4.391654775818395251, -0.7499999972688138339 ) ) ;
#11989=CARTESIAN_POINT ( 'NONE',  ( 0.000000000000000000, 0.000000000000000000, -8.499999999999996447 ) ) ;
#11991=CARTESIAN_POINT ( 'NONE',  ( 3.916244202832140253, -2.131511515620588160, 0.5625000013655921949 ) ) ;
#11996=( BOUNDED_CURVE ( )  B_SPLINE_CURVE ( 2, ( #5512, #1791, #667, #7950, #429, #5354, #2915, #7866, #15377, #4299, #13168 ),
 .UNSPECIFIED., .F., .F. ) 
 B_SPLINE_CURVE_WITH_KNOTS ( ( 3, 2, 2, 2, 2, 3 ),
 ( 0.1545872658012772960, 0.1625000000000000056, 0.1749999999999999889, 0.1875000000000000000, 0.2000000000000000111, 0.2045872658012772849 ),
 .UNSPECIFIED. ) 
 CURVE ( )  GEOMETRIC_REPRESENTATION_ITEM ( )  RATIONAL_B_SPLINE_CURVE ( ( 0.9646335149384808183, 0.9518143178943438976, 1.000000000000000000, 0.9238795325112867385, 1.000000000000000000, 0.9238795325112867385, 1.000000000000000000, 0.9238795325112867385, 1.000000000000000000, 0.9720652146169430630, 0.9646335149384808183 ) ) 
 REPRESENTATION_ITEM ( '' )  );
#12009=CARTESIAN_POINT ( 'NONE',  ( 3.753672977998667726, 3.033343224707664376, -8.249999998634409692 ) ) ;
#12012=CARTESIAN_POINT ( 'NONE',  ( 1.023706143822011194, -4.792166261265705884, -0.07488405613504552083 ) ) ;
#12017=EDGE_LOOP ( 'NONE', ( #7292, #14246, #11862, #14342 ) ) ;
#12018=ORIENTED_EDGE ( 'NONE', *, *, #1639, .F. ) ;
#12042=CARTESIAN_POINT ( 'NONE',  ( -6.439685834477302251, 4.942299687812321984, -7.659344964962857993 ) ) ;
#12046=DIRECTION ( 'NONE',  ( 0.000000000000000000, 0.000000000000000000, 1.000000000000000000 ) ) ;
#12048=CARTESIAN_POINT ( 'NONE',  ( -3.753672977998669946, -3.033343224707661712, 0.2500000013655933606 ) ) ;
#12051=CARTESIAN_POINT ( 'NONE',  ( -3.916244202832140253, 2.131511515620587272, -0.1874999986344084990 ) ) ;
#12056=ORIENTED_EDGE ( 'NONE', *, *, #625, .F. ) ;
#12061=CARTESIAN_POINT ( 'NONE',  ( 4.276409079477644148, 1.261996585732577891, -1.562499998634406140 ) ) ;
#12071=CARTESIAN_POINT ( 'NONE',  ( 2.390265326283148806, 4.391654775818395251, 0.2500000027311835571 ) ) ;
#12073=( NAMED_UNIT ( * ) SI_UNIT ( $, .STERADIAN. ) SOLID_ANGLE_UNIT ( ) );
#12075=CARTESIAN_POINT ( 'NONE',  ( 4.799145180956616130, -0.5093500532425063732, -3.374999998634407472 ) ) ;
#12077=CARTESIAN_POINT ( 'NONE',  ( 2.621328321947449691, 7.606199919102465401, -7.633618187056574911 ) ) ;
#12078=ORIENTED_EDGE ( 'NONE', *, *, #294, .F. ) ;
#12085=CARTESIAN_POINT ( 'NONE',  ( 0.000000000000000000, 0.000000000000000000, -25.03750572909317285 ) ) ;
#12092=CARTESIAN_POINT ( 'NONE',  ( -2.390265326283148806, -4.391654775818394363, -0.3750000000000003331 ) ) ;
#12093=CARTESIAN_POINT ( 'NONE',  ( 2.390265326283148806, 4.391654775818395251, -3.875000000000000000 ) ) ;
#12097=CARTESIAN_POINT ( 'NONE',  ( -3.753672977998669946, -3.033343224707661712, 1.000000001365594082 ) ) ;
#12098=ORIENTED_EDGE ( 'NONE', *, *, #1782, .F. ) ;
#12100=B_SPLINE_CURVE_WITH_KNOTS ( 'NONE', 3,
 ( #12950, #1887, #5692, #4403, #7971, #12875, #5532, #10468, #15400, #10628 ),
 .UNSPECIFIED., .F., .F.,
 ( 4, 2, 2, 2, 4 ),
 ( 0.01051144076094936118, 0.01162027323572612306, 0.01272910571050288493, 0.01383793818527964507, 0.01494677066005640695 ),
 .UNSPECIFIED. ) ;
#12118=CARTESIAN_POINT ( 'NONE',  ( 1.415196051561583790, -4.795541693661363958, -6.124999997268814944 ) ) ;
#12126=CARTESIAN_POINT ( 'NONE',  ( 7.500000000000000000, 4.330127018922190096, -9.999999999999998224 ) ) ;
#12130=CARTESIAN_POINT ( 'NONE',  ( 4.799145180956616130, -0.5093500532425063732, 0.3750000013655915843 ) ) ;
#12132=ORIENTED_EDGE ( 'NONE', *, *, #14027, .F. ) ;
#12137=ORIENTED_EDGE ( 'NONE', *, *, #14112, .T. ) ;
#12139=CARTESIAN_POINT ( 'NONE',  ( -3.033343224707664820, 3.753672977998667726, -4.249999998634407028 ) ) ;
#12145=CARTESIAN_POINT ( 'NONE',  ( -7.897850199329722543, 1.533397866934075759, -7.634054012537968781 ) ) ;
#12148=CARTESIAN_POINT ( 'NONE',  ( -4.795541693661363958, -1.415196051561583790, -1.374999997268814500 ) ) ;
#12152=CARTESIAN_POINT ( 'NONE',  ( 3.033343224707661712, -3.753672977998669946, -3.499999998634410137 ) ) ;
#12163=DIRECTION ( 'NONE',  ( 0.000000000000000000, 0.000000000000000000, 1.000000000000000000 ) ) ;
#12165=CARTESIAN_POINT ( 'NONE',  ( 5.381735091635035495, -0.5711823568785978633, -3.062500000000001776 ) ) ;
#12167=CARTESIAN_POINT ( 'NONE',  ( 2.286513180745818108, -4.371196073312955122, -0.05185736845305202042 ) ) ;
#12169=CARTESIAN_POINT ( 'NONE',  ( 3.916244202832140253, -2.131511515620588160, -1.687499998634406362 ) ) ;
#12196=ORIENTED_EDGE ( 'NONE', *, *, #15439, .F. ) ;
#12200=LINE ( 'NONE', #11010, #11576 ) ;
#12201=CARTESIAN_POINT ( 'NONE',  ( 1.261996585732578113, -4.276409079477644148, 1.437500001365592972 ) ) ;
#12204=CARTESIAN_POINT ( 'NONE',  ( 4.799145180956616130, -0.5093500532425063732, -1.624999998634406362 ) ) ;
#12215=CARTESIAN_POINT ( 'NONE',  ( 3.033343224707661712, -3.753672977998669502, -3.749999998634410137 ) ) ;
#12221=CARTESIAN_POINT ( 'NONE',  ( 1.415196051561583790, -4.795541693661363958, -1.124999997268814278 ) ) ;
#12223=SURFACE_STYLE_USAGE ( .BOTH. , #8312 ) ;
#12228=CARTESIAN_POINT ( 'NONE',  ( 2.131511515620586383, 3.916244202832140253, -6.187499998634407028 ) ) ;
#12230=B_SPLINE_CURVE_WITH_KNOTS ( 'NONE', 3,
 ( #11602, #10642, #3198, #9349 ),
 .UNSPECIFIED., .F., .F.,
 ( 4, 4 ),
 ( 1.661095388496746134E-17, 0.0005803541179376217390 ),
 .UNSPECIFIED. ) ;
#12243=CARTESIAN_POINT ( 'NONE',  ( -1.415196051561583790, 4.795541693661363958, -0.7500000000000006661 ) ) ;
#12245=CARTESIAN_POINT ( 'NONE',  ( 0.7619918569178352197, -4.833934400323800951, -0.07953229779526811705 ) ) ;
#12249=CARTESIAN_POINT ( 'NONE',  ( 0.5093500532425063732, 4.799145180956616130, -3.374999998634407472 ) ) ;
#12258=CARTESIAN_POINT ( 'NONE',  ( 4.535975386569504053, 1.338596318647080397, -8.718749997951611874 ) ) ;
#12269=CARTESIAN_POINT ( 'NONE',  ( -0.5711823568785977523, -5.381735091635034607, -1.187499997268815610 ) ) ;
#12272=CARTESIAN_POINT ( 'NONE',  ( -4.209348295687703079, -3.401574460001763445, -6.312499997268814056 ) ) ;
#12285=CARTESIAN_POINT ( 'NONE',  ( 4.276409079477644148, 1.261996585732577891, -2.312499998634407028 ) ) ;
#12289=CARTESIAN_POINT ( 'NONE',  ( -1.261996585732579224, 4.276409079477648589, -3.312499998634407916 ) ) ;
#12298=CARTESIAN_POINT ( 'NONE',  ( -4.276409079477644148, -1.261996585732578335, -3.062499998634407472 ) ) ;
#12304=CARTESIAN_POINT ( 'NONE',  ( 4.999999999999849010, -1.272547481429013416, -2.086597482644648949 ) ) ;
#12306=CARTESIAN_POINT ( 'NONE',  ( -0.5711823568785978633, -5.381735091635035495, 0.8125000027311823914 ) ) ;
#12311=CARTESIAN_POINT ( 'NONE',  ( -3.033343224707664376, 3.753672977998667726, -5.999999998634407916 ) ) ;
#12315=EDGE_LOOP ( 'NONE', ( #1020, #14106, #2251 ) ) ;
#12325=AXIS2_PLACEMENT_3D ( 'NONE', #8652, #14545, #15774 ) ;
#12327=FACE_OUTER_BOUND ( 'NONE', #4716, .T. ) ;
#12330=CARTESIAN_POINT ( 'NONE',  ( -1.415196051561583790, 4.795541693661363958, -2.750000000000002665 ) ) ;
#12332=CARTESIAN_POINT ( 'NONE',  ( -3.542429731366778967, -3.193955667491259476, -0.1664247486893449535 ) ) ;
#12334=CARTESIAN_POINT ( 'NONE',  ( 4.276409079477644148, 1.261996585732577891, -3.562499998634407916 ) ) ;
#12369=CARTESIAN_POINT ( 'NONE',  ( -3.033343224707664376, 3.753672977998667726, -3.999999998634406140 ) ) ;
#12371=CARTESIAN_POINT ( 'NONE',  ( 4.799145180956616130, -0.5093500532425063732, -5.624999998634406140 ) ) ;
#12372=CARTESIAN_POINT ( 'NONE',  ( -4.671041856245029322, -9.682850088987660890E-14, -0.2303389720127052009 ) ) ;
#12381=CARTESIAN_POINT ( 'NONE',  ( 4.799145180956616130, -0.5093500532425063732, -1.624999998634406362 ) ) ;
#12382=LINE ( 'NONE', #15145, #4000 ) ;
#12383=CARTESIAN_POINT ( 'NONE',  ( 3.916244202832140253, -2.131511515620588160, -7.437499998634407916 ) ) ;
#12387=CARTESIAN_POINT ( 'NONE',  ( 2.390265326283148806, 4.391654775818395251, -2.749999997268815832 ) ) ;
#12389=CARTESIAN_POINT ( 'NONE',  ( -0.06609243105207880664, 4.488461494241831495, -0.3660093223227993686 ) ) ;
#12393=CARTESIAN_POINT ( 'NONE',  ( -0.5093500532425060401, -4.799145180956616130, -2.624999998634407028 ) ) ;
#12398=EDGE_CURVE ( 'NONE', #3405, #513, #6598, .T. ) ;
#12404=CARTESIAN_POINT ( 'NONE',  ( -0.6249999999999978906, 8.299410119600878488, -7.298562697733107285 ) ) ;
#12407=CARTESIAN_POINT ( 'NONE',  ( -5.381735091635034607, 0.5711823568785950878, -4.562500000000000000 ) ) ;
#12408=CARTESIAN_POINT ( 'NONE',  ( 4.795541693661363958, 1.415196051561583790, -4.000000000000000000 ) ) ;
#12411=CARTESIAN_POINT ( 'NONE',  ( -3.033343224707664376, 3.753672977998667726, -3.249999998634409692 ) ) ;
#12415=ORIENTED_EDGE ( 'NONE', *, *, #13195, .F. ) ;
#12424=( BOUNDED_CURVE ( )  B_SPLINE_CURVE ( 2, ( #7062, #12942, #605, #9559, #6748, #6906, #14330, #915, #3257, #5839, #8204 ),
 .UNSPECIFIED., .F., .F. ) 
 B_SPLINE_CURVE_WITH_KNOTS ( ( 3, 2, 2, 2, 2, 3 ),
 ( 0.4045872658012772960, 0.4124999999999999778, 0.4249999999999999889, 0.4375000000000000000, 0.4500000000000000111, 0.4545872658012772849 ),
 .UNSPECIFIED. ) 
 CURVE ( )  GEOMETRIC_REPRESENTATION_ITEM ( )  RATIONAL_B_SPLINE_CURVE ( ( 0.9646335149384805963, 0.9518143178943438976, 1.000000000000000000, 0.9238795325112867385, 1.000000000000000000, 0.9238795325112867385, 1.000000000000000000, 0.9238795325112867385, 1.000000000000000000, 0.9720652146169430630, 0.9646335149384808183 ) ) 
 REPRESENTATION_ITEM ( '' )  );
#12425=FACE_OUTER_BOUND ( 'NONE', #6460, .T. ) ;
#12426=CARTESIAN_POINT ( 'NONE',  ( -1.261996585732579224, 4.276409079477648589, -3.062499998634407472 ) ) ;
#12440=CARTESIAN_POINT ( 'NONE',  ( 7.703928834700302986, 4.447865386531934639, -7.917997657324739258 ) ) ;
#12442=CARTESIAN_POINT ( 'NONE',  ( 0.000000000000000000, 0.000000000000000000, -25.03750572909317285 ) ) ;
#12445=CARTESIAN_POINT ( 'NONE',  ( 1.261996585732578113, -4.276409079477644148, -4.562499998634405252 ) ) ;
#12447=CARTESIAN_POINT ( 'NONE',  ( 1.261996585732578113, -4.276409079477644148, -6.812499998634407028 ) ) ;
#12449=FACE_OUTER_BOUND ( 'NONE', #1669, .T. ) ;
#12458=CARTESIAN_POINT ( 'NONE',  ( -4.799145180956616130, 0.5093500532425063732, -5.124999998634406140 ) ) ;
#12459=CARTESIAN_POINT ( 'NONE',  ( -3.916244202832140253, 2.131511515620587272, -7.937499998634408804 ) ) ;
#12463=CARTESIAN_POINT ( 'NONE',  ( 3.401574460001763001, -4.209348295687703967, -3.062499997268815388 ) ) ;
#12464=CARTESIAN_POINT ( 'NONE',  ( -4.391654775818395251, 2.390265326283148806, -8.499999997268814056 ) ) ;
#12470=CARTESIAN_POINT ( 'NONE',  ( 3.753672977998667726, 3.033343224707664376, -7.249999998634409692 ) ) ;
#12476=CARTESIAN_POINT ( 'NONE',  ( -6.601567268551442602, 5.319966374295968414, -7.792327460285854102 ) ) ;
#12481=CARTESIAN_POINT ( 'NONE',  ( -7.500000000000005329, 4.330127018922194537, -7.422398894150031623 ) ) ;
#12483=DIRECTION ( 'NONE',  ( 0.000000000000000000, 0.000000000000000000, -1.000000000000000000 ) ) ;
#12484=CARTESIAN_POINT ( 'NONE',  ( -3.401574460001764777, 4.209348295687701302, -4.687500000000000888 ) ) ;
#12486=CARTESIAN_POINT ( 'NONE',  ( -14.99999999999998934, -1.734723475976807094E-15, 0.000000000000000000 ) ) ;
#12488=CARTESIAN_POINT ( 'NONE',  ( -0.5093500532425060401, -4.799145180956616130, -1.874999998634406584 ) ) ;
#12502=ADVANCED_FACE ( 'NONE', ( #10041 ), #14802, .F. ) ;
#12511=ORIENTED_EDGE ( 'NONE', *, *, #799, .T. ) ;
#12516=VERTEX_POINT ( 'NONE', #8303 ) ;
#12526=CARTESIAN_POINT ( 'NONE',  ( 3.033343224707661712, -3.753672977998669946, -3.749999998634409692 ) ) ;
#12529=ORIENTED_EDGE ( 'NONE', *, *, #15114, .F. ) ;
#12537=CARTESIAN_POINT ( 'NONE',  ( -3.916244202832140253, 2.131511515620587272, -6.187499998634407028 ) ) ;
#12540=ADVANCED_FACE ( 'NONE', ( #2587 ), #7003, .F. ) ;
#12548=CARTESIAN_POINT ( 'NONE',  ( 5.381735091635035495, -0.5711823568785978633, -2.937499997268817165 ) ) ;
#12550=CARTESIAN_POINT ( 'NONE',  ( -1.955611824408503674, 4.089455165765809141, -0.3290272460762475593 ) ) ;
#12554=CARTESIAN_POINT ( 'NONE',  ( -2.131511515620587272, -3.916244202832140253, -7.687499998634407916 ) ) ;
#12558=CARTESIAN_POINT ( 'NONE',  ( -4.795541693661363958, -1.415196051561583790, 0.6250000027311839457 ) ) ;
#12566=CARTESIAN_POINT ( 'NONE',  ( -6.484173630541807398, -4.916614646774628561, -7.642786413616653896 ) ) ;
#12569=CARTESIAN_POINT ( 'NONE',  ( 5.381735091635035495, -0.5711823568785978633, -7.062500000000005329 ) ) ;
#12570=CARTESIAN_POINT ( 'NONE',  ( -1.415196051561583790, 4.795541693661363958, -2.750000000000002665 ) ) ;
#12573=CARTESIAN_POINT ( 'NONE',  ( -0.5093500532425060401, -4.799145180956616130, -7.874999998634408804 ) ) ;
#12577=ORIENTED_EDGE ( 'NONE', *, *, #294, .T. ) ;
#12578=EDGE_LOOP ( 'NONE', ( #1753, #15250, #4580, #14217 ) ) ;
#12587=CARTESIAN_POINT ( 'NONE',  ( -3.916244202832140253, 2.131511515620587272, -0.9374999986344056957 ) ) ;
#12591=CARTESIAN_POINT ( 'NONE',  ( -4.999999999999999112, -5.773502691896264416, -7.063244554130005071 ) ) ;
#12604=ORIENTED_EDGE ( 'NONE', *, *, #8343, .T. ) ;
#12605=CARTESIAN_POINT ( 'NONE',  ( 7.894787914004607998, 1.231001383561881556E-13, -7.591390474663423760 ) ) ;
#12609=CARTESIAN_POINT ( 'NONE',  ( -5.000000000000004441, -1.011557177027151181E-15, -6.420263044861759028 ) ) ;
#12610=CARTESIAN_POINT ( 'NONE',  ( 3.753672977998667726, 3.033343224707664376, -7.499999998634409692 ) ) ;
#12613=ORIENTED_EDGE ( 'NONE', *, *, #1540, .T. ) ;
#12623=CARTESIAN_POINT ( 'NONE',  ( 1.261996585732578113, -4.276409079477644148, -6.812499998634407028 ) ) ;
#12624=CARTESIAN_POINT ( 'NONE',  ( 4.209348295687701302, 3.401574460001766109, -4.812499997268817609 ) ) ;
#12628=CARTESIAN_POINT ( 'NONE',  ( 1.415196051561583790, -4.795541693661363958, -4.124999997268816720 ) ) ;
#12632=ORIENTED_EDGE ( 'NONE', *, *, #14135, .T. ) ;
#12634=CARTESIAN_POINT ( 'NONE',  ( -1.261996585732579224, 4.276409079477648589, -8.062499998634407916 ) ) ;
#12638=ORIENTED_EDGE ( 'NONE', *, *, #10158, .T. ) ;
#12641=EDGE_CURVE ( 'NONE', #11577, #9381, #8610, .T. ) ;
#12643=CARTESIAN_POINT ( 'NONE',  ( 1.415196051561583790, -4.795541693661363958, -0.2500000000000036637 ) ) ;
#12647=CARTESIAN_POINT ( 'NONE',  ( -3.750000000000011102, 6.495190528383311346, -6.991905250253764414 ) ) ;
#12649=CARTESIAN_POINT ( 'NONE',  ( 1.415196051561583790, -4.795541693661363958, -4.250000000000000000 ) ) ;
#12653=CARTESIAN_POINT ( 'NONE',  ( -3.033343224707664376, 3.753672977998667726, -6.249999998634408804 ) ) ;
#12656=ORIENTED_EDGE ( 'NONE', *, *, #14005, .F. ) ;
#12681=CARTESIAN_POINT ( 'NONE',  ( -7.894787914004613327, -1.222495057920810896E-13, -7.591390474663425536 ) ) ;
#12686=CARTESIAN_POINT ( 'NONE',  ( 5.000000000000000000, -5.773502691896266192, -7.063244554130005071 ) ) ;
#12694=CARTESIAN_POINT ( 'NONE',  ( -4.276409079477644148, -1.261996585732578335, -5.062499998634406140 ) ) ;
#12696=CARTESIAN_POINT ( 'NONE',  ( -1.415196051561583790, 4.795541693661363958, -4.624999997268817609 ) ) ;
#12698=CARTESIAN_POINT ( 'NONE',  ( -0.5711823568785977523, -5.381735091635034607, -5.187499997268819385 ) ) ;
#12703=CARTESIAN_POINT ( 'NONE',  ( -0.5711823568785978633, -5.381735091635035495, -4.187499997268818497 ) ) ;
#12709=CARTESIAN_POINT ( 'NONE',  ( -4.799145180956616130, 0.5093500532425063732, -7.874999998634408804 ) ) ;
#12722=CARTESIAN_POINT ( 'NONE',  ( 2.602085213965210642E-15, 8.660254037844392627, -7.422398894150035176 ) ) ;
#12725=CARTESIAN_POINT ( 'NONE',  ( 3.401574460001763001, -4.209348295687703967, -4.187500000000000888 ) ) ;
#12729=CARTESIAN_POINT ( 'NONE',  ( 4.276409079477644148, 1.261996585732577891, -6.562499998634407028 ) ) ;
#12738=VECTOR ( 'NONE', #6788, 1000.000000000000000 ) ;
#12739=CARTESIAN_POINT ( 'NONE',  ( 7.500000000000000000, -3.157198044629319522, -7.642795354507490480 ) ) ;
#12745=CARTESIAN_POINT ( 'NONE',  ( 2.131511515620586383, 3.916244202832140253, -5.187499998634406140 ) ) ;
#12746=CARTESIAN_POINT ( 'NONE',  ( 7.500000000000000888, 4.330127018922199866, -1.000000000000000888 ) ) ;
#12747=CARTESIAN_POINT ( 'NONE',  ( 7.500000000000003553, -4.330127018922199866, -9.999999999999998224 ) ) ;
#12749=CARTESIAN_POINT ( 'NONE',  ( -2.390265326283148806, -4.391654775818394363, -3.375000000000003109 ) ) ;
#12751=CARTESIAN_POINT ( 'NONE',  ( 2.558993250141106568, -7.638875775591494666, -7.593821156097298797 ) ) ;
#12755=ORIENTED_EDGE ( 'NONE', *, *, #11833, .T. ) ;
#12758=CARTESIAN_POINT ( 'NONE',  ( 7.914984360234579519, -3.818534719232097530, -7.907701344400641652 ) ) ;
#12760=CARTESIAN_POINT ( 'NONE',  ( 2.390265326283148806, 4.391654775818395251, -1.749999997268814722 ) ) ;
#12765=CARTESIAN_POINT ( 'NONE',  ( 3.753672977998667726, 3.033343224707664376, -8.499999998634411469 ) ) ;
#12781=CARTESIAN_POINT ( 'NONE',  ( 3.401574460001763001, -4.209348295687703967, -8.062499997268812280 ) ) ;
#12785=DIRECTION ( 'NONE',  ( 0.000000000000000000, 0.000000000000000000, -1.000000000000000000 ) ) ;
#12786=CARTESIAN_POINT ( 'NONE',  ( 7.500000000000001776, -2.886751345948134873, -7.198902722707430257 ) ) ;
#12791=ORIENTED_EDGE ( 'NONE', *, *, #100, .F. ) ;
#12795=EDGE_CURVE ( 'NONE', #15708, #1389, #6646, .T. ) ;
#12805=CARTESIAN_POINT ( 'NONE',  ( 4.209348295687701302, 3.401574460001765665, -7.937500000000003553 ) ) ;
#12810=CARTESIAN_POINT ( 'NONE',  ( 0.5093500532425063732, 4.799145180956616130, -6.374999998634407028 ) ) ;
#12812=DIRECTION ( 'NONE',  ( 0.000000000000000000, 0.000000000000000000, 1.000000000000000000 ) ) ;
#12815=ORIENTED_EDGE ( 'NONE', *, *, #13324, .T. ) ;
#12817=ADVANCED_FACE ( 'NONE', ( #14157 ), #3015, .T. ) ;
#12823=CARTESIAN_POINT ( 'NONE',  ( 7.894958282449826115, -1.603399432392641266, -7.593838100136975022 ) ) ;
#12824=CARTESIAN_POINT ( 'NONE',  ( -3.753672977998669502, -3.033343224707661712, -3.749999998634410137 ) ) ;
#12827=CARTESIAN_POINT ( 'NONE',  ( -4.799145180956616130, 0.5093500532425063732, -4.874999998634405252 ) ) ;
#12838=ORIENTED_EDGE ( 'NONE', *, *, #2831, .T. ) ;
#12841=EDGE_CURVE ( 'NONE', #13728, #14177, #11396, .T. ) ;
#12850=CARTESIAN_POINT ( 'NONE',  ( 5.000000000000004441, -2.247904837838113790E-16, -6.920263044861760804 ) ) ;
#12852=( BOUNDED_SURFACE ( )  B_SPLINE_SURFACE ( 3, 2, ( 
 ( #14151, #1783, #3080 ),
 ( #3155, #8100, #3625 ),
 ( #3457, #1041, #5976 ),
 ( #2167, #969, #8337 ),
 ( #6053, #1113, #9538 ),
 ( #3, #14539, #2248 ),
 ( #4919, #3699, #11066 ),
 ( #10898, #8644, #9845 ) ),
 .UNSPECIFIED., .F., .F., .T. ) 
 B_SPLINE_SURFACE_WITH_KNOTS ( ( 4, 2, 2, 4 ),
 ( 3, 3 ),
 ( 0.03851319102641418551, 0.04314724750133522302, 0.04546427573879573830, 0.04778130397625625359 ),
 ( 0.000000000000000000, 1.000000000000000000 ),
 .UNSPECIFIED. ) 
 GEOMETRIC_REPRESENTATION_ITEM ( )  RATIONAL_B_SPLINE_SURFACE ( (
 ( 1.000000000000000000, 0.8047781573724569482, 1.000000000000000000),
 ( 1.000000000000000000, 0.8123768202407034567, 1.000000000000000000),
 ( 1.000000000000000000, 0.8190667609308863728, 1.000000000000000000),
 ( 1.000000000000000000, 0.8191933927156080930, 1.000000000000000000),
 ( 1.000000000000000000, 0.8176088169850975751, 1.000000000000000000),
 ( 1.000000000000000000, 0.8122958474541809304, 1.000000000000000000),
 ( 1.000000000000000000, 0.8086309703845759866, 1.000000000000000000),
 ( 1.000000000000000000, 0.8047712409910814380, 1.000000000000000000) ) ) 
 REPRESENTATION_ITEM ( '' )  SURFACE ( )  );
#12853=CARTESIAN_POINT ( 'NONE',  ( -4.799145180956616130, 0.5093500532425063732, -8.124999998634409692 ) ) ;
#12854=CARTESIAN_POINT ( 'NONE',  ( -1.261996585732579224, 4.276409079477648589, 0.6875000013655923059 ) ) ;
#12863=VECTOR ( 'NONE', #8758, 1000.000000000000000 ) ;
#12869=CARTESIAN_POINT ( 'NONE',  ( 4.276409079477644148, 1.261996585732577891, 1.437500001365592972 ) ) ;
#12870=CARTESIAN_POINT ( 'NONE',  ( -4.999999999999849898, 1.272547481429008309, -0.5865974826446477275 ) ) ;
#12875=CARTESIAN_POINT ( 'NONE',  ( 7.499999999999999112, 2.575910028905298077, -0.3641256808890091512 ) ) ;
#12876=CARTESIAN_POINT ( 'NONE',  ( -7.500000000000007994, 4.330127018922187432, -7.564335161054492218 ) ) ;
#12877=CARTESIAN_POINT ( 'NONE',  ( 4.403473400622098133, 6.117907484625860093, 1.852461055645154053E-15 ) ) ;
#12890=CARTESIAN_POINT ( 'NONE',  ( 3.750000000000004441, -6.495190528383289141, 0.000000000000000000 ) ) ;
#12896=CARTESIAN_POINT ( 'NONE',  ( 3.033343224707661712, -3.753672977998669946, -4.749999998634407028 ) ) ;
#12905=CARTESIAN_POINT ( 'NONE',  ( 7.500000000000000000, -1.645076096008604383, -7.030022527230893381 ) ) ;
#12906=CARTESIAN_POINT ( 'NONE',  ( 1.261996585732578113, -4.276409079477644148, -3.562499998634407916 ) ) ;
#12909=CARTESIAN_POINT ( 'NONE',  ( -1.261996585732579224, 4.276409079477648589, -7.062499998634407916 ) ) ;
#12911=LINE ( 'NONE', #15522, #10536 ) ;
#12912=EDGE_CURVE ( 'NONE', #2474, #8373, #9693, .T. ) ;
#12914=VERTEX_POINT ( 'NONE', #4451 ) ;
#12916=CARTESIAN_POINT ( 'NONE',  ( 2.390265326283148806, 4.391654775818395251, -6.875000000000002665 ) ) ;
#12928=CARTESIAN_POINT ( 'NONE',  ( -4.795541693661363958, -1.415196051561583790, -4.500000000000000888 ) ) ;
#12936=CARTESIAN_POINT ( 'NONE',  ( -7.298354728638057232, 4.926141412640825834, -7.913704048099944544 ) ) ;
#12938=CARTESIAN_POINT ( 'NONE',  ( -4.391654775818395251, 2.390265326283148806, -4.625000000000000888 ) ) ;
#12941=( BOUNDED_CURVE ( )  B_SPLINE_CURVE ( 2, ( #3106, #5684, #12938, #7877, #1874, #3176, #15478, #1801, #11647, #10456, #5446 ),
 .UNSPECIFIED., .F., .F. ) 
 B_SPLINE_CURVE_WITH_KNOTS ( ( 3, 2, 2, 2, 2, 3 ),
 ( 0.6545872658012773515, 0.6624999999999999778, 0.6750000000000000444, 0.6875000000000000000, 0.6999999999999999556, 0.7045872658012772849 ),
 .UNSPECIFIED. ) 
 CURVE ( )  GEOMETRIC_REPRESENTATION_ITEM ( )  RATIONAL_B_SPLINE_CURVE ( ( 0.9646335149384803742, 0.9518143178943441196, 1.000000000000000000, 0.9238795325112867385, 1.000000000000000000, 0.9238795325112867385, 1.000000000000000000, 0.9238795325112867385, 1.000000000000000000, 0.9720652146169428409, 0.9646335149384808183 ) ) 
 REPRESENTATION_ITEM ( '' )  );
#12942=CARTESIAN_POINT ( 'NONE',  ( 4.999999999999849010, -1.272547481429013416, -2.961597479913464781 ) ) ;
#12945=CARTESIAN_POINT ( 'NONE',  ( 5.381735091635035495, -0.5711823568785978633, -6.937499997268816720 ) ) ;
#12947=CARTESIAN_POINT ( 'NONE',  ( 4.209348295687701302, 3.401574460001766109, -1.937500000000002665 ) ) ;
#12950=CARTESIAN_POINT ( 'NONE',  ( 7.500000000000001776, 0.000000000000000000, 0.000000000000000000 ) ) ;
#12960=CARTESIAN_POINT ( 'NONE',  ( -7.500000000000005329, 3.988838049906425987, -0.8529248949437673311 ) ) ;
#12961=CARTESIAN_POINT ( 'NONE',  ( -5.000000000000003553, -1.404940523648820476E-14, -8.420263044861757251 ) ) ;
#12968=CARTESIAN_POINT ( 'NONE',  ( 5.000000000000004441, -2.247904837838113790E-16, -2.920263044861759472 ) ) ;
#12970=CARTESIAN_POINT ( 'NONE',  ( -0.5093500532425060401, -4.799145180956616130, -0.6249999986344055847 ) ) ;
#12979=CARTESIAN_POINT ( 'NONE',  ( 3.401574460001763445, -4.209348295687703079, -6.187500000000002665 ) ) ;
#12982=CARTESIAN_POINT ( 'NONE',  ( -3.753672977998669502, -3.033343224707661712, -6.749999998634408804 ) ) ;
#12985=CARTESIAN_POINT ( 'NONE',  ( 4.276409079477644148, 1.261996585732577891, -7.312499998634407916 ) ) ;
#12992=CARTESIAN_POINT ( 'NONE',  ( -4.391654775818395251, 2.390265326283148806, -6.625000000000002665 ) ) ;
#12996=MECHANICAL_DESIGN_GEOMETRIC_PRESENTATION_REPRESENTATION('',(#3967),#4492);
#13008=CARTESIAN_POINT ( 'NONE',  ( 0.6250000000000000000, -8.299410119600885594, -7.298562697733111726 ) ) ;
#13023=CARTESIAN_POINT ( 'NONE',  ( 2.131511515620586383, 3.916244202832140253, 0.5625000013655921949 ) ) ;
#13029=CARTESIAN_POINT ( 'NONE',  ( 4.420982230657666712, -0.5789871446316176007, -0.3789984458506777676 ) ) ;
#13034=CARTESIAN_POINT ( 'NONE',  ( 1.402244460665939663, 4.313165601266486959, -0.4094021847041934281 ) ) ;
#13036=CARTESIAN_POINT ( 'NONE',  ( -5.000000000000000888, 6.123233995736767268E-16, -25.03750572909317285 ) ) ;
#13039=CARTESIAN_POINT ( 'NONE',  ( -7.500000000000005329, 1.854554393013823077, -0.1880126015361750780 ) ) ;
#13049=CARTESIAN_POINT ( 'NONE',  ( 3.916244202832140253, -2.131511515620588160, -1.437499998634406140 ) ) ;
#13055=EDGE_LOOP ( 'NONE', ( #2222, #15210, #4917 ) ) ;
#13065=CARTESIAN_POINT ( 'NONE',  ( -2.131511515620587272, -3.916244202832140253, -6.687499998634407028 ) ) ;
#13070=CARTESIAN_POINT ( 'NONE',  ( 5.381735091635035495, -0.5711823568785978633, 0.9374999999999980016 ) ) ;
#13081=CARTESIAN_POINT ( 'NONE',  ( -5.000000000000004441, -7.530481206757679743E-15, -3.420263044861759916 ) ) ;
#13091=CARTESIAN_POINT ( 'NONE',  ( -2.390265326283148806, -4.391654775818394363, -0.2499999972688168870 ) ) ;
#13099=VERTEX_POINT ( 'NONE', #9927 ) ;
#13104=CARTESIAN_POINT ( 'NONE',  ( 0.5093500532425063732, 4.799145180956616130, -0.1249999986344088321 ) ) ;
#13107=CARTESIAN_POINT ( 'NONE',  ( -1.415196051561583790, 4.795541693661363958, -6.624999997268815832 ) ) ;
#13111=ORIENTED_EDGE ( 'NONE', *, *, #15393, .F. ) ;
#13112=CARTESIAN_POINT ( 'NONE',  ( 5.000000000000000888, 0.000000000000000000, -25.03750572909317285 ) ) ;
#13113=CARTESIAN_POINT ( 'NONE',  ( 5.000000000000092371, 0.7223674278660651149, -2.896799362785969834 ) ) ;
#13124=CARTESIAN_POINT ( 'NONE',  ( -7.500000000000005329, 4.330127018922194537, -0.9999999999999974465 ) ) ;
#13125=CARTESIAN_POINT ( 'NONE',  ( 4.391654775818395251, -2.390265326283149694, -5.125000000000000888 ) ) ;
#13136=CARTESIAN_POINT ( 'NONE',  ( -0.5093500532425060401, -4.799145180956616130, 0.3750000013655915843 ) ) ;
#13139=CARTESIAN_POINT ( 'NONE',  ( 7.847095227763521308, 4.129731495738486302, -7.493596212620240671 ) ) ;
#13142=( BOUNDED_CURVE ( )  B_SPLINE_CURVE ( 2, ( #6766, #2062, #13125, #10330, #3281, #4489, #10640, #8144, #4414, #8227, #11600 ),
 .UNSPECIFIED., .F., .F. ) 
 B_SPLINE_CURVE_WITH_KNOTS ( ( 3, 2, 2, 2, 2, 3 ),
 ( 0.7045872658012772849, 0.7125000000000000222, 0.7249999999999999778, 0.7375000000000000444, 0.7500000000000000000, 0.7545872658012773293 ),
 .UNSPECIFIED. ) 
 CURVE ( )  GEOMETRIC_REPRESENTATION_ITEM ( )  RATIONAL_B_SPLINE_CURVE ( ( 0.9646335149384808183, 0.9518143178943441196, 1.000000000000000000, 0.9238795325112867385, 1.000000000000000000, 0.9238795325112867385, 1.000000000000000000, 0.9238795325112867385, 1.000000000000000000, 0.9720652146169423968, 0.9646335149384803742 ) ) 
 REPRESENTATION_ITEM ( '' )  );
#13147=CARTESIAN_POINT ( 'NONE',  ( -2.131511515620587272, -3.916244202832140253, -3.687499998634407916 ) ) ;
#13148=CARTESIAN_POINT ( 'NONE',  ( 4.795541693661363958, 1.415196051561583790, -5.874999997268814944 ) ) ;
#13150=CARTESIAN_POINT ( 'NONE',  ( 4.276409079477644148, 1.261996585732577891, -8.312499998634407916 ) ) ;
#13154=ADVANCED_FACE ( 'NONE', ( #15192 ), #13883, .F. ) ;
#13160=CARTESIAN_POINT ( 'NONE',  ( 0.5711823568785988625, 5.381735091635026613, -3.687499997268817609 ) ) ;
#13164=CARTESIAN_POINT ( 'NONE',  ( 5.000000000000091482, 0.7223674278660408010, -0.02179936551715794604 ) ) ;
#13168=CARTESIAN_POINT ( 'NONE',  ( 5.000000000000004441, 3.034671531081452754E-15, -0.9202630448617579173 ) ) ;
#13169=CARTESIAN_POINT ( 'NONE',  ( -0.5711823568785977523, -5.381735091635034607, -0.1874999972688185246 ) ) ;
#13177=EDGE_CURVE ( 'NONE', #635, #9146, #2970, .T. ) ;
#13179=CARTESIAN_POINT ( 'NONE',  ( 3.916244202832140253, -2.131511515620588160, -0.4374999986344086933 ) ) ;
#13181=CARTESIAN_POINT ( 'NONE',  ( 4.799145180956616130, -0.5093500532425063732, -0.6249999986344092484 ) ) ;
#13190=VERTEX_POINT ( 'NONE', #6304 ) ;
#13195=EDGE_CURVE ( 'NONE', #14177, #1787, #11220, .T. ) ;
#13197=CARTESIAN_POINT ( 'NONE',  ( -7.914984360234578631, 3.818534719232089980, -7.907701344400643428 ) ) ;
#13198=PLANE ( 'NONE',  #7805 ) ;
#13200=CARTESIAN_POINT ( 'NONE',  ( 4.795541693661363958, 1.415196051561583790, -0.8749999972688139449 ) ) ;
#13203=CARTESIAN_POINT ( 'NONE',  ( 0.5093500532425063732, 4.799145180956616130, -2.124999998634406584 ) ) ;
#13205=CARTESIAN_POINT ( 'NONE',  ( 3.295171437449766927, 7.213553046161560012, -7.590212325761490852 ) ) ;
#13206=ORIENTED_EDGE ( 'NONE', *, *, #7211, .F. ) ;
#13217=CARTESIAN_POINT ( 'NONE',  ( -1.415196051561583790, 4.795541693661363958, -5.624999997268814944 ) ) ;
#13219=CARTESIAN_POINT ( 'NONE',  ( 3.916244202832140253, -2.131511515620588160, -7.437499998634407916 ) ) ;
#13222=CARTESIAN_POINT ( 'NONE',  ( -4.662883599861174844, -0.5303216768924871038, -0.2203019408131941803 ) ) ;
#13233=DIRECTION ( 'NONE',  ( 0.000000000000000000, 0.000000000000000000, 1.000000000000000000 ) ) ;
#13237=CARTESIAN_POINT ( 'NONE',  ( -3.096526599377910305, 6.872473572140717302, -4.269046054161672230E-16 ) ) ;
#13238=B_SPLINE_CURVE_WITH_KNOTS ( 'NONE', 3,
 ( #9021, #13755, #6504, #13925 ),
 .UNSPECIFIED., .F., .F.,
 ( 4, 4 ),
 ( 8.125557066451241256E-17, 0.001452767664617488205 ),
 .UNSPECIFIED. ) ;
#13245=ORIENTED_EDGE ( 'NONE', *, *, #1639, .T. ) ;
#13246=EDGE_LOOP ( 'NONE', ( #15820, #4283, #3252, #2092 ) ) ;
#13247=CARTESIAN_POINT ( 'NONE',  ( -5.088535779736633735, 5.722386535632430160, -7.491772860716511495 ) ) ;
#13248=ORIENTED_EDGE ( 'NONE', *, *, #11048, .F. ) ;
#13253=CARTESIAN_POINT ( 'NONE',  ( 4.276409079477644148, 1.261996585732577891, -0.3124999986344085823 ) ) ;
#13255=CARTESIAN_POINT ( 'NONE',  ( -2.131511515620587272, -3.916244202832140253, -2.937499998634407472 ) ) ;
#13266=CARTESIAN_POINT ( 'NONE',  ( -3.916244202832140253, 2.131511515620587272, -2.187499998634407028 ) ) ;
#13270=CARTESIAN_POINT ( 'NONE',  ( 4.795541693661363958, 1.415196051561583790, -8.874999997268814056 ) ) ;
#13271=CARTESIAN_POINT ( 'NONE',  ( -2.390265326283148806, -4.391654775818394363, -2.375000000000002220 ) ) ;
#13274=DIRECTION ( 'NONE',  ( 1.000000000000000000, 0.000000000000000000, 0.000000000000000000 ) ) ;
#13277=CARTESIAN_POINT ( 'NONE',  ( -4.799145180956616130, 0.5093500532425063732, 0.1250000013655913900 ) ) ;
#13290=DIRECTION ( 'NONE',  ( 1.000000000000000000, 0.000000000000000000, 0.000000000000000000 ) ) ;
#13294=CARTESIAN_POINT ( 'NONE',  ( -1.415196051561583790, 4.795541693661363958, -1.750000000000001554 ) ) ;
#13301=CARTESIAN_POINT ( 'NONE',  ( 7.298354728637884925, -4.926141412640459905, -7.913704048099823751 ) ) ;
#13317=CARTESIAN_POINT ( 'NONE',  ( 0.000000000000000000, 0.000000000000000000, -0.5776712190230133270 ) ) ;
#13322=ADVANCED_FACE ( 'NONE', ( #6712 ), #7384, .F. ) ;
#13323=VERTEX_POINT ( 'NONE', #1766 ) ;
#13324=EDGE_CURVE ( 'NONE', #7414, #635, #2005, .T. ) ;
#13336=CARTESIAN_POINT ( 'NONE',  ( 4.276409079477644148, 1.261996585732577891, 1.687500001365593194 ) ) ;
#13338=CARTESIAN_POINT ( 'NONE',  ( 3.033343224707661712, -3.753672977998669946, -0.7499999986344074721 ) ) ;
#13342=ORIENTED_EDGE ( 'NONE', *, *, #9442, .T. ) ;
#13344=AXIS2_PLACEMENT_3D ( 'NONE', #14491, #8526, #11096 ) ;
#13348=CARTESIAN_POINT ( 'NONE',  ( -0.5711823568785977523, -5.381735091635034607, -1.312500000000000222 ) ) ;
#13353=CARTESIAN_POINT ( 'NONE',  ( -2.131511515620587272, -3.916244202832140253, -1.937499998634406584 ) ) ;
#13358=FACE_OUTER_BOUND ( 'NONE', #4138, .T. ) ;
#13362=CARTESIAN_POINT ( 'NONE',  ( 2.390265326283148806, 4.391654775818395251, -1.749999997268814722 ) ) ;
#13366=CARTESIAN_POINT ( 'NONE',  ( -4.799145180956616130, 0.5093500532425063732, -2.874999998634407472 ) ) ;
#13367=CARTESIAN_POINT ( 'NONE',  ( 0.000000000000000000, 0.000000000000000000, -8.499999999999996447 ) ) ;
#13370=VERTEX_POINT ( 'NONE', #877 ) ;
#13377=ADVANCED_FACE ( 'NONE', ( #2460 ), #8398, .F. ) ;
#13382=CARTESIAN_POINT ( 'NONE',  ( 4.391654775818395251, -2.390265326283149694, -1.125000000000000888 ) ) ;
#13384=CARTESIAN_POINT ( 'NONE',  ( -3.364693435263333310, -3.390744528670103453, -0.1614628718363220472 ) ) ;
#13386=CARTESIAN_POINT ( 'NONE',  ( -1.261996585732579224, 4.276409079477648589, -2.312499998634407028 ) ) ;
#13416=CARTESIAN_POINT ( 'NONE',  ( -1.261996585732579224, 4.276409079477648589, 0.9375000013655925279 ) ) ;
#13418=CARTESIAN_POINT ( 'NONE',  ( -3.916244202832140253, 2.131511515620587272, -3.187499998634407916 ) ) ;
#13425=CARTESIAN_POINT ( 'NONE',  ( -3.753672977998669502, -3.033343224707661712, -2.999999998634409248 ) ) ;
#13432=CARTESIAN_POINT ( 'NONE',  ( -3.401574460001764777, 4.209348295687701302, -1.562499997268814056 ) ) ;
#13436=CARTESIAN_POINT ( 'NONE',  ( -3.916244202832140253, 2.131511515620587272, -5.937499998634407028 ) ) ;
#13444=CYLINDRICAL_SURFACE ( 'NONE', #6578, 5.000000000000000888 ) ;
#13449=CARTESIAN_POINT ( 'NONE',  ( -4.795541693661363958, -1.415196051561583790, -0.5000000000000004441 ) ) ;
#13452=CARTESIAN_POINT ( 'NONE',  ( 4.799145180956616130, -0.5093500532425063732, -2.624999998634407028 ) ) ;
#13454=FACE_OUTER_BOUND ( 'NONE', #3513, .T. ) ;
#13478=ADVANCED_FACE ( 'NONE', ( #10814 ), #13444, .F. ) ;
#13479=EDGE_LOOP ( 'NONE', ( #9941, #4818, #11210, #41 ) ) ;
#13485=CARTESIAN_POINT ( 'NONE',  ( 0.5093500532425063732, 4.799145180956616130, -3.124999998634407916 ) ) ;
#13487=CARTESIAN_POINT ( 'NONE',  ( -1.261996585732579224, 4.276409079477648589, -2.312499998634407028 ) ) ;
#13488=FACE_OUTER_BOUND ( 'NONE', #12578, .T. ) ;
#13496=EDGE_LOOP ( 'NONE', ( #15730, #10372, #15139, #11507, #5270 ) ) ;
#13500=CARTESIAN_POINT ( 'NONE',  ( 0.5093500532425063732, 4.799145180956616130, -4.374999998634405252 ) ) ;
#13508=CARTESIAN_POINT ( 'NONE',  ( -4.209348295687703967, -3.401574460001763001, 0.6875000027311841677 ) ) ;
#13514=CARTESIAN_POINT ( 'NONE',  ( -4.799145180956616130, 0.5093500532425063732, -5.874999998634406140 ) ) ;
#13530=CARTESIAN_POINT ( 'NONE',  ( 4.391654775818395251, -2.390265326283149694, -2.125000000000001776 ) ) ;
#13534=CARTESIAN_POINT ( 'NONE',  ( 3.753672977998667726, 3.033343224707664376, -2.499999998634408804 ) ) ;
#13539=VERTEX_POINT ( 'NONE', #3925 ) ;
#13558=CARTESIAN_POINT ( 'NONE',  ( 2.131511515620586383, 3.916244202832140253, -8.437499998634409692 ) ) ;
#13572=CARTESIAN_POINT ( 'NONE',  ( -0.5093500532425060401, -4.799145180956616130, -3.624999998634407916 ) ) ;
#13576=CARTESIAN_POINT ( 'NONE',  ( 3.916244202832140253, -2.131511515620588160, -3.687499998634407916 ) ) ;
#13589=CARTESIAN_POINT ( 'NONE',  ( 0.5093500532425063732, 4.799145180956616130, -2.374999998634407028 ) ) ;
#13591=CARTESIAN_POINT ( 'NONE',  ( 4.276409079477644148, 1.261996585732577891, -8.562499998634409692 ) ) ;
#13598=CARTESIAN_POINT ( 'NONE',  ( 4.209348295687701302, 3.401574460001765665, -4.812499997268817609 ) ) ;
#13604=B_SPLINE_CURVE_WITH_KNOTS ( 'NONE', 3,
 ( #3114, #4325, #9337, #10469, #12876, #6997 ),
 .UNSPECIFIED., .F., .F.,
 ( 4, 2, 4 ),
 ( -5.145455527297706927E-06, 0.0004153350442917282375, 0.0008358155441107520661 ),
 .UNSPECIFIED. ) ;
#13605=CARTESIAN_POINT ( 'NONE',  ( 3.033343224707661712, -3.753672977998669946, -5.499999998634407916 ) ) ;
#13606=CONICAL_SURFACE ( 'NONE', #8990, 7.500000000000001776, 0.8594454914424796144 ) ;
#13622=CARTESIAN_POINT ( 'NONE',  ( -5.381735091635034607, 0.5711823568785950878, 0.4374999999999975020 ) ) ;
#13628=CARTESIAN_POINT ( 'NONE',  ( 2.131511515620586383, 3.916244202832140253, -4.437499998634405252 ) ) ;
#13654=( NAMED_UNIT ( * ) PLANE_ANGLE_UNIT ( ) SI_UNIT ( $, .RADIAN. ) );
#13657=( BOUNDED_SURFACE ( )  B_SPLINE_SURFACE ( 1, 2, ( 
 ( #13336, #14415, #5758, #14649, #12201, #3341, #5841, #3258, #6081, #8205, #10695, #9627, #13416, #11011, #15630, #2043, #4549, #7064, #15950, #14562, #11888, #4873, #6001, #12048, #4786, #11965, #14331, #8522, #3571, #13104, #6989, #9483, #13253, #8443, #13179, #2115, #8289, #916, #2194, #10777, #15715, #14487, #3409, #8360, #2278, #7145, #1065, #993, #5927, #10849, #15789, #4706, #7230, #10925, #9711, #9138, #13661, #3650, #5334, #6328, #7376, #104, #14050, #14727, #12285, #1222, #2423, #9800, #11245, #9874, #6247, #6170, #10351, #8595, #11093, #29, #4945, #13485, #192, #14805, #11161, #3727, #15278, #10272, #8671, #13572, #11543, #5023, #2503, #13965, #7464, #12369, #9952, #1302, #7931, #14891, #3811, #8759, #7544, #2591, #12445, #1379, #15200, #4115, #4192, #12827, #9063, #2897, #2977, #7847, #12745, #6718, #1771, #1690, #6631, #495, #5419, #11621, #571, #11695, #3144, #2085, #8091, #650, #729, #9528, #3378, #805, #5655, #11777, #9447, #15520, #14457, #8013, #5492, #5574, #15444, #15593, #4512, #10511, #12909, #5800, #8329, #4366, #12985, #10422, #13219, #15357, #1844, #5725, #4590, #2158, #6787, #9218, #9300, #14223, #7107, #10660, #3070, #12009, #13150 ),
 ( #10596, #14378, #1921, #4277, #6870, #2007, #7030, #3304, #4436, #9371, #14296, #3219, #14140, #11930, #8258, #8168, #882, #13070, #6957, #11858, #10739, #15676, #3615, #8560, #4909, #13622, #8402, #11126, #9910, #1032, #14531, #14767, #2320, #6212, #67, #8636, #2758, #3771, #12092, #14693, #13449, #5967, #2389, #10888, #12243, #4670, #14850, #7425, #15829, #2553, #13382, #6129, #4985, #4749, #9669, #4831, #3449, #9594, #1267, #7506, #13294, #960, #7338, #9835, #14607, #7192, #13530, #9755, #3689, #1103, #1184, #2465, #10819, #8716, #8481, #7264, #12330, #3528, #5885, #2236, #15759, #12165, #6043, #10968, #11055, #15910, #5228, #6371, #8958, #2633, #2877, #9118, #7584, #5069, #13869, #1424, #2954, #8874, #1341, #12725, #12649, #13946, #2801, #4170, #3858, #12407, #1664, #12484, #11205, #14025, #6290, #1516, #6527, #3929, #149, #11289, #7758, #4092, #11442, #13778, #6454, #11366, #239, #10001, #7828, #10248, #471, #1588, #15259, #5395, #14938, #7671, #8797, #15088, #4005, #389, #13701, #5158, #6606, #10333, #10088, #15015, #15176, #2713, #11521, #12569, #318, #5308, #10164, #9043, #859, #5779, #10720, #553, #4417, #1824, #14202, #9507, #4572, #12805, #15654 ) ),
 .UNSPECIFIED., .F., .F., .F. ) 
 B_SPLINE_SURFACE_WITH_KNOTS ( ( 2, 2 ),
 ( 3, 2, 2, 2, 2, 2, 2, 2, 2, 2, 2, 2, 2, 2, 2, 2, 2, 2, 2, 2, 2, 2, 2, 2, 2, 2, 2, 2, 2, 2, 2, 2, 2, 2, 2, 2, 2, 2, 2, 2, 2, 2, 2, 2, 2, 2, 2, 2, 2, 2, 2, 2, 2, 2, 2, 2, 2, 2, 2, 2, 2, 2, 2, 2, 2, 2, 2, 2, 2, 2, 2, 2, 2, 2, 2, 2, 2, 2, 2, 2, 3 ),
 ( 0.000000000000000000, 1.000000000000000000 ),
 ( 0.000000000000000000, 0.01250000000000000069, 0.02500000000000000139, 0.03749999999999999861, 0.05000000000000000278, 0.06250000000000000000, 0.07499999999999999722, 0.08749999999999999445, 0.1000000000000000056, 0.1125000000000000028, 0.1250000000000000000, 0.1375000000000000111, 0.1499999999999999944, 0.1625000000000000056, 0.1749999999999999889, 0.1875000000000000000, 0.2000000000000000111, 0.2124999999999999944, 0.2250000000000000056, 0.2374999999999999889, 0.2500000000000000000, 0.2625000000000000111, 0.2750000000000000222, 0.2874999999999999778, 0.2999999999999999889, 0.3125000000000000000, 0.3250000000000000111, 0.3375000000000000222, 0.3499999999999999778, 0.3624999999999999889, 0.3750000000000000000, 0.3875000000000000111, 0.4000000000000000222, 0.4124999999999999778, 0.4249999999999999889, 0.4375000000000000000, 0.4500000000000000111, 0.4625000000000000222, 0.4749999999999999778, 0.4874999999999999889, 0.5000000000000000000, 0.5124999999999999556, 0.5250000000000000222, 0.5374999999999999778, 0.5500000000000000444, 0.5625000000000000000, 0.5749999999999999556, 0.5875000000000000222, 0.5999999999999999778, 0.6125000000000000444, 0.6250000000000000000, 0.6374999999999999556, 0.6500000000000000222, 0.6624999999999999778, 0.6750000000000000444, 0.6875000000000000000, 0.6999999999999999556, 0.7125000000000000222, 0.7249999999999999778, 0.7375000000000000444, 0.7500000000000000000, 0.7624999999999999556, 0.7750000000000000222, 0.7874999999999999778, 0.8000000000000000444, 0.8125000000000000000, 0.8249999999999999556, 0.8375000000000000222, 0.8499999999999999778, 0.8625000000000000444, 0.8750000000000000000, 0.8874999999999999556, 0.9000000000000000222, 0.9124999999999999778, 0.9250000000000000444, 0.9375000000000000000, 0.9499999999999999556, 0.9625000000000000222, 0.9749999999999999778, 0.9875000000000000444, 1.000000000000000000 ),
 .UNSPECIFIED. ) 
 GEOMETRIC_REPRESENTATION_ITEM ( )  RATIONAL_B_SPLINE_SURFACE ( (
 ( 1.000000000000000000, 0.9238795325112867385, 1.000000000000000000, 0.9238795325112867385, 1.000000000000000000, 0.9238795325112867385, 1.000000000000000000, 0.9238795325112867385, 1.000000000000000000, 0.9238795325112867385, 1.000000000000000000, 0.9238795325112867385, 1.000000000000000000, 0.9238795325112867385, 1.000000000000000000, 0.9238795325112867385, 1.000000000000000000, 0.9238795325112867385, 1.000000000000000000, 0.9238795325112867385, 1.000000000000000000, 0.9238795325112867385, 1.000000000000000000, 0.9238795325112867385, 1.000000000000000000, 0.9238795325112867385, 1.000000000000000000, 0.9238795325112867385, 1.000000000000000000, 0.9238795325112867385, 1.000000000000000000, 0.9238795325112867385, 1.000000000000000000, 0.9238795325112867385, 1.000000000000000000, 0.9238795325112867385, 1.000000000000000000, 0.9238795325112867385, 1.000000000000000000, 0.9238795325112867385, 1.000000000000000000, 0.9238795325112867385, 1.000000000000000000, 0.9238795325112867385, 1.000000000000000000, 0.9238795325112867385, 1.000000000000000000, 0.9238795325112867385, 1.000000000000000000, 0.9238795325112867385, 1.000000000000000000, 0.9238795325112867385, 1.000000000000000000, 0.9238795325112867385, 1.000000000000000000, 0.9238795325112867385, 1.000000000000000000, 0.9238795325112867385, 1.000000000000000000, 0.9238795325112867385, 1.000000000000000000, 0.9238795325112867385, 1.000000000000000000, 0.9238795325112867385, 1.000000000000000000, 0.9238795325112867385, 1.000000000000000000, 0.9238795325112867385, 1.000000000000000000, 0.9238795325112867385, 1.000000000000000000, 0.9238795325112867385, 1.000000000000000000, 0.9238795325112867385, 1.000000000000000000, 0.9238795325112867385, 1.000000000000000000, 0.9238795325112867385, 1.000000000000000000, 0.9238795325112867385, 1.000000000000000000, 0.9238795325112867385, 1.000000000000000000, 0.9238795325112867385, 1.000000000000000000, 0.9238795325112867385, 1.000000000000000000, 0.9238795325112867385, 1.000000000000000000, 0.9238795325112867385, 1.000000000000000000, 0.9238795325112867385, 1.000000000000000000, 0.9238795325112867385, 1.000000000000000000, 0.9238795325112867385, 1.000000000000000000, 0.9238795325112867385, 1.000000000000000000, 0.9238795325112867385, 1.000000000000000000, 0.9238795325112867385, 1.000000000000000000, 0.9238795325112867385, 1.000000000000000000, 0.9238795325112867385, 1.000000000000000000, 0.9238795325112867385, 1.000000000000000000, 0.9238795325112867385, 1.000000000000000000, 0.9238795325112867385, 1.000000000000000000, 0.9238795325112867385, 1.000000000000000000, 0.9238795325112867385, 1.000000000000000000, 0.9238795325112867385, 1.000000000000000000, 0.9238795325112867385, 1.000000000000000000, 0.9238795325112867385, 1.000000000000000000, 0.9238795325112867385, 1.000000000000000000, 0.9238795325112867385, 1.000000000000000000, 0.9238795325112867385, 1.000000000000000000, 0.9238795325112867385, 1.000000000000000000, 0.9238795325112867385, 1.000000000000000000, 0.9238795325112867385, 1.000000000000000000, 0.9238795325112867385, 1.000000000000000000, 0.9238795325112867385, 1.000000000000000000, 0.9238795325112867385, 1.000000000000000000, 0.9238795325112867385, 1.000000000000000000, 0.9238795325112867385, 1.000000000000000000, 0.9238795325112867385, 1.000000000000000000, 0.9238795325112867385, 1.000000000000000000, 0.9238795325112867385, 1.000000000000000000, 0.9238795325112867385, 1.000000000000000000, 0.9238795325112867385, 1.000000000000000000, 0.9238795325112867385, 1.000000000000000000, 0.9238795325112867385, 1.000000000000000000, 0.9238795325112867385, 1.000000000000000000),
 ( 1.000000000000000000, 0.9238795325112867385, 1.000000000000000000, 0.9238795325112867385, 1.000000000000000000, 0.9238795325112867385, 1.000000000000000000, 0.9238795325112867385, 1.000000000000000000, 0.9238795325112867385, 1.000000000000000000, 0.9238795325112867385, 1.000000000000000000, 0.9238795325112867385, 1.000000000000000000, 0.9238795325112867385, 1.000000000000000000, 0.9238795325112867385, 1.000000000000000000, 0.9238795325112867385, 1.000000000000000000, 0.9238795325112867385, 1.000000000000000000, 0.9238795325112867385, 1.000000000000000000, 0.9238795325112867385, 1.000000000000000000, 0.9238795325112867385, 1.000000000000000000, 0.9238795325112867385, 1.000000000000000000, 0.9238795325112867385, 1.000000000000000000, 0.9238795325112867385, 1.000000000000000000, 0.9238795325112867385, 1.000000000000000000, 0.9238795325112867385, 1.000000000000000000, 0.9238795325112867385, 1.000000000000000000, 0.9238795325112867385, 1.000000000000000000, 0.9238795325112867385, 1.000000000000000000, 0.9238795325112867385, 1.000000000000000000, 0.9238795325112867385, 1.000000000000000000, 0.9238795325112867385, 1.000000000000000000, 0.9238795325112867385, 1.000000000000000000, 0.9238795325112867385, 1.000000000000000000, 0.9238795325112867385, 1.000000000000000000, 0.9238795325112867385, 1.000000000000000000, 0.9238795325112867385, 1.000000000000000000, 0.9238795325112867385, 1.000000000000000000, 0.9238795325112867385, 1.000000000000000000, 0.9238795325112867385, 1.000000000000000000, 0.9238795325112867385, 1.000000000000000000, 0.9238795325112867385, 1.000000000000000000, 0.9238795325112867385, 1.000000000000000000, 0.9238795325112867385, 1.000000000000000000, 0.9238795325112867385, 1.000000000000000000, 0.9238795325112867385, 1.000000000000000000, 0.9238795325112867385, 1.000000000000000000, 0.9238795325112867385, 1.000000000000000000, 0.9238795325112867385, 1.000000000000000000, 0.9238795325112867385, 1.000000000000000000, 0.9238795325112867385, 1.000000000000000000, 0.9238795325112867385, 1.000000000000000000, 0.9238795325112867385, 1.000000000000000000, 0.9238795325112867385, 1.000000000000000000, 0.9238795325112867385, 1.000000000000000000, 0.9238795325112867385, 1.000000000000000000, 0.9238795325112867385, 1.000000000000000000, 0.9238795325112867385, 1.000000000000000000, 0.9238795325112867385, 1.000000000000000000, 0.9238795325112867385, 1.000000000000000000, 0.9238795325112867385, 1.000000000000000000, 0.9238795325112867385, 1.000000000000000000, 0.9238795325112867385, 1.000000000000000000, 0.9238795325112867385, 1.000000000000000000, 0.9238795325112867385, 1.000000000000000000, 0.9238795325112867385, 1.000000000000000000, 0.9238795325112867385, 1.000000000000000000, 0.9238795325112867385, 1.000000000000000000, 0.9238795325112867385, 1.000000000000000000, 0.9238795325112867385, 1.000000000000000000, 0.9238795325112867385, 1.000000000000000000, 0.9238795325112867385, 1.000000000000000000, 0.9238795325112867385, 1.000000000000000000, 0.9238795325112867385, 1.000000000000000000, 0.9238795325112867385, 1.000000000000000000, 0.9238795325112867385, 1.000000000000000000, 0.9238795325112867385, 1.000000000000000000, 0.9238795325112867385, 1.000000000000000000, 0.9238795325112867385, 1.000000000000000000, 0.9238795325112867385, 1.000000000000000000, 0.9238795325112867385, 1.000000000000000000, 0.9238795325112867385, 1.000000000000000000, 0.9238795325112867385, 1.000000000000000000, 0.9238795325112867385, 1.000000000000000000, 0.9238795325112867385, 1.000000000000000000, 0.9238795325112867385, 1.000000000000000000, 0.9238795325112867385, 1.000000000000000000) ) ) 
 REPRESENTATION_ITEM ( '' )  SURFACE ( )  );
#13661=CARTESIAN_POINT ( 'NONE',  ( -4.276409079477644148, -1.261996585732578335, -1.812499998634406584 ) ) ;
#13662=SHAPE_DEFINITION_REPRESENTATION ( #15846, #3173 ) ;
#13663=CARTESIAN_POINT ( 'NONE',  ( -3.033343224707664376, 3.753672977998667726, -6.249999998634408804 ) ) ;
#13667=CARTESIAN_POINT ( 'NONE',  ( -7.500000000000005329, 2.886751345948128655, -7.198902722707430257 ) ) ;
#13674=CARTESIAN_POINT ( 'NONE',  ( 1.261996585732578113, -4.276409079477644148, -5.812499998634406140 ) ) ;
#13677=CARTESIAN_POINT ( 'NONE',  ( 1.261996585732578113, -4.276409079477644148, -7.562499998634407916 ) ) ;
#13681=CARTESIAN_POINT ( 'NONE',  ( 4.391654775818395251, -2.390265326283149694, -4.999999997268817609 ) ) ;
#13687=CARTESIAN_POINT ( 'NONE',  ( -1.261996585732579224, 4.276409079477648589, -7.062499998634407916 ) ) ;
#13694=EDGE_CURVE ( 'NONE', #4036, #15708, #1837, .T. ) ;
#13701=CARTESIAN_POINT ( 'NONE',  ( -4.795541693661363958, -1.415196051561583790, -6.500000000000002665 ) ) ;
#13705=CARTESIAN_POINT ( 'NONE',  ( -1.261996585732579224, 4.276409079477648589, -1.312499998634406140 ) ) ;
#13708=ORIENTED_EDGE ( 'NONE', *, *, #7005, .T. ) ;
#13718=CARTESIAN_POINT ( 'NONE',  ( -3.753672977998669502, -3.033343224707661712, -0.7499999986344074721 ) ) ;
#13719=CARTESIAN_POINT ( 'NONE',  ( 0.5789871446316211534, 4.420982230657665824, -0.3789984458506777676 ) ) ;
#13728=VERTEX_POINT ( 'NONE', #11832 ) ;
#13735=CARTESIAN_POINT ( 'NONE',  ( 7.894787914004607998, -0.7647108141804138670, -7.591390474663419319 ) ) ;
#13736=CARTESIAN_POINT ( 'NONE',  ( -5.000000000000004441, -1.011557177027151181E-15, -4.420263044861760804 ) ) ;
#13739=CARTESIAN_POINT ( 'NONE',  ( -3.753672977998669946, -3.033343224707661712, -6.999999998634408804 ) ) ;
#13752=CARTESIAN_POINT ( 'NONE',  ( 3.033343224707661712, -3.753672977998669502, -5.749999998634407916 ) ) ;
#13753=B_SPLINE_CURVE_WITH_KNOTS ( 'NONE', 3,
 ( #5981, #13237, #14544, #3393, #7124, #9688 ),
 .UNSPECIFIED., .F., .F.,
 ( 4, 2, 4 ),
 ( 0.004444412883774334112, 0.006655097293744433734, 0.008865781703714532488 ),
 .UNSPECIFIED. ) ;
#13755=CARTESIAN_POINT ( 'NONE',  ( 4.817610911465698642, 0.9367903645274751057, -0.07999226725963382023 ) ) ;
#13759=CARTESIAN_POINT ( 'NONE',  ( -4.391654775818395251, 2.390265326283148806, -5.499999997268814944 ) ) ;
#13766=CARTESIAN_POINT ( 'NONE',  ( 4.276409079477644148, 1.261996585732577891, -8.312499998634407916 ) ) ;
#13768=EDGE_LOOP ( 'NONE', ( #7838, #14736, #9227 ) ) ;
#13774=CARTESIAN_POINT ( 'NONE',  ( -3.280815508853482054, -7.221948645665451139, -7.591546097228400569 ) ) ;
#13775=CARTESIAN_POINT ( 'NONE',  ( -3.295171437451513974, -7.213553046160526172, -7.590212325761485523 ) ) ;
#13778=CARTESIAN_POINT ( 'NONE',  ( -4.209348295687703967, -3.401574460001763001, -5.437500000000002665 ) ) ;
#13784=CARTESIAN_POINT ( 'NONE',  ( 1.261996585732578113, -4.276409079477644148, -7.812499998634407916 ) ) ;
#13788=EDGE_LOOP ( 'NONE', ( #9679, #1697, #15215, #9415, #15856 ) ) ;
#13795=CARTESIAN_POINT ( 'NONE',  ( -4.276409079477644148, -1.261996585732578335, -0.8124999986344055847 ) ) ;
#13805=CARTESIAN_POINT ( 'NONE',  ( -4.795541693661363958, -1.415196051561583790, -3.499999999999999556 ) ) ;
#13816=AXIS2_PLACEMENT_3D ( 'NONE', #7041, #6969, #4449 ) ;
#13820=CARTESIAN_POINT ( 'NONE',  ( 5.000000000000000888, 0.000000000000000000, -25.03750572909317285 ) ) ;
#13822=EDGE_CURVE ( 'NONE', #1389, #4036, #7529, .T. ) ;
#13826=CONICAL_SURFACE ( 'NONE', #10738, 10.39117206796836079, 1.221730476396047926 ) ;
#13827=CARTESIAN_POINT ( 'NONE',  ( -4.276409079477644148, -1.261996585732578335, -7.062499998634407916 ) ) ;
#13831=CARTESIAN_POINT ( 'NONE',  ( 0.000000000000000000, 0.000000000000000000, -25.03750572909317285 ) ) ;
#13835=CARTESIAN_POINT ( 'NONE',  ( -4.209348295687703079, -3.401574460001763445, -7.437500000000004441 ) ) ;
#13839=CARTESIAN_POINT ( 'NONE',  ( 0.5093500532425063732, 4.799145180956616130, -5.374999998634405252 ) ) ;
#13842=CARTESIAN_POINT ( 'NONE',  ( 1.415196051561583790, -4.795541693661363958, -5.124999997268817609 ) ) ;
#13848=CARTESIAN_POINT ( 'NONE',  ( 5.381735091635035495, -0.5711823568785978633, -1.937499997268816276 ) ) ;
#13855=CARTESIAN_POINT ( 'NONE',  ( 7.500000000000002665, -3.608439182435168036, -7.298562697733106397 ) ) ;
#13866=CARTESIAN_POINT ( 'NONE',  ( -3.093533885184382104, -6.874201416485830940, -7.446478553994769989 ) ) ;
#13867=CARTESIAN_POINT ( 'NONE',  ( 5.000000000000004441, -2.247904837838113790E-16, -6.045263047592945860 ) ) ;
#13869=CARTESIAN_POINT ( 'NONE',  ( 2.390265326283148806, 4.391654775818395251, -3.875000000000000000 ) ) ;
#13873=CARTESIAN_POINT ( 'NONE',  ( -3.916244202832140253, 2.131511515620587272, -6.187499998634407028 ) ) ;
#13881=ORIENTED_EDGE ( 'NONE', *, *, #12912, .T. ) ;
#13883=CYLINDRICAL_SURFACE ( 'NONE', #14084, 5.000000000000000888 ) ;
#13886=DIRECTION ( 'NONE',  ( 0.000000000000000000, -1.000000000000000000, 0.000000000000000000 ) ) ;
#13887=( GEOMETRIC_REPRESENTATION_CONTEXT ( 3 ) GLOBAL_UNCERTAINTY_ASSIGNED_CONTEXT ( ( #6613 ) ) GLOBAL_UNIT_ASSIGNED_CONTEXT ( ( #4813, #3598, #12073 ) ) REPRESENTATION_CONTEXT ( 'NONE', 'WORKASPACE' ) );
#13888=CARTESIAN_POINT ( 'NONE',  ( 2.131511515620586383, 3.916244202832140253, -2.187499998634407028 ) ) ;
#13910=CARTESIAN_POINT ( 'NONE',  ( 7.907996613752301229, 3.055722423191985726, -7.792112796859421486 ) ) ;
#13912=CARTESIAN_POINT ( 'NONE',  ( -3.401574460001765221, 4.209348295687701302, -5.687500000000003553 ) ) ;
#13913=CARTESIAN_POINT ( 'NONE',  ( -0.5093500532425060401, -4.799145180956616130, -3.874999998634408360 ) ) ;
#13921=CARTESIAN_POINT ( 'NONE',  ( -1.261996585732579224, 4.276409079477648589, -6.312499998634407028 ) ) ;
#13924=CARTESIAN_POINT ( 'NONE',  ( 4.795541693661363958, 1.415196051561583790, -4.874999997268817609 ) ) ;
#13925=CARTESIAN_POINT ( 'NONE',  ( 4.631580223510930239, 1.444531747605005878E-11, -0.2579703047231843294 ) ) ;
#13927=CARTESIAN_POINT ( 'NONE',  ( -2.390265326283148806, -4.391654775818394363, -2.249999997268815388 ) ) ;
#13933=CARTESIAN_POINT ( 'NONE',  ( -3.753672977998669946, -3.033343224707661712, -6.749999998634408804 ) ) ;
#13946=CARTESIAN_POINT ( 'NONE',  ( -0.5711823568785978633, -5.381735091635035495, -4.312500000000000000 ) ) ;
#13950=CARTESIAN_POINT ( 'NONE',  ( 1.261996585732578113, -4.276409079477644148, -4.812499998634405252 ) ) ;
#13952=CARTESIAN_POINT ( 'NONE',  ( 7.549006887134069643, -4.358421158401204032, -7.700127545397315032 ) ) ;
#13959=ORIENTED_EDGE ( 'NONE', *, *, #12641, .F. ) ;
#13961=CARTESIAN_POINT ( 'NONE',  ( 7.908217798048329250, 3.084840533507072102, -7.795645399445197299 ) ) ;
#13962=CARTESIAN_POINT ( 'NONE',  ( -3.916244202832140253, 2.131511515620587272, -1.937499998634406584 ) ) ;
#13965=CARTESIAN_POINT ( 'NONE',  ( -4.799145180956616130, 0.5093500532425063732, -3.874999998634404363 ) ) ;
#13966=CARTESIAN_POINT ( 'NONE',  ( -0.6250000000000003331, -8.299410119600885594, -7.298562697733111726 ) ) ;
#13972=CARTESIAN_POINT ( 'NONE',  ( 2.325424218456833003, -7.317669739338271917, -7.030005583190793494 ) ) ;
#13981=CARTESIAN_POINT ( 'NONE',  ( -4.999999999999849898, 1.272547481429008309, -1.461597479913463005 ) ) ;
#13982=B_SPLINE_CURVE_WITH_KNOTS ( 'NONE', 3,
 ( #7754, #8794, #146, #1585, #13774, #6523, #3926, #5224, #11439, #14847 ),
 .UNSPECIFIED., .F., .F.,
 ( 4, 2, 2, 2, 4 ),
 ( 0.000000000000000000, 0.002305503304226489900, 0.004611006608452982401, 0.006916509912679474036, 0.009222013216905966537 ),
 .UNSPECIFIED. ) ;
#13984=CARTESIAN_POINT ( 'NONE',  ( 5.000000000000095923, 0.7223674278660565662, -6.021799365517157554 ) ) ;
#13985=( BOUNDED_CURVE ( )  B_SPLINE_CURVE ( 2, ( #15865, #3726, #4785, #8670, #5925, #14647, #15221, #6563, #2590, #7543, #13736 ),
 .UNSPECIFIED., .F., .F. ) 
 B_SPLINE_CURVE_WITH_KNOTS ( ( 3, 2, 2, 2, 2, 3 ),
 ( 0.5045872658012773293, 0.5124999999999999556, 0.5250000000000000222, 0.5374999999999999778, 0.5500000000000000444, 0.5545872658012773737 ),
 .UNSPECIFIED. ) 
 CURVE ( )  GEOMETRIC_REPRESENTATION_ITEM ( )  RATIONAL_B_SPLINE_CURVE ( ( 0.9646335149384803742, 0.9518143178943441196, 1.000000000000000000, 0.9238795325112867385, 1.000000000000000000, 0.9238795325112867385, 1.000000000000000000, 0.9238795325112867385, 1.000000000000000000, 0.9720652146169423968, 0.9646335149384803742 ) ) 
 REPRESENTATION_ITEM ( '' )  );
#13987=CARTESIAN_POINT ( 'NONE',  ( -0.5093500532425060401, -4.799145180956616130, 1.125000001365592306 ) ) ;
#13993=CARTESIAN_POINT ( 'NONE',  ( -5.000000000000091482, -0.7223674278660691117, -1.521799365517154667 ) ) ;
#13999=CARTESIAN_POINT ( 'NONE',  ( 4.391654775818395251, -2.390265326283149694, -4.999999997268817609 ) ) ;
#14000=CARTESIAN_POINT ( 'NONE',  ( -4.795541693661363958, -1.415196051561583790, -8.374999997268814056 ) ) ;
#14002=CARTESIAN_POINT ( 'NONE',  ( 1.415196051561583790, -4.795541693661363958, -7.124999997268815832 ) ) ;
#14005=EDGE_CURVE ( 'NONE', #2401, #9162, #1382, .T. ) ;
#14011=CARTESIAN_POINT ( 'NONE',  ( -2.131511515620587272, -3.916244202832140253, -6.687499998634407028 ) ) ;
#14016=ORIENTED_EDGE ( 'NONE', *, *, #10103, .F. ) ;
#14024=CARTESIAN_POINT ( 'NONE',  ( -7.703920929261759198, -4.447860822324870789, -7.917989418073290153 ) ) ;
#14025=CARTESIAN_POINT ( 'NONE',  ( 0.5711823568785989735, 5.381735091635026613, -4.812500000000000000 ) ) ;
#14027=EDGE_CURVE ( 'NONE', #13323, #2517, #12382, .T. ) ;
#14032=CARTESIAN_POINT ( 'NONE',  ( -1.261996585732579224, 4.276409079477648589, -8.312499998634407916 ) ) ;
#14046=CARTESIAN_POINT ( 'NONE',  ( 7.922811941611899833, 4.628808333142396592, -8.057670691780701944 ) ) ;
#14047=CARTESIAN_POINT ( 'NONE',  ( 1.261996585732578113, -4.276409079477644148, -5.562499998634406140 ) ) ;
#14050=CARTESIAN_POINT ( 'NONE',  ( 2.131511515620586383, 3.916244202832140253, -2.187499998634407028 ) ) ;
#14051=CARTESIAN_POINT ( 'NONE',  ( 10.39117206796836079, 0.000000000000000000, -8.499999999999996447 ) ) ;
#14058=CARTESIAN_POINT ( 'NONE',  ( 4.795541693661363958, 1.415196051561583790, -7.000000000000002665 ) ) ;
#14062=DIRECTION ( 'NONE',  ( 0.000000000000000000, 0.000000000000000000, 1.000000000000000000 ) ) ;
#14070=CARTESIAN_POINT ( 'NONE',  ( 4.795541693661363958, 1.415196051561583790, -1.874999997268814944 ) ) ;
#14075=CARTESIAN_POINT ( 'NONE',  ( 5.000000000000095923, 0.7223674278660565662, -7.896799362785968945 ) ) ;
#14076=LINE ( 'NONE', #1947, #4037 ) ;
#14084=AXIS2_PLACEMENT_3D ( 'NONE', #2892, #1680, #4107 ) ;
#14095=CARTESIAN_POINT ( 'NONE',  ( -1.415196051561583790, 4.795541693661363958, -7.624999997268816720 ) ) ;
#14101=CARTESIAN_POINT ( 'NONE',  ( 4.504907258964289340, -0.3910024795134889319, -0.3378236062164368114 ) ) ;
#14103=CARTESIAN_POINT ( 'NONE',  ( 6.902527771671632451, 4.675077770780897701, -0.7026937717022812002 ) ) ;
#14104=ORIENTED_EDGE ( 'NONE', *, *, #11570, .F. ) ;
#14106=ORIENTED_EDGE ( 'NONE', *, *, #13195, .T. ) ;
#14107=ORIENTED_EDGE ( 'NONE', *, *, #4867, .F. ) ;
#14112=EDGE_CURVE ( 'NONE', #3896, #15071, #442, .T. ) ;
#14116=CARTESIAN_POINT ( 'NONE',  ( -7.922281120364393914, -4.573931137438277617, -8.047472243342932430 ) ) ;
#14123=CARTESIAN_POINT ( 'NONE',  ( -3.753672977998669946, -3.033343224707661712, -4.999999998634407028 ) ) ;
#14126=ORIENTED_EDGE ( 'NONE', *, *, #7190, .T. ) ;
#14132=ORIENTED_EDGE ( 'NONE', *, *, #12398, .F. ) ;
#14135=EDGE_CURVE ( 'NONE', #5622, #1601, #14326, .T. ) ;
#14136=CARTESIAN_POINT ( 'NONE',  ( 0.000000000000000000, 0.000000000000000000, -25.03750572909317285 ) ) ;
#14137=CARTESIAN_POINT ( 'NONE',  ( 3.916244202832140253, -2.131511515620588160, -5.437499998634406140 ) ) ;
#14138=CARTESIAN_POINT ( 'NONE',  ( -3.401574460001765221, 4.209348295687701302, -5.562499997268814056 ) ) ;
#14140=CARTESIAN_POINT ( 'NONE',  ( -1.415196051561583790, 4.795541693661363958, 1.249999999999997558 ) ) ;
#14151=CARTESIAN_POINT ( 'NONE',  ( -7.500000000000003553, 4.730921838224047882, -7.493596905200506697 ) ) ;
#14155=B_SPLINE_CURVE_WITH_KNOTS ( 'NONE', 3,
 ( #496, #10352, #6473, #12591, #10105, #11385, #4193, #13966, #7848 ),
 .UNSPECIFIED., .F., .F.,
 ( 4, 2, 1, 2, 4 ),
 ( 0.000000000000000000, 0.002165063509461097931, 0.004330127018922195863, 0.006495190528383293360, 0.008660254037844391725 ),
 .UNSPECIFIED. ) ;
#14157=FACE_OUTER_BOUND ( 'NONE', #4882, .T. ) ;
#14158=AXIS2_PLACEMENT_3D ( 'NONE', #12486, #6373, #1519 ) ;
#14160=EDGE_CURVE ( 'NONE', #5937, #2247, #12941, .T. ) ;
#14168=CARTESIAN_POINT ( 'NONE',  ( -5.000000000000002665, -1.404940523648820476E-14, -7.420263044861759028 ) ) ;
#14169=CARTESIAN_POINT ( 'NONE',  ( -4.276409079477644148, -1.261996585732578335, 0.9375000013655925279 ) ) ;
#14171=EDGE_LOOP ( 'NONE', ( #7513, #8178, #6219, #3273, #15004, #15264, #12838, #15559, #6217, #11090, #11867, #7057, #6706, #12613, #1891, #2921, #7328, #8116, #3866, #6385, #14104, #2437 ) ) ;
#14174=CARTESIAN_POINT ( 'NONE',  ( -7.970070017554224506, 4.546953124339779606, -8.057670357645367432 ) ) ;
#14177=VERTEX_POINT ( 'NONE', #1719 ) ;
#14182=CARTESIAN_POINT ( 'NONE',  ( 2.390265326283148806, 4.391654775818395251, -7.749999997268816720 ) ) ;
#14184=CARTESIAN_POINT ( 'NONE',  ( 2.390265326283148806, 4.391654775818395251, -1.875000000000001776 ) ) ;
#14202=CARTESIAN_POINT ( 'NONE',  ( -1.415196051561583790, 4.795541693661363958, -7.750000000000003553 ) ) ;
#14206=CARTESIAN_POINT ( 'NONE',  ( -3.033343224707664376, 3.753672977998667726, 1.000000001365594082 ) ) ;
#14212=ORIENTED_EDGE ( 'NONE', *, *, #2887, .F. ) ;
#14217=ORIENTED_EDGE ( 'NONE', *, *, #10156, .F. ) ;
#14220=CARTESIAN_POINT ( 'NONE',  ( 3.033343224707661712, -3.753672977998669502, -6.499999998634408804 ) ) ;
#14223=CARTESIAN_POINT ( 'NONE',  ( -3.033343224707664376, 3.753672977998667726, -7.999999998634409692 ) ) ;
#14243=CARTESIAN_POINT ( 'NONE',  ( -3.753672977998669946, -3.033343224707661712, -7.999999998634409692 ) ) ;
#14244=CARTESIAN_POINT ( 'NONE',  ( 2.131511515620586383, 3.916244202832140253, -0.4374999986344086933 ) ) ;
#14246=ORIENTED_EDGE ( 'NONE', *, *, #14819, .T. ) ;
#14253=CARTESIAN_POINT ( 'NONE',  ( 0.000000000000000000, 0.000000000000000000, -9.999999999999998224 ) ) ;
#14255=CARTESIAN_POINT ( 'NONE',  ( 3.033343224707661712, -3.753672977998669946, 1.250000001365594304 ) ) ;
#14281=CARTESIAN_POINT ( 'NONE',  ( 3.033343224707661712, -3.753672977998669946, -1.499999998634408138 ) ) ;
#14282=ORIENTED_EDGE ( 'NONE', *, *, #8326, .T. ) ;
#14286=( BOUNDED_CURVE ( )  B_SPLINE_CURVE ( 2, ( #14168, #3096, #11566, #11483, #5356, #10532, #15223, #1864, #6809, #14075, #11718 ),
 .UNSPECIFIED., .F., .F. ) 
 B_SPLINE_CURVE_WITH_KNOTS ( ( 3, 2, 2, 2, 2, 3 ),
 ( 0.8545872658012773071, 0.8625000000000000444, 0.8750000000000000000, 0.8874999999999999556, 0.9000000000000000222, 0.9045872658012773515 ),
 .UNSPECIFIED. ) 
 CURVE ( )  GEOMETRIC_REPRESENTATION_ITEM ( )  RATIONAL_B_SPLINE_CURVE ( ( 0.9646335149384808183, 0.9518143178943441196, 1.000000000000000000, 0.9238795325112867385, 1.000000000000000000, 0.9238795325112867385, 1.000000000000000000, 0.9238795325112867385, 1.000000000000000000, 0.9720652146169423968, 0.9646335149384803742 ) ) 
 REPRESENTATION_ITEM ( '' )  );
#14290=CARTESIAN_POINT ( 'NONE',  ( 7.499999999999654499, 3.105728215500202172, -7.659336188854535266 ) ) ;
#14292=CARTESIAN_POINT ( 'NONE',  ( -3.916244202832140253, 2.131511515620587272, -5.937499998634407028 ) ) ;
#14293=CARTESIAN_POINT ( 'NONE',  ( 2.390265326283148806, 4.391654775818395251, -5.749999997268814944 ) ) ;
#14294=EDGE_CURVE ( 'NONE', #1787, #1633, #7635, .T. ) ;
#14296=CARTESIAN_POINT ( 'NONE',  ( -4.391654775818395251, 2.390265326283148806, 1.374999999999997780 ) ) ;
#14300=EDGE_LOOP ( 'NONE', ( #13881, #13708, #12018, #11042 ) ) ;
#14302=CARTESIAN_POINT ( 'NONE',  ( 7.779103221381269861, -4.168986698926033796, -7.929128246061908136 ) ) ;
#14305=CARTESIAN_POINT ( 'NONE',  ( 7.500000000000000000, -3.988190556646209028, -0.8526458641284334616 ) ) ;
#14320=ORIENTED_EDGE ( 'NONE', *, *, #15781, .T. ) ;
#14322=CARTESIAN_POINT ( 'NONE',  ( -4.406466114817408020, 6.116179640279713503, -7.446478553995123484 ) ) ;
#14326=CIRCLE ( 'NONE', #5304, 7.500000000000001776 ) ;
#14329=EDGE_CURVE ( 'NONE', #1925, #2616, #5997, .T. ) ;
#14330=CARTESIAN_POINT ( 'NONE',  ( -2.390265326283148806, -4.391654775818394363, -3.249999997268816276 ) ) ;
#14331=CARTESIAN_POINT ( 'NONE',  ( -3.916244202832140253, 2.131511515620587272, 0.06250000136559172303 ) ) ;
#14333=CARTESIAN_POINT ( 'NONE',  ( -4.795541693661363958, -1.415196051561583790, -6.374999997268815832 ) ) ;
#14335=CARTESIAN_POINT ( 'NONE',  ( 5.000000000000004441, -2.247904837838113790E-16, -2.045263047592944528 ) ) ;
#14340=CARTESIAN_POINT ( 'NONE',  ( 4.795541693661363958, 1.415196051561583790, -2.874999997268815832 ) ) ;
#14342=ORIENTED_EDGE ( 'NONE', *, *, #2127, .F. ) ;
#14360=CARTESIAN_POINT ( 'NONE',  ( -4.276409079477644148, -1.261996585732578335, 1.187500001365592750 ) ) ;
#14362=CARTESIAN_POINT ( 'NONE',  ( 5.147825380264579920, 5.688155668807426402, -7.450218641349906079 ) ) ;
#14367=CARTESIAN_POINT ( 'NONE',  ( 2.390265326283148806, 4.391654775818395251, -7.875000000000003553 ) ) ;
#14371=CARTESIAN_POINT ( 'NONE',  ( -4.799145180956616130, 0.5093500532425063732, -7.874999998634408804 ) ) ;
#14372=CARTESIAN_POINT ( 'NONE',  ( -4.799145180956616130, 0.5093500532425063732, -5.874999998634406140 ) ) ;
#14378=CARTESIAN_POINT ( 'NONE',  ( 5.381735091635035495, -0.5711823568785978633, 1.937499999999998890 ) ) ;
#14382=B_SPLINE_CURVE_WITH_KNOTS ( 'NONE', 3,
 ( #5571, #8010, #5798, #3376, #3302, #2004 ),
 .UNSPECIFIED., .F., .F.,
 ( 4, 2, 4 ),
 ( 2.475503369269340592E-07, 0.002222330217055639313, 0.004444412883774352327 ),
 .UNSPECIFIED. ) ;
#14394=VERTEX_POINT ( 'NONE', #14551 ) ;
#14395=DIRECTION ( 'NONE',  ( 1.000000000000000000, 0.000000000000000000, 0.000000000000000000 ) ) ;
#14400=CARTESIAN_POINT ( 'NONE',  ( 5.000000000000002665, 1.275685995473128912E-14, -4.045263047592942307 ) ) ;
#14410=CARTESIAN_POINT ( 'NONE',  ( 0.3470952277635127037, 8.860649561028118626, -7.493596212620251329 ) ) ;
#14415=CARTESIAN_POINT ( 'NONE',  ( 4.799145180956616130, -0.5093500532425063732, 1.625000001365592528 ) ) ;
#14417=CARTESIAN_POINT ( 'NONE',  ( 2.131511515620586383, 3.916244202832140253, -3.437499998634407916 ) ) ;
#14418=CARTESIAN_POINT ( 'NONE',  ( 5.000000000000004441, 6.350331166892669572E-15, -1.045263047592943417 ) ) ;
#14425=VERTEX_POINT ( 'NONE', #10839 ) ;
#14430=CARTESIAN_POINT ( 'NONE',  ( -2.131511515620587272, -3.916244202832140253, -0.9374999986344056957 ) ) ;
#14442=CARTESIAN_POINT ( 'NONE',  ( 4.799145180956616130, -0.5093500532425063732, -1.374999998634406140 ) ) ;
#14443=ORIENTED_EDGE ( 'NONE', *, *, #6203, .F. ) ;
#14446=EDGE_LOOP ( 'NONE', ( #2969, #6183, #11392, #10040 ) ) ;
#14454=DIRECTION ( 'NONE',  ( 0.000000000000000000, 0.000000000000000000, 1.000000000000000000 ) ) ;
#14457=CARTESIAN_POINT ( 'NONE',  ( 1.261996585732578113, -4.276409079477644148, -6.562499998634407028 ) ) ;
#14459=CARTESIAN_POINT ( 'NONE',  ( 0.2323655586075058233, -4.874496464951329600, -0.08906361846652831316 ) ) ;
#14479=ORIENTED_EDGE ( 'NONE', *, *, #8065, .F. ) ;
#14487=CARTESIAN_POINT ( 'NONE',  ( -4.799145180956616130, 0.5093500532425063732, -0.8749999986344056957 ) ) ;
#14490=CARTESIAN_POINT ( 'NONE',  ( 3.753672977998667726, 3.033343224707664376, -0.4999999986344072500 ) ) ;
#14491=CARTESIAN_POINT ( 'NONE',  ( 0.000000000000000000, 0.000000000000000000, -25.03750572909317285 ) ) ;
#14497=CARTESIAN_POINT ( 'NONE',  ( 5.000000000000000888, 0.000000000000000000, -25.03750572909317285 ) ) ;
#14499=ORIENTED_EDGE ( 'NONE', *, *, #7024, .F. ) ;
#14500=CARTESIAN_POINT ( 'NONE',  ( -5.000000000000004441, -7.530481206757679743E-15, -2.420263044861759472 ) ) ;
#14508=CARTESIAN_POINT ( 'NONE',  ( -4.336808689942016257E-16, -8.660254037844397956, -7.564338275809346257 ) ) ;
#14512=CARTESIAN_POINT ( 'NONE',  ( 3.033343224707661712, -3.753672977998669946, 0.5000000013655936382 ) ) ;
#14527=DIRECTION ( 'NONE',  ( 1.000000000000000000, 0.000000000000000000, 0.000000000000000000 ) ) ;
#14531=CARTESIAN_POINT ( 'NONE',  ( 2.390265326283148806, 4.391654775818395251, 0.1249999999999966416 ) ) ;
#14533=CARTESIAN_POINT ( 'NONE',  ( -0.5688975254463102260, -4.825649467606618614, -0.1037993411750909034 ) ) ;
#14536=CARTESIAN_POINT ( 'NONE',  ( -5.000000000000000888, 6.123233995736767268E-16, 0.000000000000000000 ) ) ;
#14537=EDGE_LOOP ( 'NONE', ( #9844, #4099, #12638, #4311, #15471 ) ) ;
#14539=CARTESIAN_POINT ( 'NONE',  ( -7.500000000000003553, -3.105855721450407447, -7.659356991635974943 ) ) ;
#14544=CARTESIAN_POINT ( 'NONE',  ( -2.459698528280934049, 7.240146430416067425, -0.09933465333851286549 ) ) ;
#14545=DIRECTION ( 'NONE',  ( 0.000000000000000000, 0.000000000000000000, 1.000000000000000000 ) ) ;
#14551=CARTESIAN_POINT ( 'NONE',  ( -4.336808689942017736E-16, -8.660254037844399733, -7.422398894150038728 ) ) ;
#14554=( NAMED_UNIT ( * ) PLANE_ANGLE_UNIT ( ) SI_UNIT ( $, .RADIAN. ) );
#14557=EDGE_LOOP ( 'NONE', ( #11319, #9809, #10232, #13248, #11922, #10830, #3863, #3354, #15510, #4157, #8767, #9323, #14212, #15491, #9882, #7121, #1728, #1355, #11071, #12078, #795 ) ) ;
#14562=CARTESIAN_POINT ( 'NONE',  ( 3.033343224707661712, -3.753672977998669946, 0.5000000013655936382 ) ) ;
#14564=CARTESIAN_POINT ( 'NONE',  ( -3.033343224707664376, 3.753672977998667726, -1.249999998634407916 ) ) ;
#14570=EDGE_LOOP ( 'NONE', ( #11412, #987, #3883, #12656 ) ) ;
#14574=CARTESIAN_POINT ( 'NONE',  ( 4.799145180956616130, -0.5093500532425063732, -2.624999998634407028 ) ) ;
#14584=CARTESIAN_POINT ( 'NONE',  ( -0.5711823568785978633, -5.381735091635035495, -1.187499997268816054 ) ) ;
#14588=CARTESIAN_POINT ( 'NONE',  ( -4.276409079477644148, -1.261996585732578335, -5.812499998634406140 ) ) ;
#14599=CIRCLE ( 'NONE', #6086, 7.500000000000001776 ) ;
#14607=CARTESIAN_POINT ( 'NONE',  ( 4.795541693661363958, 1.415196051561583790, -2.000000000000001776 ) ) ;
#14608=CARTESIAN_POINT ( 'NONE',  ( -2.390265326283148806, -4.391654775818394363, -2.249999997268815388 ) ) ;
#14609=CARTESIAN_POINT ( 'NONE',  ( -4.586482550153569981, -1.057820282786336108, -0.2105217688629980877 ) ) ;
#14613=CARTESIAN_POINT ( 'NONE',  ( 3.916244202832140253, -2.131511515620588160, -2.687499998634407028 ) ) ;
#14622=EDGE_CURVE ( 'NONE', #13190, #14775, #1807, .T. ) ;
#14634=DIRECTION ( 'NONE',  ( 1.000000000000000000, 0.000000000000000000, 0.000000000000000000 ) ) ;
#14636=CARTESIAN_POINT ( 'NONE',  ( -2.390265326283148806, -4.391654775818394363, -6.249999997268814944 ) ) ;
#14647=CARTESIAN_POINT ( 'NONE',  ( -0.5711823568785977523, -5.381735091635034607, -4.187499997268818497 ) ) ;
#14649=CARTESIAN_POINT ( 'NONE',  ( 3.033343224707661712, -3.753672977998669946, 1.500000001365594304 ) ) ;
#14651=CARTESIAN_POINT ( 'NONE',  ( 4.276409079477644148, 1.261996585732577891, -2.562499998634407028 ) ) ;
#14662=CARTESIAN_POINT ( 'NONE',  ( -3.753672977998669502, -3.033343224707661712, -1.999999998634408360 ) ) ;
#14668=CARTESIAN_POINT ( 'NONE',  ( 5.000000000000004441, -2.247904837838113790E-16, -2.045263047592944528 ) ) ;
#14671=CARTESIAN_POINT ( 'NONE',  ( 5.381735091635035495, -0.5711823568785978633, 0.06250000273118166971 ) ) ;
#14676=CARTESIAN_POINT ( 'NONE',  ( -0.5093500532425060401, -4.799145180956616130, -3.624999998634407916 ) ) ;
#14693=CARTESIAN_POINT ( 'NONE',  ( -4.209348295687703967, -3.401574460001763001, -0.4375000000000013323 ) ) ;
#14698=CARTESIAN_POINT ( 'NONE',  ( 0.5093500532425063732, 4.799145180956616130, -1.374999998634406140 ) ) ;
#14708=( BOUNDED_SURFACE ( )  B_SPLINE_SURFACE ( 3, 2, ( 
 ( #14410, #5601, #758 ),
 ( #3404, #830, #10618 ),
 ( #10769, #15706, #2186 ),
 ( #4464, #14322, #15473 ),
 ( #4625, #13247, #5752 ),
 ( #7139, #12042, #15623 ),
 ( #5521, #1952, #12936 ),
 ( #4307, #9248, #14174 ) ),
 .UNSPECIFIED., .F., .F., .F. ) 
 B_SPLINE_SURFACE_WITH_KNOTS ( ( 4, 2, 2, 4 ),
 ( 3, 3 ),
 ( 0.03861844051980969222, 0.04325213341840641879, 0.04556897986770477860, 0.04788582631700313841 ),
 ( 0.000000000000000000, 1.000000000000000000 ),
 .UNSPECIFIED. ) 
 GEOMETRIC_REPRESENTATION_ITEM ( )  RATIONAL_B_SPLINE_SURFACE ( (
 ( 1.000000000000000000, 0.8047781759831923454, 1.000000000000000000),
 ( 1.000000000000000000, 0.8123762462803808537, 1.000000000000000000),
 ( 1.000000000000000000, 0.8190659850618393634, 1.000000000000000000),
 ( 1.000000000000000000, 0.8191937571012808394, 1.000000000000000000),
 ( 1.000000000000000000, 0.8176092952779425715, 1.000000000000000000),
 ( 1.000000000000000000, 0.8122962088597516228, 1.000000000000000000),
 ( 1.000000000000000000, 0.8086311330827178345, 1.000000000000000000),
 ( 1.000000000000000000, 0.8047712282214325441, 1.000000000000000000) ) ) 
 REPRESENTATION_ITEM ( '' )  SURFACE ( )  );
#14715=CARTESIAN_POINT ( 'NONE',  ( 4.999999999999849898, -1.272547481429012084, -0.9615974799134627826 ) ) ;
#14723=DIRECTION ( 'NONE',  ( -0.8306121863236411995, -0.2451191463975535001, -0.4999999999999953371 ) ) ;
#14725=DIRECTION ( 'NONE',  ( 1.000000000000000000, 0.000000000000000000, 0.000000000000000000 ) ) ;
#14727=CARTESIAN_POINT ( 'NONE',  ( 3.753672977998667726, 3.033343224707664376, -2.249999998634408804 ) ) ;
#14730=CARTESIAN_POINT ( 'NONE',  ( -3.033343224707664376, 3.753672977998667726, -2.249999998634408804 ) ) ;
#14736=ORIENTED_EDGE ( 'NONE', *, *, #6179, .T. ) ;
#14740=CARTESIAN_POINT ( 'NONE',  ( -4.276409079477644148, -1.261996585732578335, -1.062499998634405696 ) ) ;
#14747=CARTESIAN_POINT ( 'NONE',  ( -1.415196051561583790, 4.795541693661363958, -1.624999997268814722 ) ) ;
#14751=CARTESIAN_POINT ( 'NONE',  ( -3.033343224707664376, 3.753672977998667726, -2.999999998634409248 ) ) ;
#14761=DIRECTION ( 'NONE',  ( 1.000000000000000000, 0.000000000000000000, 0.000000000000000000 ) ) ;
#14763=B_SPLINE_CURVE_WITH_KNOTS ( 'NONE', 3,
 ( #6264, #9022, #11107, #11178, #8851, #2776 ),
 .UNSPECIFIED., .F., .F.,
 ( 4, 2, 4 ),
 ( 2.475503369425938985E-07, 0.002222330217055646252, 0.004444412883774351460 ),
 .UNSPECIFIED. ) ;
#14767=CARTESIAN_POINT ( 'NONE',  ( 4.209348295687701302, 3.401574460001765665, 0.06249999999999536482 ) ) ;
#14771=CARTESIAN_POINT ( 'NONE',  ( -4.276409079477644148, -1.261996585732578335, -4.062499998634405252 ) ) ;
#14775=VERTEX_POINT ( 'NONE', #11391 ) ;
#14789=DIRECTION ( 'NONE',  ( 1.000000000000000000, 0.000000000000000000, 0.000000000000000000 ) ) ;
#14790=CARTESIAN_POINT ( 'NONE',  ( 0.000000000000000000, 0.000000000000000000, -25.03750572909317285 ) ) ;
#14802=CYLINDRICAL_SURFACE ( 'NONE', #11514, 5.000000000000000888 ) ;
#14805=CARTESIAN_POINT ( 'NONE',  ( 3.753672977998667726, 3.033343224707664376, -3.249999998634409692 ) ) ;
#14807=CARTESIAN_POINT ( 'NONE',  ( -1.261996585732579224, 4.276409079477648589, -4.312499998634405252 ) ) ;
#14816=CARTESIAN_POINT ( 'NONE',  ( 4.799145180956616130, -0.5093500532425063732, -4.624999998634405252 ) ) ;
#14819=EDGE_CURVE ( 'NONE', #635, #5764, #2505, .T. ) ;
#14821=DIRECTION ( 'NONE',  ( 0.000000000000000000, 0.000000000000000000, 1.000000000000000000 ) ) ;
#14828=CARTESIAN_POINT ( 'NONE',  ( 1.415196051561583790, -4.795541693661363958, -3.124999997268815832 ) ) ;
#14830=CARTESIAN_POINT ( 'NONE',  ( -4.619058391327882873, 0.6486937841448088271, -0.2428057022536735388 ) ) ;
#14835=CARTESIAN_POINT ( 'NONE',  ( -0.5093500532425060401, -4.799145180956616130, -4.624999998634405252 ) ) ;
#14847=CARTESIAN_POINT ( 'NONE',  ( -7.922281120364393914, -4.573931137438277617, -8.047472243342932430 ) ) ;
#14850=CARTESIAN_POINT ( 'NONE',  ( 2.390265326283148806, 4.391654775818395251, -0.8750000000000007772 ) ) ;
#14851=CARTESIAN_POINT ( 'NONE',  ( -4.391654775818395251, 2.390265326283148806, -3.624999999999999556 ) ) ;
#14854=CARTESIAN_POINT ( 'NONE',  ( -4.276409079477644148, -1.261996585732578335, -1.062499998634405696 ) ) ;
#14856=AXIS2_PLACEMENT_3D ( 'NONE', #6554, #5498, #2903 ) ;
#14857=CARTESIAN_POINT ( 'NONE',  ( -7.500000000000007105, -2.571118828324944428, -0.3627527587569141510 ) ) ;
#14867=CARTESIAN_POINT ( 'NONE',  ( 6.601567268551446155, -5.319966374295976408, -7.792327460285857654 ) ) ;
#14868=CYLINDRICAL_SURFACE ( 'NONE', #12325, 5.000000000000000888 ) ;
#14876=CARTESIAN_POINT ( 'NONE',  ( -4.336808689942017736E-16, 9.147862274876558786, -8.047472243342932430 ) ) ;
#14878=ADVANCED_FACE ( 'NONE', ( #7937, #15208 ), #6879, .F. ) ;
#14882=( LENGTH_UNIT ( ) NAMED_UNIT ( * ) SI_UNIT ( .MILLI., .METRE. ) );
#14891=CARTESIAN_POINT ( 'NONE',  ( 3.753672977998667726, 3.033343224707664376, -4.249999998634406140 ) ) ;
#14894=AXIS2_PLACEMENT_3D ( 'NONE', #4294, #4606, #14395 ) ;
#14895=CARTESIAN_POINT ( 'NONE',  ( 4.799145180956616130, -0.5093500532425063732, -4.624999998634405252 ) ) ;
#14906=CARTESIAN_POINT ( 'NONE',  ( 0.000000000000000000, 0.000000000000000000, 0.000000000000000000 ) ) ;
#14909=CARTESIAN_POINT ( 'NONE',  ( -4.799145180956616130, 0.5093500532425063732, -6.124999998634407916 ) ) ;
#14911=CARTESIAN_POINT ( 'NONE',  ( -2.131511515620587272, -3.916244202832140253, -7.687499998634407916 ) ) ;
#14915=CARTESIAN_POINT ( 'NONE',  ( 4.795541693661363958, 1.415196051561583790, -4.874999997268817609 ) ) ;
#14921=ORIENTED_EDGE ( 'NONE', *, *, #12795, .T. ) ;
#14923=CARTESIAN_POINT ( 'NONE',  ( 4.799145180956616130, -0.5093500532425063732, -2.374999998634407028 ) ) ;
#14928=ORIENTED_EDGE ( 'NONE', *, *, #2217, .T. ) ;
#14938=CARTESIAN_POINT ( 'NONE',  ( 4.391654775818395251, -2.390265326283149694, -6.125000000000001776 ) ) ;
#14945=CARTESIAN_POINT ( 'NONE',  ( 1.261996585732578113, -4.276409079477644148, -1.812499998634406584 ) ) ;
#14957=VECTOR ( 'NONE', #8414, 1000.000000000000000 ) ;
#14959=CARTESIAN_POINT ( 'NONE',  ( 4.276409079477644148, 1.261996585732577891, -3.312499998634407916 ) ) ;
#14960=CARTESIAN_POINT ( 'NONE',  ( 4.078246330773204420, 1.822159612333905887, -0.3789984458506753806 ) ) ;
#14965=ADVANCED_FACE ( 'NONE', ( #4121 ), #4175, .F. ) ;
#14974=DIRECTION ( 'NONE',  ( 0.000000000000000000, 0.000000000000000000, 1.000000000000000000 ) ) ;
#14979=CARTESIAN_POINT ( 'NONE',  ( 3.753672977998667726, 3.033343224707664376, -4.499999998634407028 ) ) ;
#14985=CARTESIAN_POINT ( 'NONE',  ( 5.000000000000004441, -2.247904837838113790E-16, -7.045263047592947636 ) ) ;
#14988=CARTESIAN_POINT ( 'NONE',  ( 4.276409079477644148, 1.261996585732577891, -5.562499998634406140 ) ) ;
#14996=CARTESIAN_POINT ( 'NONE',  ( -5.381735091635034607, 0.5711823568785950878, -5.437499997268815832 ) ) ;
#14997=CARTESIAN_POINT ( 'NONE',  ( -7.922281120364393914, 4.573931137438272287, -8.047472243342932430 ) ) ;
#14998=CARTESIAN_POINT ( 'NONE',  ( -2.799455000695346918, 3.610413774745345528, -0.3100886528999980407 ) ) ;
#15001=FACE_OUTER_BOUND ( 'NONE', #4124, .T. ) ;
#15004=ORIENTED_EDGE ( 'NONE', *, *, #8308, .T. ) ;
#15015=CARTESIAN_POINT ( 'NONE',  ( 0.5711823568785989735, 5.381735091635026613, -6.812500000000005329 ) ) ;
#15019=CARTESIAN_POINT ( 'NONE',  ( 4.799145180956616130, -0.5093500532425063732, -4.624999998634405252 ) ) ;
#15027=DIRECTION ( 'NONE',  ( 0.000000000000000000, 0.000000000000000000, 1.000000000000000000 ) ) ;
#15033=DIRECTION ( 'NONE',  ( 0.000000000000000000, 0.000000000000000000, -1.000000000000000000 ) ) ;
#15034=CARTESIAN_POINT ( 'NONE',  ( -3.753672977998669502, -3.033343224707661712, -1.749999998634408360 ) ) ;
#15035=CARTESIAN_POINT ( 'NONE',  ( 4.434540660362028319, 0.5348740976411813230, -0.3789984458506921450 ) ) ;
#15040=DIRECTION ( 'NONE',  ( 0.000000000000000000, 0.000000000000000000, 1.000000000000000000 ) ) ;
#15047=CARTESIAN_POINT ( 'NONE',  ( 4.276409079477644148, 1.261996585732577891, -8.312499998634407916 ) ) ;
#15055=CARTESIAN_POINT ( 'NONE',  ( -2.131511515620587272, -3.916244202832140253, -5.937499998634407028 ) ) ;
#15058=CYLINDRICAL_SURFACE ( 'NONE', #8477, 5.000000000000000888 ) ;
#15060=CARTESIAN_POINT ( 'NONE',  ( 1.415196051561583790, -4.795541693661363958, -7.250000000000002665 ) ) ;
#15063=CARTESIAN_POINT ( 'NONE',  ( 3.753672977998667726, 3.033343224707664820, -5.499999998634407916 ) ) ;
#15067=CARTESIAN_POINT ( 'NONE',  ( 4.209348295687701302, 3.401574460001765665, -5.812499997268813168 ) ) ;
#15071=VERTEX_POINT ( 'NONE', #14536 ) ;
#15073=CARTESIAN_POINT ( 'NONE',  ( -3.916244202832140253, 2.131511515620587272, -7.937499998634408804 ) ) ;
#15088=CARTESIAN_POINT ( 'NONE',  ( -0.5711823568785978633, -5.381735091635035495, -6.312500000000000888 ) ) ;
#15091=CARTESIAN_POINT ( 'NONE',  ( -3.753672977998669946, -3.033343224707661712, -6.999999998634408804 ) ) ;
#15114=EDGE_CURVE ( 'NONE', #1389, #5622, #9687, .T. ) ;
#15127=CARTESIAN_POINT ( 'NONE',  ( 4.795541693661363958, 1.415196051561583790, -6.874999997268815832 ) ) ;
#15129=( BOUNDED_CURVE ( )  B_SPLINE_CURVE ( 2, ( #4231, #5529, #10463, #4321, #9260, #8049, #14184, #12947, #5614, #5762, #14335 ),
 .UNSPECIFIED., .F., .F. ) 
 B_SPLINE_CURVE_WITH_KNOTS ( ( 3, 2, 2, 2, 2, 3 ),
 ( 0.3545872658012772516, 0.3624999999999999889, 0.3750000000000000000, 0.3875000000000000111, 0.4000000000000000222, 0.4045872658012772960 ),
 .UNSPECIFIED. ) 
 CURVE ( )  GEOMETRIC_REPRESENTATION_ITEM ( )  RATIONAL_B_SPLINE_CURVE ( ( 0.9646335149384808183, 0.9518143178943437865, 1.000000000000000000, 0.9238795325112867385, 1.000000000000000000, 0.9238795325112867385, 1.000000000000000000, 0.9238795325112867385, 1.000000000000000000, 0.9720652146169428409, 0.9646335149384805963 ) ) 
 REPRESENTATION_ITEM ( '' )  );
#15132=CARTESIAN_POINT ( 'NONE',  ( 4.276409079477644148, 1.261996585732577891, -3.562499998634407916 ) ) ;
#15139=ORIENTED_EDGE ( 'NONE', *, *, #520, .T. ) ;
#15140=CARTESIAN_POINT ( 'NONE',  ( -4.795541693661363958, -1.415196051561583790, -7.500000000000003553 ) ) ;
#15143=CARTESIAN_POINT ( 'NONE',  ( 4.799145180956616130, -0.5093500532425063732, -7.624999998634407916 ) ) ;
#15145=CARTESIAN_POINT ( 'NONE',  ( 5.000000000000000888, 0.000000000000000000, -25.03750572909317285 ) ) ;
#15147=CARTESIAN_POINT ( 'NONE',  ( -4.276409079477644148, -1.261996585732578335, -7.812499998634407916 ) ) ;
#15152=CARTESIAN_POINT ( 'NONE',  ( -2.390265326283148806, -4.391654775818394363, -3.249999997268816276 ) ) ;
#15159=CARTESIAN_POINT ( 'NONE',  ( 4.799145180956616130, -0.5093500532425063732, -6.374999998634407028 ) ) ;
#15170=EDGE_CURVE ( 'NONE', #3351, #1389, #8542, .T. ) ;
#15176=CARTESIAN_POINT ( 'NONE',  ( 2.390265326283148806, 4.391654775818395251, -6.875000000000002665 ) ) ;
#15177=CARTESIAN_POINT ( 'NONE',  ( 4.209348295687701302, 3.401574460001766109, -2.937500000000003553 ) ) ;
#15180=CARTESIAN_POINT ( 'NONE',  ( 3.753672977998667726, 3.033343224707664376, -8.499999998634411469 ) ) ;
#15187=APPLICATION_CONTEXT ( 'automotive_design' ) ;
#15192=FACE_OUTER_BOUND ( 'NONE', #13246, .T. ) ;
#15193=DIRECTION ( 'NONE',  ( 0.000000000000000000, 0.000000000000000000, 1.000000000000000000 ) ) ;
#15194=EDGE_CURVE ( 'NONE', #11803, #7219, #1001, .T. ) ;
#15195=CARTESIAN_POINT ( 'NONE',  ( -0.5093500532425060401, -4.799145180956616130, -0.6249999986344054737 ) ) ;
#15196=CARTESIAN_POINT ( 'NONE',  ( -7.500000000000001776, 0.000000000000000000, 0.000000000000000000 ) ) ;
#15200=CARTESIAN_POINT ( 'NONE',  ( -2.131511515620587272, -3.916244202832140253, -4.687499998634405252 ) ) ;
#15208=FACE_OUTER_BOUND ( 'NONE', #4392, .T. ) ;
#15210=ORIENTED_EDGE ( 'NONE', *, *, #7624, .F. ) ;
#15211=VERTEX_POINT ( 'NONE', #11134 ) ;
#15215=ORIENTED_EDGE ( 'NONE', *, *, #14329, .T. ) ;
#15221=CARTESIAN_POINT ( 'NONE',  ( -2.390265326283148806, -4.391654775818394363, -4.249999997268816720 ) ) ;
#15223=CARTESIAN_POINT ( 'NONE',  ( 2.390265326283148806, 4.391654775818395251, -7.749999997268816720 ) ) ;
#15224=AXIS2_PLACEMENT_3D ( 'NONE', #4541, #3250, #8199 ) ;
#15231=CARTESIAN_POINT ( 'NONE',  ( -3.753672977998669502, -3.033343224707661712, -7.999999998634411469 ) ) ;
#15233=DIRECTION ( 'NONE',  ( 0.000000000000000000, 0.000000000000000000, 1.000000000000000000 ) ) ;
#15237=ADVANCED_FACE ( 'NONE', ( #13454 ), #3761, .T. ) ;
#15239=CARTESIAN_POINT ( 'NONE',  ( -2.390265326283148806, -4.391654775818394363, -8.249999997268814056 ) ) ;
#15240=CARTESIAN_POINT ( 'NONE',  ( -2.390265326283148806, -4.391654775818394363, -6.249999997268814944 ) ) ;
#15241=CARTESIAN_POINT ( 'NONE',  ( 4.795541693661363958, 1.415196051561583790, -8.874999997268814056 ) ) ;
#15246=CARTESIAN_POINT ( 'NONE',  ( -4.276409079477644148, -1.261996585732578335, -6.812499998634407028 ) ) ;
#15250=ORIENTED_EDGE ( 'NONE', *, *, #2887, .T. ) ;
#15251=ORIENTED_EDGE ( 'NONE', *, *, #7629, .T. ) ;
#15252=CARTESIAN_POINT ( 'NONE',  ( -0.6511518506208979762, 8.763486134561274454, -7.907570769506046204 ) ) ;
#15257=CARTESIAN_POINT ( 'NONE',  ( -7.777900015783941967, -4.169681370001539378, -7.928862157988302073 ) ) ;
#15259=CARTESIAN_POINT ( 'NONE',  ( 4.795541693661363958, 1.415196051561583790, -6.000000000000001776 ) ) ;
#15263=CARTESIAN_POINT ( 'NONE',  ( -4.276409079477644148, -1.261996585732578335, -6.062499998634407028 ) ) ;
#15264=ORIENTED_EDGE ( 'NONE', *, *, #908, .T. ) ;
#15265=CARTESIAN_POINT ( 'NONE',  ( 7.808623696107861889, -4.508310992946700679, -7.999704684617483963 ) ) ;
#15271=CARTESIAN_POINT ( 'NONE',  ( -1.415196051561583790, 4.795541693661363958, -7.750000000000003553 ) ) ;
#15275=CARTESIAN_POINT ( 'NONE',  ( -3.033343224707664820, 3.753672977998667726, -1.999999998634408360 ) ) ;
#15276=CARTESIAN_POINT ( 'NONE',  ( 3.962264623424024190, 2.061996207999744701, -0.3789984458506767684 ) ) ;
#15278=CARTESIAN_POINT ( 'NONE',  ( 3.916244202832140253, -2.131511515620588160, -3.437499998634407916 ) ) ;
#15284=CARTESIAN_POINT ( 'NONE',  ( 7.169303301815073581, -4.521054846639389169, -7.349897473155027505 ) ) ;
#15285=ORIENTED_EDGE ( 'NONE', *, *, #8608, .F. ) ;
#15291=CARTESIAN_POINT ( 'NONE',  ( -8.673617379884035472E-16, -9.147862274876560562, -8.047472243342939535 ) ) ;
#15299=CARTESIAN_POINT ( 'NONE',  ( 2.131511515620586383, 3.916244202832140253, -8.437499998634409692 ) ) ;
#15300=CARTESIAN_POINT ( 'NONE',  ( 4.799145180956616130, -0.5093500532425063732, 1.375000001365592528 ) ) ;
#15309=DIRECTION ( 'NONE',  ( -0.8191520442889907994, 1.003171929053523514E-16, 0.5735764363510474917 ) ) ;
#15315=CARTESIAN_POINT ( 'NONE',  ( 4.391654775818395251, -2.390265326283149694, -6.999999997268815832 ) ) ;
#15316=CARTESIAN_POINT ( 'NONE',  ( 0.5711823568785988625, 5.381735091635026613, -0.8124999999999997780 ) ) ;
#15321=CARTESIAN_POINT ( 'NONE',  ( 7.500000000000003553, -4.330127018922199866, -7.422398894150035176 ) ) ;
#15328=EDGE_CURVE ( 'NONE', #15838, #1307, #7912, .T. ) ;
#15330=DIRECTION ( 'NONE',  ( 0.000000000000000000, 0.000000000000000000, 1.000000000000000000 ) ) ;
#15332=( BOUNDED_SURFACE ( )  B_SPLINE_SURFACE ( 1, 2, ( 
 ( #2215, #9649, #4964, #48, #8310, #12306, #7402, #13508, #12558, #2373, #11109, #7169, #10948, #4810, #12071, #9734, #1015, #14671, #7085, #1245, #9817, #5948, #9891, #15810, #8544, #2445, #10868, #4727, #7248, #937, #11986, #3670, #13200, #4651, #2138, #3596, #12221, #14584, #9576, #4891, #12148, #1163, #3504, #13432, #14747, #8463, #13362, #2303, #6105, #13848, #8779, #4070, #6267, #2778, #13927, #11499, #1322, #2530, #11181, #7565, #449, #10143, #12387, #5372, #6508, #12548, #369, #12463, #14828, #9024, #15152, #2853, #3747, #126, #7808, #11346, #11422, #7737, #6348, #3908, #8854, #3836, #8693, #5286, #12628, #12703, #3984, #1643, #6584, #5047, #10067, #9976, #1495, #6435, #1569, #13598, #14915, #7484, #13681, #2612, #10226, #1402, #11267, #215, #5136, #14996, #13759, #2693, #298, #7651, #5208, #15067, #8937, #6823, #4228, #610, #11890, #6991, #15240, #3260, #14333, #4472, #1962, #9331, #13107, #5452, #8047, #11730, #10383, #12945, #15315, #5611, #14002, #8207, #766, #9174, #838, #6751, #15481, #9406, #14095, #3019, #14182, #7885, #2930, #10624, #10315, #12781, #4149, #685, #3181, #7966, #535, #6908, #3109, #8126, #10461, #10552, #11816, #9095, #2046 ),
 ( #12869, #1804, #4399, #14255, #11655, #1723, #15555, #6674, #5527, #15395, #11583, #4318, #9258, #1881, #13023, #5687, #6084, #12130, #5845, #7068, #7302, #7148, #11967, #9714, #9485, #5760, #12051, #2117, #3654, #10851, #5930, #14490, #3486, #13181, #15791, #13338, #996, #15634, #15952, #8597, #4709, #9630, #4877, #14564, #10779, #2425, #9802, #919, #8446, #12204, #1144, #2283, #8525, #15720, #3411, #2355, #8363, #4633, #7232, #14730, #13487, #1067, #6003, #10929, #14651, #15868, #7379, #8292, #10697, #9561, #13255, #4790, #3576, #2197, #13418, #11014, #12289, #4552, #14417, #3343, #15132, #11095, #13576, #12526, #355, #13913, #3728, #4948, #8674, #9955, #2840, #1470, #14807, #7792, #8919, #14979, #2760, #14895, #1224, #11405, #1553, #1384, #6174, #6413, #6329, #11331, #106, #5025, #5268, #31, #5111, #2506, #7467, #12371, #6250, #1304, #5193, #11165, #15055, #9876, #3814, #11248, #8762, #13663, #6493, #10208, #9002, #4053, #10048, #195, #2593, #7547, #12447, #3891, #8836, #13739, #13827, #2672, #7630, #280, #10123, #3968, #7715, #12610, #11800, #591, #1710, #9394, #752, #2918, #1793, #14243, #3167, #12853, #15467, #7868, #10370, #9320, #15299, #12765, #7951 ) ),
 .UNSPECIFIED., .F., .F., .F. ) 
 B_SPLINE_SURFACE_WITH_KNOTS ( ( 2, 2 ),
 ( 3, 2, 2, 2, 2, 2, 2, 2, 2, 2, 2, 2, 2, 2, 2, 2, 2, 2, 2, 2, 2, 2, 2, 2, 2, 2, 2, 2, 2, 2, 2, 2, 2, 2, 2, 2, 2, 2, 2, 2, 2, 2, 2, 2, 2, 2, 2, 2, 2, 2, 2, 2, 2, 2, 2, 2, 2, 2, 2, 2, 2, 2, 2, 2, 2, 2, 2, 2, 2, 2, 2, 2, 2, 2, 2, 2, 2, 2, 2, 2, 3 ),
 ( 0.000000000000000000, 1.000000000000000000 ),
 ( 0.000000000000000000, 0.01250000000000000069, 0.02500000000000000139, 0.03749999999999999861, 0.05000000000000000278, 0.06250000000000000000, 0.07499999999999999722, 0.08749999999999999445, 0.1000000000000000056, 0.1125000000000000028, 0.1250000000000000000, 0.1375000000000000111, 0.1499999999999999944, 0.1625000000000000056, 0.1749999999999999889, 0.1875000000000000000, 0.2000000000000000111, 0.2124999999999999944, 0.2250000000000000056, 0.2374999999999999889, 0.2500000000000000000, 0.2625000000000000111, 0.2750000000000000222, 0.2874999999999999778, 0.2999999999999999889, 0.3125000000000000000, 0.3250000000000000111, 0.3375000000000000222, 0.3499999999999999778, 0.3624999999999999889, 0.3750000000000000000, 0.3875000000000000111, 0.4000000000000000222, 0.4124999999999999778, 0.4249999999999999889, 0.4375000000000000000, 0.4500000000000000111, 0.4625000000000000222, 0.4749999999999999778, 0.4874999999999999889, 0.5000000000000000000, 0.5124999999999999556, 0.5250000000000000222, 0.5374999999999999778, 0.5500000000000000444, 0.5625000000000000000, 0.5749999999999999556, 0.5875000000000000222, 0.5999999999999999778, 0.6125000000000000444, 0.6250000000000000000, 0.6374999999999999556, 0.6500000000000000222, 0.6624999999999999778, 0.6750000000000000444, 0.6875000000000000000, 0.6999999999999999556, 0.7125000000000000222, 0.7249999999999999778, 0.7375000000000000444, 0.7500000000000000000, 0.7624999999999999556, 0.7750000000000000222, 0.7874999999999999778, 0.8000000000000000444, 0.8125000000000000000, 0.8249999999999999556, 0.8375000000000000222, 0.8499999999999999778, 0.8625000000000000444, 0.8750000000000000000, 0.8874999999999999556, 0.9000000000000000222, 0.9124999999999999778, 0.9250000000000000444, 0.9375000000000000000, 0.9499999999999999556, 0.9625000000000000222, 0.9749999999999999778, 0.9875000000000000444, 1.000000000000000000 ),
 .UNSPECIFIED. ) 
 GEOMETRIC_REPRESENTATION_ITEM ( )  RATIONAL_B_SPLINE_SURFACE ( (
 ( 1.000000000000000000, 0.9238795325112867385, 1.000000000000000000, 0.9238795325112867385, 1.000000000000000000, 0.9238795325112867385, 1.000000000000000000, 0.9238795325112867385, 1.000000000000000000, 0.9238795325112867385, 1.000000000000000000, 0.9238795325112867385, 1.000000000000000000, 0.9238795325112867385, 1.000000000000000000, 0.9238795325112867385, 1.000000000000000000, 0.9238795325112867385, 1.000000000000000000, 0.9238795325112867385, 1.000000000000000000, 0.9238795325112867385, 1.000000000000000000, 0.9238795325112867385, 1.000000000000000000, 0.9238795325112867385, 1.000000000000000000, 0.9238795325112867385, 1.000000000000000000, 0.9238795325112867385, 1.000000000000000000, 0.9238795325112867385, 1.000000000000000000, 0.9238795325112867385, 1.000000000000000000, 0.9238795325112867385, 1.000000000000000000, 0.9238795325112867385, 1.000000000000000000, 0.9238795325112867385, 1.000000000000000000, 0.9238795325112867385, 1.000000000000000000, 0.9238795325112867385, 1.000000000000000000, 0.9238795325112867385, 1.000000000000000000, 0.9238795325112867385, 1.000000000000000000, 0.9238795325112867385, 1.000000000000000000, 0.9238795325112867385, 1.000000000000000000, 0.9238795325112867385, 1.000000000000000000, 0.9238795325112867385, 1.000000000000000000, 0.9238795325112867385, 1.000000000000000000, 0.9238795325112867385, 1.000000000000000000, 0.9238795325112867385, 1.000000000000000000, 0.9238795325112867385, 1.000000000000000000, 0.9238795325112867385, 1.000000000000000000, 0.9238795325112867385, 1.000000000000000000, 0.9238795325112867385, 1.000000000000000000, 0.9238795325112867385, 1.000000000000000000, 0.9238795325112867385, 1.000000000000000000, 0.9238795325112867385, 1.000000000000000000, 0.9238795325112867385, 1.000000000000000000, 0.9238795325112867385, 1.000000000000000000, 0.9238795325112867385, 1.000000000000000000, 0.9238795325112867385, 1.000000000000000000, 0.9238795325112867385, 1.000000000000000000, 0.9238795325112867385, 1.000000000000000000, 0.9238795325112867385, 1.000000000000000000, 0.9238795325112867385, 1.000000000000000000, 0.9238795325112867385, 1.000000000000000000, 0.9238795325112867385, 1.000000000000000000, 0.9238795325112867385, 1.000000000000000000, 0.9238795325112867385, 1.000000000000000000, 0.9238795325112867385, 1.000000000000000000, 0.9238795325112867385, 1.000000000000000000, 0.9238795325112867385, 1.000000000000000000, 0.9238795325112867385, 1.000000000000000000, 0.9238795325112867385, 1.000000000000000000, 0.9238795325112867385, 1.000000000000000000, 0.9238795325112867385, 1.000000000000000000, 0.9238795325112867385, 1.000000000000000000, 0.9238795325112867385, 1.000000000000000000, 0.9238795325112867385, 1.000000000000000000, 0.9238795325112867385, 1.000000000000000000, 0.9238795325112867385, 1.000000000000000000, 0.9238795325112867385, 1.000000000000000000, 0.9238795325112867385, 1.000000000000000000, 0.9238795325112867385, 1.000000000000000000, 0.9238795325112867385, 1.000000000000000000, 0.9238795325112867385, 1.000000000000000000, 0.9238795325112867385, 1.000000000000000000, 0.9238795325112867385, 1.000000000000000000, 0.9238795325112867385, 1.000000000000000000, 0.9238795325112867385, 1.000000000000000000, 0.9238795325112867385, 1.000000000000000000, 0.9238795325112867385, 1.000000000000000000, 0.9238795325112867385, 1.000000000000000000, 0.9238795325112867385, 1.000000000000000000, 0.9238795325112867385, 1.000000000000000000, 0.9238795325112867385, 1.000000000000000000, 0.9238795325112867385, 1.000000000000000000, 0.9238795325112867385, 1.000000000000000000, 0.9238795325112867385, 1.000000000000000000),
 ( 1.000000000000000000, 0.9238795325112867385, 1.000000000000000000, 0.9238795325112867385, 1.000000000000000000, 0.9238795325112867385, 1.000000000000000000, 0.9238795325112867385, 1.000000000000000000, 0.9238795325112867385, 1.000000000000000000, 0.9238795325112867385, 1.000000000000000000, 0.9238795325112867385, 1.000000000000000000, 0.9238795325112867385, 1.000000000000000000, 0.9238795325112867385, 1.000000000000000000, 0.9238795325112867385, 1.000000000000000000, 0.9238795325112867385, 1.000000000000000000, 0.9238795325112867385, 1.000000000000000000, 0.9238795325112867385, 1.000000000000000000, 0.9238795325112867385, 1.000000000000000000, 0.9238795325112867385, 1.000000000000000000, 0.9238795325112867385, 1.000000000000000000, 0.9238795325112867385, 1.000000000000000000, 0.9238795325112867385, 1.000000000000000000, 0.9238795325112867385, 1.000000000000000000, 0.9238795325112867385, 1.000000000000000000, 0.9238795325112867385, 1.000000000000000000, 0.9238795325112867385, 1.000000000000000000, 0.9238795325112867385, 1.000000000000000000, 0.9238795325112867385, 1.000000000000000000, 0.9238795325112867385, 1.000000000000000000, 0.9238795325112867385, 1.000000000000000000, 0.9238795325112867385, 1.000000000000000000, 0.9238795325112867385, 1.000000000000000000, 0.9238795325112867385, 1.000000000000000000, 0.9238795325112867385, 1.000000000000000000, 0.9238795325112867385, 1.000000000000000000, 0.9238795325112867385, 1.000000000000000000, 0.9238795325112867385, 1.000000000000000000, 0.9238795325112867385, 1.000000000000000000, 0.9238795325112867385, 1.000000000000000000, 0.9238795325112867385, 1.000000000000000000, 0.9238795325112867385, 1.000000000000000000, 0.9238795325112867385, 1.000000000000000000, 0.9238795325112867385, 1.000000000000000000, 0.9238795325112867385, 1.000000000000000000, 0.9238795325112867385, 1.000000000000000000, 0.9238795325112867385, 1.000000000000000000, 0.9238795325112867385, 1.000000000000000000, 0.9238795325112867385, 1.000000000000000000, 0.9238795325112867385, 1.000000000000000000, 0.9238795325112867385, 1.000000000000000000, 0.9238795325112867385, 1.000000000000000000, 0.9238795325112867385, 1.000000000000000000, 0.9238795325112867385, 1.000000000000000000, 0.9238795325112867385, 1.000000000000000000, 0.9238795325112867385, 1.000000000000000000, 0.9238795325112867385, 1.000000000000000000, 0.9238795325112867385, 1.000000000000000000, 0.9238795325112867385, 1.000000000000000000, 0.9238795325112867385, 1.000000000000000000, 0.9238795325112867385, 1.000000000000000000, 0.9238795325112867385, 1.000000000000000000, 0.9238795325112867385, 1.000000000000000000, 0.9238795325112867385, 1.000000000000000000, 0.9238795325112867385, 1.000000000000000000, 0.9238795325112867385, 1.000000000000000000, 0.9238795325112867385, 1.000000000000000000, 0.9238795325112867385, 1.000000000000000000, 0.9238795325112867385, 1.000000000000000000, 0.9238795325112867385, 1.000000000000000000, 0.9238795325112867385, 1.000000000000000000, 0.9238795325112867385, 1.000000000000000000, 0.9238795325112867385, 1.000000000000000000, 0.9238795325112867385, 1.000000000000000000, 0.9238795325112867385, 1.000000000000000000, 0.9238795325112867385, 1.000000000000000000, 0.9238795325112867385, 1.000000000000000000, 0.9238795325112867385, 1.000000000000000000, 0.9238795325112867385, 1.000000000000000000, 0.9238795325112867385, 1.000000000000000000, 0.9238795325112867385, 1.000000000000000000, 0.9238795325112867385, 1.000000000000000000, 0.9238795325112867385, 1.000000000000000000, 0.9238795325112867385, 1.000000000000000000, 0.9238795325112867385, 1.000000000000000000) ) ) 
 REPRESENTATION_ITEM ( '' )  SURFACE ( )  );
#15333=CARTESIAN_POINT ( 'NONE',  ( -3.750000000000004885, 6.495190528383289141, 0.000000000000000000 ) ) ;
#15338=CARTESIAN_POINT ( 'NONE',  ( 7.500000000000004441, -4.330127018922205195, -1.000000000000000888 ) ) ;
#15342=CARTESIAN_POINT ( 'NONE',  ( 0.5093500532425063732, 4.799145180956616130, -8.374999998634409692 ) ) ;
#15352=CARTESIAN_POINT ( 'NONE',  ( 7.894705354777833861, 0.7527931906211283719, -7.590204373988224340 ) ) ;
#15353=B_SPLINE_CURVE_WITH_KNOTS ( 'NONE', 3,
 ( #14116, #3042, #14024, #2876, #10575, #6846 ),
 .UNSPECIFIED., .F., .F.,
 ( 4, 2, 4 ),
 ( -5.145455527300660531E-06, 0.0004153350442917267738, 0.0008358155441107542345 ),
 .UNSPECIFIED. ) ;
#15354=CARTESIAN_POINT ( 'NONE',  ( 0.5093500532425063732, 4.799145180956616130, -5.124999998634406140 ) ) ;
#15357=CARTESIAN_POINT ( 'NONE',  ( 3.033343224707661712, -3.753672977998669946, -7.499999998634409692 ) ) ;
#15364=CARTESIAN_POINT ( 'NONE',  ( 4.419133455865364546, -6.108866147515648493, -7.026396753507437865 ) ) ;
#15368=CARTESIAN_POINT ( 'NONE',  ( -3.401574460001765221, 4.209348295687701302, -3.562499997268815832 ) ) ;
#15377=CARTESIAN_POINT ( 'NONE',  ( 4.795541693661363958, 1.415196051561583790, -0.8749999972688139449 ) ) ;
#15378=EDGE_CURVE ( 'NONE', #1925, #13190, #438, .T. ) ;
#15380=CARTESIAN_POINT ( 'NONE',  ( -5.000000000000004441, -7.530481206757679743E-15, -0.5452630475929430842 ) ) ;
#15389=CARTESIAN_POINT ( 'NONE',  ( -4.174999999999999822, 5.112900386440199535E-16, -0.5776712190230133270 ) ) ;
#15393=EDGE_CURVE ( 'NONE', #15546, #13190, #9868, .T. ) ;
#15395=CARTESIAN_POINT ( 'NONE',  ( -4.799145180956616130, 0.5093500532425063732, 0.8750000013655920839 ) ) ;
#15400=CARTESIAN_POINT ( 'NONE',  ( 7.500000000000000888, 3.988838049906433092, -0.8529248949437668870 ) ) ;
#15410=VECTOR ( 'NONE', #4486, 1000.000000000000000 ) ;
#15412=AXIS2_PLACEMENT_3D ( 'NONE', #14906, #2602, #5123 ) ;
#15425=CARTESIAN_POINT ( 'NONE',  ( -3.033343224707664376, 3.753672977998667726, 1.365593156898739876E-09 ) ) ;
#15436=CARTESIAN_POINT ( 'NONE',  ( -0.5711823568785977523, -5.381735091635034607, -6.312500000000000000 ) ) ;
#15438=CARTESIAN_POINT ( 'NONE',  ( 7.500000000000000000, 1.572594658376105459, -7.069792055233640404 ) ) ;
#15439=EDGE_CURVE ( 'NONE', #637, #9381, #4465, .T. ) ;
#15440=CARTESIAN_POINT ( 'NONE',  ( -3.753672977998669502, -3.033343224707661712, -5.749999998634407916 ) ) ;
#15444=CARTESIAN_POINT ( 'NONE',  ( -4.276409079477644148, -1.261996585732578335, -6.812499998634407028 ) ) ;
#15450=ORIENTED_EDGE ( 'NONE', *, *, #11333, .T. ) ;
#15452=CARTESIAN_POINT ( 'NONE',  ( 0.9763930676203995684, -8.096533237418878315, -7.213065638943601421 ) ) ;
#15453=EDGE_LOOP ( 'NONE', ( #7520, #2054, #5975, #15285 ) ) ;
#15465=CARTESIAN_POINT ( 'NONE',  ( -0.5711823568785977523, -5.381735091635034607, -4.312499999999999112 ) ) ;
#15467=CARTESIAN_POINT ( 'NONE',  ( -3.916244202832140253, 2.131511515620587272, -8.187499998634407916 ) ) ;
#15468=CARTESIAN_POINT ( 'NONE',  ( -4.799145180956616130, 0.5093500532425063732, -0.1249999986344088321 ) ) ;
#15471=ORIENTED_EDGE ( 'NONE', *, *, #9644, .T. ) ;
#15473=CARTESIAN_POINT ( 'NONE',  ( -4.599534470797605579, 6.460478697737046971, -7.590212325761443779 ) ) ;
#15474=AXIS2_PLACEMENT_3D ( 'NONE', #15758, #6127, #2157 ) ;
#15477=ADVANCED_FACE ( 'NONE', ( #15508 ), #13826, .T. ) ;
#15478=CARTESIAN_POINT ( 'NONE',  ( 2.390265326283148806, 4.391654775818395251, -4.875000000000000888 ) ) ;
#15481=CARTESIAN_POINT ( 'NONE',  ( -4.391654775818395251, 2.390265326283148806, -7.499999997268816720 ) ) ;
#15482=CARTESIAN_POINT ( 'NONE',  ( -5.000000000000004441, -7.530481206757679743E-15, -0.5452630475929430842 ) ) ;
#15486=CARTESIAN_POINT ( 'NONE',  ( -1.415196051561583790, 4.795541693661363958, -2.624999997268815388 ) ) ;
#15491=ORIENTED_EDGE ( 'NONE', *, *, #799, .F. ) ;
#15505=CARTESIAN_POINT ( 'NONE',  ( 2.131511515620586383, 3.916244202832140253, -1.187499998634405918 ) ) ;
#15508=FACE_OUTER_BOUND ( 'NONE', #5121, .T. ) ;
#15510=ORIENTED_EDGE ( 'NONE', *, *, #2217, .F. ) ;
#15516=CARTESIAN_POINT ( 'NONE',  ( 7.499999999999650946, 0.7577384720642122984, -7.446470314338120566 ) ) ;
#15517=CARTESIAN_POINT ( 'NONE',  ( 1.261996585732578113, -4.276409079477644148, -4.562499998634405252 ) ) ;
#15520=CARTESIAN_POINT ( 'NONE',  ( 3.033343224707661712, -3.753672977998669946, -6.499999998634407916 ) ) ;
#15522=CARTESIAN_POINT ( 'NONE',  ( 5.000000000000000888, 0.000000000000000000, -25.03750572909317285 ) ) ;
#15526=CARTESIAN_POINT ( 'NONE',  ( -1.415196051561583790, 4.795541693661363958, -6.750000000000002665 ) ) ;
#15528=ORIENTED_EDGE ( 'NONE', *, *, #6192, .T. ) ;
#15534=ADVANCED_FACE ( 'NONE', ( #5713 ), #5830, .F. ) ;
#15542=FACE_OUTER_BOUND ( 'NONE', #2097, .T. ) ;
#15543=CARTESIAN_POINT ( 'NONE',  ( 4.276409079477644148, 1.261996585732577891, -0.5624999986344088043 ) ) ;
#15546=VERTEX_POINT ( 'NONE', #4733 ) ;
#15551=B_SPLINE_CURVE_WITH_KNOTS ( 'NONE', 3,
 ( #4807, #5945, #12145, #8306, #13197, #11982 ),
 .UNSPECIFIED., .F., .F.,
 ( 4, 2, 4 ),
 ( 0.004615310220740751271, 0.006918661718823357169, 0.009222013216905963068 ),
 .UNSPECIFIED. ) ;
#15555=CARTESIAN_POINT ( 'NONE',  ( -2.131511515620587272, -3.916244202832140253, 1.062500001365592528 ) ) ;
#15559=ORIENTED_EDGE ( 'NONE', *, *, #4233, .T. ) ;
#15561=CARTESIAN_POINT ( 'NONE',  ( -4.999999999999849898, 1.272547481429008309, -2.461597479913463893 ) ) ;
#15566=VECTOR ( 'NONE', #9854, 1000.000000000000114 ) ;
#15580=CARTESIAN_POINT ( 'NONE',  ( -3.033343224707664376, 3.753672977998667726, -1.999999998634408360 ) ) ;
#15582=CARTESIAN_POINT ( 'NONE',  ( 6.523606932381143864, 4.893847819346820671, -7.213065638944192060 ) ) ;
#15588=CARTESIAN_POINT ( 'NONE',  ( -4.209348295687703079, -3.401574460001763445, -6.437500000000003553 ) ) ;
#15590=CARTESIAN_POINT ( 'NONE',  ( 0.5093500532425063732, 4.799145180956616130, -6.124999998634407916 ) ) ;
#15593=CARTESIAN_POINT ( 'NONE',  ( -4.799145180956616130, 0.5093500532425063732, -6.874999998634407916 ) ) ;
#15602=ORIENTED_EDGE ( 'NONE', *, *, #9869, .F. ) ;
#15606=CARTESIAN_POINT ( 'NONE',  ( 3.401574460001763445, -4.209348295687703079, -7.062499997268814944 ) ) ;
#15615=CARTESIAN_POINT ( 'NONE',  ( -5.000000000000095035, -0.7223674278660573433, -4.521799365517152225 ) ) ;
#15622=ORIENTED_EDGE ( 'NONE', *, *, #2570, .T. ) ;
#15623=CARTESIAN_POINT ( 'NONE',  ( -6.625705691649780960, 5.306270977113050513, -7.795653906408979594 ) ) ;
#15629=CARTESIAN_POINT ( 'NONE',  ( -7.500000000000005329, 4.330127018922194537, -7.422398894150031623 ) ) ;
#15630=CARTESIAN_POINT ( 'NONE',  ( 2.131511515620586383, 3.916244202832140253, 0.8125000013655924169 ) ) ;
#15634=CARTESIAN_POINT ( 'NONE',  ( -0.5093500532425060401, -4.799145180956616130, -0.8749999986344056957 ) ) ;
#15635=CARTESIAN_POINT ( 'NONE',  ( 2.390265326283148806, 4.391654775818395251, -0.8750000000000007772 ) ) ;
#15642=ORIENTED_EDGE ( 'NONE', *, *, #5540, .F. ) ;
#15646=CARTESIAN_POINT ( 'NONE',  ( 3.033343224707661712, -3.753672977998669502, -0.7499999986344074721 ) ) ;
#15650=PLANE ( 'NONE',  #11785 ) ;
#15654=CARTESIAN_POINT ( 'NONE',  ( 4.795541693661363958, 1.415196051561583790, -8.000000000000003553 ) ) ;
#15658=CARTESIAN_POINT ( 'NONE',  ( -3.916244202832140253, 2.131511515620587272, -0.9374999986344056957 ) ) ;
#15659=ORIENTED_EDGE ( 'NONE', *, *, #400, .T. ) ;
#15661=CARTESIAN_POINT ( 'NONE',  ( 3.093533885182924159, 6.874201416486802607, -7.446478553994766436 ) ) ;
#15672=CARTESIAN_POINT ( 'NONE',  ( 4.276409079477644148, 1.261996585732577891, -7.312499998634407916 ) ) ;
#15676=CARTESIAN_POINT ( 'NONE',  ( -0.5711823568785978633, -5.381735091635035495, 0.6874999999999977796 ) ) ;
#15686=CARTESIAN_POINT ( 'NONE',  ( 5.000000000000000888, 0.000000000000000000, -9.999999999999998224 ) ) ;
#15706=CARTESIAN_POINT ( 'NONE',  ( -2.352174619735676320, 7.302225387958832137, -7.450218641349214188 ) ) ;
#15708=VERTEX_POINT ( 'NONE', #6112 ) ;
#15715=CARTESIAN_POINT ( 'NONE',  ( -4.276409079477644148, -1.261996585732578335, -0.8124999986344055847 ) ) ;
#15720=CARTESIAN_POINT ( 'NONE',  ( -0.5093500532425060401, -4.799145180956616130, -1.874999998634406584 ) ) ;
#15730=ORIENTED_EDGE ( 'NONE', *, *, #7624, .T. ) ;
#15743=CARTESIAN_POINT ( 'NONE',  ( 3.033343224707661712, -3.753672977998669946, 1.500000001365594304 ) ) ;
#15754=DIRECTION ( 'NONE',  ( 0.000000000000000000, 0.000000000000000000, 1.000000000000000000 ) ) ;
#15757=( BOUNDED_CURVE ( )  B_SPLINE_CURVE ( 2, ( #14985, #11339, #5200, #5363, #15060, #8926, #6498, #13835, #15140, #4058, #2844 ),
 .UNSPECIFIED., .F., .F. ) 
 B_SPLINE_CURVE_WITH_KNOTS ( ( 3, 2, 2, 2, 2, 3 ),
 ( 0.9045872658012773515, 0.9124999999999999778, 0.9250000000000000444, 0.9375000000000000000, 0.9499999999999999556, 0.9545872658012772849 ),
 .UNSPECIFIED. ) 
 CURVE ( )  GEOMETRIC_REPRESENTATION_ITEM ( )  RATIONAL_B_SPLINE_CURVE ( ( 0.9646335149384803742, 0.9518143178943441196, 1.000000000000000000, 0.9238795325112867385, 1.000000000000000000, 0.9238795325112867385, 1.000000000000000000, 0.9238795325112867385, 1.000000000000000000, 0.9720652146169428409, 0.9646335149384808183 ) ) 
 REPRESENTATION_ITEM ( '' )  );
#15758=CARTESIAN_POINT ( 'NONE',  ( 0.000000000000000000, 0.000000000000000000, -25.03750572909317285 ) ) ;
#15759=CARTESIAN_POINT ( 'NONE',  ( 4.795541693661363958, 1.415196051561583790, -3.000000000000002665 ) ) ;
#15761=CARTESIAN_POINT ( 'NONE',  ( 1.797450215652874217, -4.579636122706331136, -0.06122359487011186374 ) ) ;
#15766=ORIENTED_EDGE ( 'NONE', *, *, #9442, .F. ) ;
#15768=CARTESIAN_POINT ( 'NONE',  ( -10.39117206796836079, 0.000000000000000000, -8.499999999999996447 ) ) ;
#15774=DIRECTION ( 'NONE',  ( 1.000000000000000000, 0.000000000000000000, 0.000000000000000000 ) ) ;
#15781=EDGE_CURVE ( 'NONE', #15211, #2616, #10623, .T. ) ;
#15786=EDGE_LOOP ( 'NONE', ( #1653, #7726, #7435, #1800 ) ) ;
#15789=CARTESIAN_POINT ( 'NONE',  ( 3.916244202832140253, -2.131511515620588160, -1.437499998634406140 ) ) ;
#15791=CARTESIAN_POINT ( 'NONE',  ( 3.916244202832140253, -2.131511515620588160, -0.6874999986344089153 ) ) ;
#15800=ORIENTED_EDGE ( 'NONE', *, *, #4108, .F. ) ;
#15804=CARTESIAN_POINT ( 'NONE',  ( 1.261996585732578113, -4.276409079477644148, -1.812499998634406584 ) ) ;
#15810=CARTESIAN_POINT ( 'NONE',  ( -4.209348295687703967, -3.401574460001763001, -0.3124999972688167760 ) ) ;
#15816=CARTESIAN_POINT ( 'NONE',  ( -3.033343224707664376, 3.753672977998667726, -3.999999998634406140 ) ) ;
#15820=ORIENTED_EDGE ( 'NONE', *, *, #11333, .F. ) ;
#15829=CARTESIAN_POINT ( 'NONE',  ( 4.795541693661363958, 1.415196051561583790, -1.000000000000000888 ) ) ;
#15834=ADVANCED_BREP_SHAPE_REPRESENTATION ( '', ( #9140, #3223 ), #7084 ) ;
#15835=CARTESIAN_POINT ( 'NONE',  ( 1.261996585732578113, -4.276409079477644148, -0.8124999986344090264 ) ) ;
#15838=VERTEX_POINT ( 'NONE', #542 ) ;
#15845=( BOUNDED_CURVE ( )  B_SPLINE_CURVE ( 2, ( #10997, #3881, #7530, #7216, #12118, #1054, #14636, #12272, #6235, #1128, #6068 ),
 .UNSPECIFIED., .F., .F. ) 
 B_SPLINE_CURVE_WITH_KNOTS ( ( 3, 2, 2, 2, 2, 3 ),
 ( 0.7045872658012772849, 0.7125000000000000222, 0.7249999999999999778, 0.7375000000000000444, 0.7500000000000000000, 0.7545872658012773293 ),
 .UNSPECIFIED. ) 
 CURVE ( )  GEOMETRIC_REPRESENTATION_ITEM ( )  RATIONAL_B_SPLINE_CURVE ( ( 0.9646335149384808183, 0.9518143178943441196, 1.000000000000000000, 0.9238795325112867385, 1.000000000000000000, 0.9238795325112867385, 1.000000000000000000, 0.9238795325112867385, 1.000000000000000000, 0.9720652146169423968, 0.9646335149384803742 ) ) 
 REPRESENTATION_ITEM ( '' )  );
#15846=PRODUCT_DEFINITION_SHAPE ( 'NONE', 'NONE',  #6026 ) ;
#15852=CARTESIAN_POINT ( 'NONE',  ( -4.795541693661363958, -1.415196051561583790, -1.374999997268814500 ) ) ;
#15853=CARTESIAN_POINT ( 'NONE',  ( 5.274401269815137461, 6.074457022762082659, -7.633824513837106807 ) ) ;
#15856=ORIENTED_EDGE ( 'NONE', *, *, #10134, .F. ) ;
#15863=AXIS2_PLACEMENT_3D ( 'NONE', #6780, #9364, #8251 ) ;
#15864=TOROIDAL_SURFACE ( 'NONE', #2173, 10.12668159690567649, 0.7733184030943209830 ) ;
#15865=CARTESIAN_POINT ( 'NONE',  ( 5.000000000000004441, -2.247904837838113790E-16, -3.920263044861760360 ) ) ;
#15868=CARTESIAN_POINT ( 'NONE',  ( 4.799145180956616130, -0.5093500532425063732, -2.624999998634407028 ) ) ;
#15872=DIRECTION ( 'NONE',  ( -1.000000000000000000, 0.000000000000000000, 0.000000000000000000 ) ) ;
#15879=CARTESIAN_POINT ( 'NONE',  ( -3.753672977998669502, -3.033343224707661712, -4.999999998634407028 ) ) ;
#15886=CARTESIAN_POINT ( 'NONE',  ( -0.5711823568785977523, -5.381735091635034607, -2.312500000000001332 ) ) ;
#15889=CARTESIAN_POINT ( 'NONE',  ( 1.605140903214875142E-15, -8.895730773063899477, -7.917997657324742811 ) ) ;
#15892=SURFACE_STYLE_FILL_AREA ( #5868 ) ;
#15894=CARTESIAN_POINT ( 'NONE',  ( 4.276409079477644148, 1.261996585732577891, -5.312499998634406140 ) ) ;
#15910=CARTESIAN_POINT ( 'NONE',  ( -0.5711823568785978633, -5.381735091635035495, -3.312500000000001776 ) ) ;
#15915=CARTESIAN_POINT ( 'NONE',  ( -0.5093500532425060401, -4.799145180956616130, -0.8749999986344056957 ) ) ;
#15936=CARTESIAN_POINT ( 'NONE',  ( 7.500000000000003553, -4.330127018922199866, -7.422398894150035176 ) ) ;
#15950=CARTESIAN_POINT ( 'NONE',  ( 3.916244202832140253, -2.131511515620588160, 0.5625000013655921949 ) ) ;
#15952=CARTESIAN_POINT ( 'NONE',  ( -2.131511515620587272, -3.916244202832140253, -0.9374999986344056957 ) ) ;
#15955=FACE_OUTER_BOUND ( 'NONE', #1190, .T. ) ;
#15963=CARTESIAN_POINT ( 'NONE',  ( -4.799145180956616130, 0.5093500532425063732, -1.124999998634405918 ) ) ;
ENDSEC;
END-ISO-10303-21;
